ISO-10303-21;
HEADER;
/* Generated by software containing ST-Developer
 * from STEP Tools, Inc. (www.steptools.com) 
 */

FILE_DESCRIPTION(
/* description */ (''),
/* implementation_level */ '2;1');

FILE_NAME(
/* name */ 'Base (1).step',
/* time_stamp */ '2026-10-22T15:07:41+06:00',
/* author */ (''),
/* organization */ (''),
/* preprocessor_version */ 'ST-DEVELOPER v20.2',
/* originating_system */ 'Autodesk Translation Framework v15.15.0.0',
/* authorisation */ '');

FILE_SCHEMA (('AUTOMOTIVE_DESIGN { 1 0 10303 214 3 1 1 }'));
ENDSEC;

DATA;
#10=MECHANICAL_DESIGN_GEOMETRIC_PRESENTATION_REPRESENTATION('',(#2883),#19220);
#72=SHAPE_REPRESENTATION_RELATIONSHIP('SRR','None',#19275,#86);
#86=ADVANCED_BREP_SHAPE_REPRESENTATION('',(#100),#19211);
#100=MANIFOLD_SOLID_BREP('Base',#11319);
#187=FACE_BOUND('',#3774,.T.);
#188=FACE_BOUND('',#3775,.T.);
#189=FACE_BOUND('',#3776,.T.);
#190=FACE_BOUND('',#3777,.T.);
#191=FACE_BOUND('',#3778,.T.);
#192=FACE_BOUND('',#3779,.T.);
#193=FACE_BOUND('',#3780,.T.);
#194=FACE_BOUND('',#3781,.T.);
#195=FACE_BOUND('',#3782,.T.);
#196=FACE_BOUND('',#3783,.T.);
#197=FACE_BOUND('',#3784,.T.);
#198=FACE_BOUND('',#3785,.T.);
#199=FACE_BOUND('',#3786,.T.);
#200=FACE_BOUND('',#3787,.T.);
#201=FACE_BOUND('',#3788,.T.);
#202=FACE_BOUND('',#3789,.T.);
#203=FACE_BOUND('',#3790,.T.);
#204=FACE_BOUND('',#3791,.T.);
#205=FACE_BOUND('',#3792,.T.);
#206=FACE_BOUND('',#3793,.T.);
#207=FACE_BOUND('',#3794,.T.);
#208=FACE_BOUND('',#3795,.T.);
#209=FACE_BOUND('',#3796,.T.);
#210=FACE_BOUND('',#3797,.T.);
#211=FACE_BOUND('',#3798,.T.);
#212=FACE_BOUND('',#3799,.T.);
#213=FACE_BOUND('',#3800,.T.);
#214=FACE_BOUND('',#3801,.T.);
#215=FACE_BOUND('',#3802,.T.);
#216=FACE_BOUND('',#3803,.T.);
#217=FACE_BOUND('',#3804,.T.);
#218=FACE_BOUND('',#3805,.T.);
#219=FACE_BOUND('',#3806,.T.);
#220=FACE_BOUND('',#3807,.T.);
#221=FACE_BOUND('',#3808,.T.);
#222=FACE_BOUND('',#3809,.T.);
#223=FACE_BOUND('',#3810,.T.);
#224=FACE_BOUND('',#3811,.T.);
#225=FACE_BOUND('',#3812,.T.);
#226=FACE_BOUND('',#3813,.T.);
#227=FACE_BOUND('',#3814,.T.);
#228=FACE_BOUND('',#3815,.T.);
#229=FACE_BOUND('',#3816,.T.);
#230=FACE_BOUND('',#3817,.T.);
#231=FACE_BOUND('',#3818,.T.);
#232=FACE_BOUND('',#3819,.T.);
#233=FACE_BOUND('',#3820,.T.);
#234=FACE_BOUND('',#3821,.T.);
#235=FACE_BOUND('',#3822,.T.);
#236=FACE_BOUND('',#3823,.T.);
#237=FACE_BOUND('',#3824,.T.);
#238=FACE_BOUND('',#3825,.T.);
#239=FACE_BOUND('',#3826,.T.);
#240=FACE_BOUND('',#3827,.T.);
#241=FACE_BOUND('',#3828,.T.);
#242=FACE_BOUND('',#3829,.T.);
#243=FACE_BOUND('',#3830,.T.);
#244=FACE_BOUND('',#3831,.T.);
#245=FACE_BOUND('',#3832,.T.);
#246=FACE_BOUND('',#3833,.T.);
#247=FACE_BOUND('',#3834,.T.);
#248=FACE_BOUND('',#3835,.T.);
#249=FACE_BOUND('',#3836,.T.);
#250=FACE_BOUND('',#3837,.T.);
#251=FACE_BOUND('',#3838,.T.);
#252=FACE_BOUND('',#3839,.T.);
#253=FACE_BOUND('',#3840,.T.);
#254=FACE_BOUND('',#3841,.T.);
#255=FACE_BOUND('',#3842,.T.);
#256=FACE_BOUND('',#3843,.T.);
#257=FACE_BOUND('',#3846,.T.);
#258=FACE_BOUND('',#3847,.T.);
#259=FACE_BOUND('',#3848,.T.);
#260=FACE_BOUND('',#3849,.T.);
#261=FACE_BOUND('',#3850,.T.);
#262=FACE_BOUND('',#3851,.T.);
#263=FACE_BOUND('',#3852,.T.);
#264=FACE_BOUND('',#3853,.T.);
#265=FACE_BOUND('',#3854,.T.);
#266=FACE_BOUND('',#3855,.T.);
#267=FACE_BOUND('',#3856,.T.);
#268=FACE_BOUND('',#3857,.T.);
#269=FACE_BOUND('',#3858,.T.);
#270=FACE_BOUND('',#3859,.T.);
#271=FACE_BOUND('',#3860,.T.);
#272=FACE_BOUND('',#3861,.T.);
#273=FACE_BOUND('',#3862,.T.);
#274=FACE_BOUND('',#3863,.T.);
#275=FACE_BOUND('',#3864,.T.);
#276=FACE_BOUND('',#3865,.T.);
#277=FACE_BOUND('',#3866,.T.);
#278=FACE_BOUND('',#3867,.T.);
#279=FACE_BOUND('',#3868,.T.);
#280=FACE_BOUND('',#3869,.T.);
#281=FACE_BOUND('',#3870,.T.);
#282=FACE_BOUND('',#3871,.T.);
#283=FACE_BOUND('',#3872,.T.);
#284=FACE_BOUND('',#3873,.T.);
#285=FACE_BOUND('',#3874,.T.);
#286=FACE_BOUND('',#3875,.T.);
#287=FACE_BOUND('',#3876,.T.);
#288=FACE_BOUND('',#3877,.T.);
#289=FACE_BOUND('',#3878,.T.);
#290=FACE_BOUND('',#3879,.T.);
#291=FACE_BOUND('',#3880,.T.);
#292=FACE_BOUND('',#3881,.T.);
#293=FACE_BOUND('',#3882,.T.);
#294=FACE_BOUND('',#3883,.T.);
#295=FACE_BOUND('',#3884,.T.);
#296=FACE_BOUND('',#3885,.T.);
#297=FACE_BOUND('',#3886,.T.);
#298=FACE_BOUND('',#3887,.T.);
#299=FACE_BOUND('',#3888,.T.);
#300=FACE_BOUND('',#3889,.T.);
#301=FACE_BOUND('',#3890,.T.);
#302=FACE_BOUND('',#3891,.T.);
#303=FACE_BOUND('',#3892,.T.);
#304=FACE_BOUND('',#3895,.T.);
#305=FACE_BOUND('',#3896,.T.);
#306=FACE_BOUND('',#3897,.T.);
#307=FACE_BOUND('',#3898,.T.);
#308=FACE_BOUND('',#3899,.T.);
#309=FACE_BOUND('',#3900,.T.);
#310=FACE_BOUND('',#3901,.T.);
#311=FACE_BOUND('',#3902,.T.);
#312=FACE_BOUND('',#3903,.T.);
#313=FACE_BOUND('',#3904,.T.);
#314=FACE_BOUND('',#3905,.T.);
#315=FACE_BOUND('',#3906,.T.);
#316=FACE_BOUND('',#3907,.T.);
#317=FACE_BOUND('',#3908,.T.);
#318=FACE_BOUND('',#3909,.T.);
#319=FACE_BOUND('',#3910,.T.);
#320=FACE_BOUND('',#3911,.T.);
#321=FACE_BOUND('',#3912,.T.);
#322=FACE_BOUND('',#3913,.T.);
#323=FACE_BOUND('',#3914,.T.);
#324=FACE_BOUND('',#3915,.T.);
#325=FACE_BOUND('',#3916,.T.);
#326=FACE_BOUND('',#3917,.T.);
#327=FACE_BOUND('',#3918,.T.);
#328=FACE_BOUND('',#3919,.T.);
#329=FACE_BOUND('',#3920,.T.);
#330=FACE_BOUND('',#3921,.T.);
#331=FACE_BOUND('',#3922,.T.);
#332=FACE_BOUND('',#3923,.T.);
#333=FACE_BOUND('',#3924,.T.);
#334=FACE_BOUND('',#3925,.T.);
#335=FACE_BOUND('',#3926,.T.);
#336=FACE_BOUND('',#3927,.T.);
#337=FACE_BOUND('',#3928,.T.);
#338=FACE_BOUND('',#3929,.T.);
#339=FACE_BOUND('',#3930,.T.);
#340=FACE_BOUND('',#3931,.T.);
#341=FACE_BOUND('',#3932,.T.);
#342=FACE_BOUND('',#3933,.T.);
#343=FACE_BOUND('',#3934,.T.);
#344=FACE_BOUND('',#3935,.T.);
#345=FACE_BOUND('',#3936,.T.);
#346=FACE_BOUND('',#3937,.T.);
#347=FACE_BOUND('',#3938,.T.);
#348=FACE_BOUND('',#3939,.T.);
#349=FACE_BOUND('',#3940,.T.);
#350=FACE_BOUND('',#3941,.T.);
#351=FACE_BOUND('',#3942,.T.);
#352=FACE_BOUND('',#3943,.T.);
#353=FACE_BOUND('',#3944,.T.);
#354=FACE_BOUND('',#3945,.T.);
#355=FACE_BOUND('',#3946,.T.);
#356=FACE_BOUND('',#3947,.T.);
#357=FACE_BOUND('',#3948,.T.);
#358=FACE_BOUND('',#3949,.T.);
#359=FACE_BOUND('',#3950,.T.);
#360=FACE_BOUND('',#3951,.T.);
#361=FACE_BOUND('',#3952,.T.);
#362=FACE_BOUND('',#3953,.T.);
#363=FACE_BOUND('',#3954,.T.);
#364=FACE_BOUND('',#3955,.T.);
#365=FACE_BOUND('',#3956,.T.);
#366=FACE_BOUND('',#3957,.T.);
#367=FACE_BOUND('',#3958,.T.);
#368=FACE_BOUND('',#3959,.T.);
#369=FACE_BOUND('',#3960,.T.);
#370=FACE_BOUND('',#3961,.T.);
#371=FACE_BOUND('',#3962,.T.);
#372=FACE_BOUND('',#3963,.T.);
#373=FACE_BOUND('',#3964,.T.);
#374=FACE_BOUND('',#4016,.T.);
#375=FACE_BOUND('',#4017,.T.);
#376=FACE_BOUND('',#4018,.T.);
#377=FACE_BOUND('',#4019,.T.);
#378=FACE_BOUND('',#4020,.T.);
#379=FACE_BOUND('',#4021,.T.);
#380=FACE_BOUND('',#4022,.T.);
#381=FACE_BOUND('',#4023,.T.);
#382=FACE_BOUND('',#4024,.T.);
#383=FACE_BOUND('',#4025,.T.);
#384=FACE_BOUND('',#4026,.T.);
#385=FACE_BOUND('',#4027,.T.);
#386=FACE_BOUND('',#4028,.T.);
#387=FACE_BOUND('',#4029,.T.);
#388=FACE_BOUND('',#4030,.T.);
#389=FACE_BOUND('',#4031,.T.);
#390=FACE_BOUND('',#4032,.T.);
#391=FACE_BOUND('',#4033,.T.);
#392=FACE_BOUND('',#4034,.T.);
#393=FACE_BOUND('',#4035,.T.);
#394=FACE_BOUND('',#4036,.T.);
#395=FACE_BOUND('',#4037,.T.);
#396=FACE_BOUND('',#4038,.T.);
#397=FACE_BOUND('',#4039,.T.);
#398=FACE_BOUND('',#4040,.T.);
#399=FACE_BOUND('',#4041,.T.);
#400=FACE_BOUND('',#4042,.T.);
#401=FACE_BOUND('',#4043,.T.);
#402=FACE_BOUND('',#4044,.T.);
#403=FACE_BOUND('',#4045,.T.);
#404=FACE_BOUND('',#4046,.T.);
#405=FACE_BOUND('',#4047,.T.);
#406=FACE_BOUND('',#4048,.T.);
#407=FACE_BOUND('',#4049,.T.);
#408=FACE_BOUND('',#4050,.T.);
#409=FACE_BOUND('',#4051,.T.);
#410=FACE_BOUND('',#4052,.T.);
#411=FACE_BOUND('',#4053,.T.);
#412=FACE_BOUND('',#4054,.T.);
#413=FACE_BOUND('',#4055,.T.);
#414=FACE_BOUND('',#4056,.T.);
#415=FACE_BOUND('',#4057,.T.);
#416=FACE_BOUND('',#4058,.T.);
#417=FACE_BOUND('',#4059,.T.);
#418=FACE_BOUND('',#4060,.T.);
#419=FACE_BOUND('',#4061,.T.);
#420=FACE_BOUND('',#4062,.T.);
#421=FACE_BOUND('',#4113,.T.);
#422=FACE_BOUND('',#4114,.T.);
#423=FACE_BOUND('',#4115,.T.);
#424=FACE_BOUND('',#4116,.T.);
#425=FACE_BOUND('',#4117,.T.);
#426=FACE_BOUND('',#4118,.T.);
#427=FACE_BOUND('',#4119,.T.);
#428=FACE_BOUND('',#4120,.T.);
#429=FACE_BOUND('',#4121,.T.);
#430=FACE_BOUND('',#4122,.T.);
#431=FACE_BOUND('',#4123,.T.);
#432=FACE_BOUND('',#4124,.T.);
#433=FACE_BOUND('',#4125,.T.);
#434=FACE_BOUND('',#4126,.T.);
#435=FACE_BOUND('',#4127,.T.);
#436=FACE_BOUND('',#4128,.T.);
#437=FACE_BOUND('',#4129,.T.);
#438=FACE_BOUND('',#4130,.T.);
#439=FACE_BOUND('',#4131,.T.);
#440=FACE_BOUND('',#4132,.T.);
#441=FACE_BOUND('',#4133,.T.);
#442=FACE_BOUND('',#4134,.T.);
#443=FACE_BOUND('',#4135,.T.);
#444=FACE_BOUND('',#4136,.T.);
#445=FACE_BOUND('',#4137,.T.);
#446=FACE_BOUND('',#4138,.T.);
#447=FACE_BOUND('',#4139,.T.);
#448=FACE_BOUND('',#4140,.T.);
#449=FACE_BOUND('',#4141,.T.);
#450=FACE_BOUND('',#4142,.T.);
#451=FACE_BOUND('',#4143,.T.);
#452=FACE_BOUND('',#4144,.T.);
#453=FACE_BOUND('',#4145,.T.);
#454=FACE_BOUND('',#4146,.T.);
#455=FACE_BOUND('',#4147,.T.);
#456=FACE_BOUND('',#4148,.T.);
#457=FACE_BOUND('',#4149,.T.);
#458=FACE_BOUND('',#4150,.T.);
#459=FACE_BOUND('',#4151,.T.);
#460=FACE_BOUND('',#4152,.T.);
#461=FACE_BOUND('',#4153,.T.);
#462=FACE_BOUND('',#4154,.T.);
#463=FACE_BOUND('',#4155,.T.);
#464=FACE_BOUND('',#4156,.T.);
#465=FACE_BOUND('',#4157,.T.);
#466=FACE_BOUND('',#4158,.T.);
#467=FACE_BOUND('',#4159,.T.);
#468=FACE_BOUND('',#4161,.T.);
#469=FACE_BOUND('',#4162,.T.);
#470=FACE_BOUND('',#4163,.T.);
#471=FACE_BOUND('',#4164,.T.);
#472=FACE_BOUND('',#4165,.T.);
#473=FACE_BOUND('',#4166,.T.);
#474=FACE_BOUND('',#4167,.T.);
#475=FACE_BOUND('',#4168,.T.);
#476=FACE_BOUND('',#4169,.T.);
#477=FACE_BOUND('',#4170,.T.);
#478=FACE_BOUND('',#4171,.T.);
#479=FACE_BOUND('',#4172,.T.);
#480=FACE_BOUND('',#4173,.T.);
#481=FACE_BOUND('',#4174,.T.);
#482=FACE_BOUND('',#4175,.T.);
#483=FACE_BOUND('',#4176,.T.);
#484=FACE_BOUND('',#4177,.T.);
#485=FACE_BOUND('',#4178,.T.);
#486=FACE_BOUND('',#4179,.T.);
#487=FACE_BOUND('',#4180,.T.);
#488=FACE_BOUND('',#4181,.T.);
#489=FACE_BOUND('',#4182,.T.);
#490=FACE_BOUND('',#4183,.T.);
#491=FACE_BOUND('',#4184,.T.);
#492=FACE_BOUND('',#4185,.T.);
#493=FACE_BOUND('',#4186,.T.);
#494=FACE_BOUND('',#4187,.T.);
#495=FACE_BOUND('',#4188,.T.);
#496=FACE_BOUND('',#4189,.T.);
#497=FACE_BOUND('',#4190,.T.);
#498=FACE_BOUND('',#4191,.T.);
#499=FACE_BOUND('',#4192,.T.);
#500=FACE_BOUND('',#4193,.T.);
#501=FACE_BOUND('',#4194,.T.);
#502=FACE_BOUND('',#4195,.T.);
#503=FACE_BOUND('',#4196,.T.);
#504=FACE_BOUND('',#4197,.T.);
#505=FACE_BOUND('',#4198,.T.);
#506=FACE_BOUND('',#4199,.T.);
#507=FACE_BOUND('',#4200,.T.);
#508=FACE_BOUND('',#4201,.T.);
#509=FACE_BOUND('',#4202,.T.);
#510=FACE_BOUND('',#4203,.T.);
#511=FACE_BOUND('',#4204,.T.);
#512=FACE_BOUND('',#4205,.T.);
#513=FACE_BOUND('',#4206,.T.);
#514=FACE_BOUND('',#4207,.T.);
#682=PLANE('',#11775);
#683=PLANE('',#11779);
#684=PLANE('',#11783);
#685=PLANE('',#11787);
#686=PLANE('',#11806);
#687=PLANE('',#11810);
#688=PLANE('',#11814);
#689=PLANE('',#11818);
#690=PLANE('',#11837);
#691=PLANE('',#11841);
#692=PLANE('',#11845);
#693=PLANE('',#11849);
#694=PLANE('',#11868);
#695=PLANE('',#11872);
#696=PLANE('',#11876);
#697=PLANE('',#11880);
#698=PLANE('',#11899);
#699=PLANE('',#11903);
#700=PLANE('',#11907);
#701=PLANE('',#11911);
#702=PLANE('',#11930);
#703=PLANE('',#11934);
#704=PLANE('',#11938);
#705=PLANE('',#11942);
#706=PLANE('',#11961);
#707=PLANE('',#11965);
#708=PLANE('',#11969);
#709=PLANE('',#11973);
#710=PLANE('',#11992);
#711=PLANE('',#11996);
#712=PLANE('',#12000);
#713=PLANE('',#12004);
#714=PLANE('',#12023);
#715=PLANE('',#12027);
#716=PLANE('',#12031);
#717=PLANE('',#12035);
#718=PLANE('',#12045);
#719=PLANE('',#12049);
#720=PLANE('',#12053);
#721=PLANE('',#12057);
#722=PLANE('',#12073);
#723=PLANE('',#12077);
#724=PLANE('',#12128);
#725=PLANE('',#12129);
#726=PLANE('',#12227);
#727=PLANE('',#12228);
#728=PLANE('',#12370);
#729=PLANE('',#12371);
#730=PLANE('',#12372);
#731=PLANE('',#12373);
#1017=LINE('',#16746,#1872);
#1018=LINE('',#16752,#1873);
#1019=LINE('',#16758,#1874);
#1020=LINE('',#16764,#1875);
#1021=LINE('',#16770,#1876);
#1022=LINE('',#16775,#1877);
#1023=LINE('',#16777,#1878);
#1024=LINE('',#16779,#1879);
#1025=LINE('',#16780,#1880);
#1026=LINE('',#16786,#1881);
#1027=LINE('',#16789,#1882);
#1028=LINE('',#16791,#1883);
#1029=LINE('',#16792,#1884);
#1030=LINE('',#16799,#1885);
#1031=LINE('',#16801,#1886);
#1032=LINE('',#16803,#1887);
#1033=LINE('',#16804,#1888);
#1034=LINE('',#16810,#1889);
#1035=LINE('',#16813,#1890);
#1036=LINE('',#16815,#1891);
#1037=LINE('',#16816,#1892);
#1038=LINE('',#16824,#1893);
#1039=LINE('',#16830,#1894);
#1040=LINE('',#16836,#1895);
#1041=LINE('',#16842,#1896);
#1042=LINE('',#16848,#1897);
#1043=LINE('',#16853,#1898);
#1044=LINE('',#16855,#1899);
#1045=LINE('',#16857,#1900);
#1046=LINE('',#16858,#1901);
#1047=LINE('',#16864,#1902);
#1048=LINE('',#16867,#1903);
#1049=LINE('',#16869,#1904);
#1050=LINE('',#16870,#1905);
#1051=LINE('',#16877,#1906);
#1052=LINE('',#16879,#1907);
#1053=LINE('',#16881,#1908);
#1054=LINE('',#16882,#1909);
#1055=LINE('',#16888,#1910);
#1056=LINE('',#16891,#1911);
#1057=LINE('',#16893,#1912);
#1058=LINE('',#16894,#1913);
#1059=LINE('',#16902,#1914);
#1060=LINE('',#16908,#1915);
#1061=LINE('',#16914,#1916);
#1062=LINE('',#16920,#1917);
#1063=LINE('',#16926,#1918);
#1064=LINE('',#16931,#1919);
#1065=LINE('',#16933,#1920);
#1066=LINE('',#16935,#1921);
#1067=LINE('',#16936,#1922);
#1068=LINE('',#16942,#1923);
#1069=LINE('',#16945,#1924);
#1070=LINE('',#16947,#1925);
#1071=LINE('',#16948,#1926);
#1072=LINE('',#16955,#1927);
#1073=LINE('',#16957,#1928);
#1074=LINE('',#16959,#1929);
#1075=LINE('',#16960,#1930);
#1076=LINE('',#16966,#1931);
#1077=LINE('',#16969,#1932);
#1078=LINE('',#16971,#1933);
#1079=LINE('',#16972,#1934);
#1080=LINE('',#16980,#1935);
#1081=LINE('',#16986,#1936);
#1082=LINE('',#16992,#1937);
#1083=LINE('',#16998,#1938);
#1084=LINE('',#17004,#1939);
#1085=LINE('',#17009,#1940);
#1086=LINE('',#17011,#1941);
#1087=LINE('',#17013,#1942);
#1088=LINE('',#17014,#1943);
#1089=LINE('',#17020,#1944);
#1090=LINE('',#17023,#1945);
#1091=LINE('',#17025,#1946);
#1092=LINE('',#17026,#1947);
#1093=LINE('',#17033,#1948);
#1094=LINE('',#17035,#1949);
#1095=LINE('',#17037,#1950);
#1096=LINE('',#17038,#1951);
#1097=LINE('',#17044,#1952);
#1098=LINE('',#17047,#1953);
#1099=LINE('',#17049,#1954);
#1100=LINE('',#17050,#1955);
#1101=LINE('',#17058,#1956);
#1102=LINE('',#17064,#1957);
#1103=LINE('',#17070,#1958);
#1104=LINE('',#17076,#1959);
#1105=LINE('',#17082,#1960);
#1106=LINE('',#17087,#1961);
#1107=LINE('',#17089,#1962);
#1108=LINE('',#17091,#1963);
#1109=LINE('',#17092,#1964);
#1110=LINE('',#17098,#1965);
#1111=LINE('',#17101,#1966);
#1112=LINE('',#17103,#1967);
#1113=LINE('',#17104,#1968);
#1114=LINE('',#17111,#1969);
#1115=LINE('',#17113,#1970);
#1116=LINE('',#17115,#1971);
#1117=LINE('',#17116,#1972);
#1118=LINE('',#17122,#1973);
#1119=LINE('',#17125,#1974);
#1120=LINE('',#17127,#1975);
#1121=LINE('',#17128,#1976);
#1122=LINE('',#17136,#1977);
#1123=LINE('',#17142,#1978);
#1124=LINE('',#17148,#1979);
#1125=LINE('',#17154,#1980);
#1126=LINE('',#17160,#1981);
#1127=LINE('',#17165,#1982);
#1128=LINE('',#17167,#1983);
#1129=LINE('',#17169,#1984);
#1130=LINE('',#17170,#1985);
#1131=LINE('',#17176,#1986);
#1132=LINE('',#17179,#1987);
#1133=LINE('',#17181,#1988);
#1134=LINE('',#17182,#1989);
#1135=LINE('',#17189,#1990);
#1136=LINE('',#17191,#1991);
#1137=LINE('',#17193,#1992);
#1138=LINE('',#17194,#1993);
#1139=LINE('',#17200,#1994);
#1140=LINE('',#17203,#1995);
#1141=LINE('',#17205,#1996);
#1142=LINE('',#17206,#1997);
#1143=LINE('',#17214,#1998);
#1144=LINE('',#17220,#1999);
#1145=LINE('',#17226,#2000);
#1146=LINE('',#17232,#2001);
#1147=LINE('',#17238,#2002);
#1148=LINE('',#17243,#2003);
#1149=LINE('',#17245,#2004);
#1150=LINE('',#17247,#2005);
#1151=LINE('',#17248,#2006);
#1152=LINE('',#17254,#2007);
#1153=LINE('',#17257,#2008);
#1154=LINE('',#17259,#2009);
#1155=LINE('',#17260,#2010);
#1156=LINE('',#17267,#2011);
#1157=LINE('',#17269,#2012);
#1158=LINE('',#17271,#2013);
#1159=LINE('',#17272,#2014);
#1160=LINE('',#17278,#2015);
#1161=LINE('',#17281,#2016);
#1162=LINE('',#17283,#2017);
#1163=LINE('',#17284,#2018);
#1164=LINE('',#17292,#2019);
#1165=LINE('',#17298,#2020);
#1166=LINE('',#17304,#2021);
#1167=LINE('',#17310,#2022);
#1168=LINE('',#17316,#2023);
#1169=LINE('',#17321,#2024);
#1170=LINE('',#17323,#2025);
#1171=LINE('',#17325,#2026);
#1172=LINE('',#17326,#2027);
#1173=LINE('',#17332,#2028);
#1174=LINE('',#17335,#2029);
#1175=LINE('',#17337,#2030);
#1176=LINE('',#17338,#2031);
#1177=LINE('',#17345,#2032);
#1178=LINE('',#17347,#2033);
#1179=LINE('',#17349,#2034);
#1180=LINE('',#17350,#2035);
#1181=LINE('',#17356,#2036);
#1182=LINE('',#17359,#2037);
#1183=LINE('',#17361,#2038);
#1184=LINE('',#17362,#2039);
#1185=LINE('',#17370,#2040);
#1186=LINE('',#17376,#2041);
#1187=LINE('',#17382,#2042);
#1188=LINE('',#17388,#2043);
#1189=LINE('',#17394,#2044);
#1190=LINE('',#17399,#2045);
#1191=LINE('',#17401,#2046);
#1192=LINE('',#17403,#2047);
#1193=LINE('',#17404,#2048);
#1194=LINE('',#17410,#2049);
#1195=LINE('',#17413,#2050);
#1196=LINE('',#17415,#2051);
#1197=LINE('',#17416,#2052);
#1198=LINE('',#17423,#2053);
#1199=LINE('',#17425,#2054);
#1200=LINE('',#17427,#2055);
#1201=LINE('',#17428,#2056);
#1202=LINE('',#17434,#2057);
#1203=LINE('',#17437,#2058);
#1204=LINE('',#17439,#2059);
#1205=LINE('',#17440,#2060);
#1206=LINE('',#17448,#2061);
#1207=LINE('',#17454,#2062);
#1208=LINE('',#17459,#2063);
#1209=LINE('',#17461,#2064);
#1210=LINE('',#17463,#2065);
#1211=LINE('',#17464,#2066);
#1212=LINE('',#17470,#2067);
#1213=LINE('',#17473,#2068);
#1214=LINE('',#17475,#2069);
#1215=LINE('',#17476,#2070);
#1216=LINE('',#17483,#2071);
#1217=LINE('',#17485,#2072);
#1218=LINE('',#17487,#2073);
#1219=LINE('',#17488,#2074);
#1220=LINE('',#17494,#2075);
#1221=LINE('',#17497,#2076);
#1222=LINE('',#17499,#2077);
#1223=LINE('',#17500,#2078);
#1224=LINE('',#17508,#2079);
#1225=LINE('',#17514,#2080);
#1226=LINE('',#17520,#2081);
#1227=LINE('',#17527,#2082);
#1228=LINE('',#17530,#2083);
#1229=LINE('',#17533,#2084);
#1230=LINE('',#17535,#2085);
#1231=LINE('',#17536,#2086);
#1232=LINE('',#17541,#2087);
#1233=LINE('',#17545,#2088);
#1234=LINE('',#17547,#2089);
#1235=LINE('',#17548,#2090);
#1236=LINE('',#17648,#2091);
#1237=LINE('',#17651,#2092);
#1238=LINE('',#17654,#2093);
#1239=LINE('',#17656,#2094);
#1240=LINE('',#17657,#2095);
#1241=LINE('',#17660,#2096);
#1242=LINE('',#17661,#2097);
#1243=LINE('',#17663,#2098);
#1244=LINE('',#17665,#2099);
#1245=LINE('',#17667,#2100);
#1246=LINE('',#17672,#2101);
#1247=LINE('',#17676,#2102);
#1248=LINE('',#17680,#2103);
#1249=LINE('',#17684,#2104);
#1250=LINE('',#17688,#2105);
#1251=LINE('',#17692,#2106);
#1252=LINE('',#17696,#2107);
#1253=LINE('',#17700,#2108);
#1254=LINE('',#17704,#2109);
#1255=LINE('',#17708,#2110);
#1256=LINE('',#17712,#2111);
#1257=LINE('',#17716,#2112);
#1258=LINE('',#17720,#2113);
#1259=LINE('',#17724,#2114);
#1260=LINE('',#17728,#2115);
#1261=LINE('',#17732,#2116);
#1262=LINE('',#17736,#2117);
#1263=LINE('',#17740,#2118);
#1264=LINE('',#17744,#2119);
#1265=LINE('',#17748,#2120);
#1266=LINE('',#17752,#2121);
#1267=LINE('',#17756,#2122);
#1268=LINE('',#17760,#2123);
#1269=LINE('',#17764,#2124);
#1270=LINE('',#17768,#2125);
#1271=LINE('',#17772,#2126);
#1272=LINE('',#17776,#2127);
#1273=LINE('',#17780,#2128);
#1274=LINE('',#17784,#2129);
#1275=LINE('',#17788,#2130);
#1276=LINE('',#17792,#2131);
#1277=LINE('',#17796,#2132);
#1278=LINE('',#17800,#2133);
#1279=LINE('',#17804,#2134);
#1280=LINE('',#17808,#2135);
#1281=LINE('',#17812,#2136);
#1282=LINE('',#17816,#2137);
#1283=LINE('',#17820,#2138);
#1284=LINE('',#17824,#2139);
#1285=LINE('',#17828,#2140);
#1286=LINE('',#17832,#2141);
#1287=LINE('',#17836,#2142);
#1288=LINE('',#17840,#2143);
#1289=LINE('',#17844,#2144);
#1290=LINE('',#17848,#2145);
#1291=LINE('',#17852,#2146);
#1292=LINE('',#17856,#2147);
#1293=LINE('',#17860,#2148);
#1294=LINE('',#17863,#2149);
#1295=LINE('',#17864,#2150);
#1296=LINE('',#17866,#2151);
#1297=LINE('',#17871,#2152);
#1298=LINE('',#17877,#2153);
#1299=LINE('',#17883,#2154);
#1300=LINE('',#17889,#2155);
#1301=LINE('',#17895,#2156);
#1302=LINE('',#17901,#2157);
#1303=LINE('',#17907,#2158);
#1304=LINE('',#17913,#2159);
#1305=LINE('',#17919,#2160);
#1306=LINE('',#17925,#2161);
#1307=LINE('',#17931,#2162);
#1308=LINE('',#17937,#2163);
#1309=LINE('',#17943,#2164);
#1310=LINE('',#17949,#2165);
#1311=LINE('',#17955,#2166);
#1312=LINE('',#17961,#2167);
#1313=LINE('',#17967,#2168);
#1314=LINE('',#17973,#2169);
#1315=LINE('',#17979,#2170);
#1316=LINE('',#17985,#2171);
#1317=LINE('',#17991,#2172);
#1318=LINE('',#17997,#2173);
#1319=LINE('',#18003,#2174);
#1320=LINE('',#18009,#2175);
#1321=LINE('',#18015,#2176);
#1322=LINE('',#18021,#2177);
#1323=LINE('',#18027,#2178);
#1324=LINE('',#18033,#2179);
#1325=LINE('',#18039,#2180);
#1326=LINE('',#18045,#2181);
#1327=LINE('',#18051,#2182);
#1328=LINE('',#18057,#2183);
#1329=LINE('',#18063,#2184);
#1330=LINE('',#18069,#2185);
#1331=LINE('',#18075,#2186);
#1332=LINE('',#18081,#2187);
#1333=LINE('',#18087,#2188);
#1334=LINE('',#18093,#2189);
#1335=LINE('',#18099,#2190);
#1336=LINE('',#18105,#2191);
#1337=LINE('',#18111,#2192);
#1338=LINE('',#18117,#2193);
#1339=LINE('',#18123,#2194);
#1340=LINE('',#18129,#2195);
#1341=LINE('',#18135,#2196);
#1342=LINE('',#18141,#2197);
#1343=LINE('',#18147,#2198);
#1344=LINE('',#18151,#2199);
#1345=LINE('',#18153,#2200);
#1346=LINE('',#18154,#2201);
#1347=LINE('',#18156,#2202);
#1348=LINE('',#18157,#2203);
#1872=VECTOR('',#13464,2.5);
#1873=VECTOR('',#13471,2.5);
#1874=VECTOR('',#13478,2.5);
#1875=VECTOR('',#13485,2.5);
#1876=VECTOR('',#13492,10.);
#1877=VECTOR('',#13497,10.);
#1878=VECTOR('',#13498,10.);
#1879=VECTOR('',#13499,10.);
#1880=VECTOR('',#13500,10.);
#1881=VECTOR('',#13507,10.);
#1882=VECTOR('',#13510,10.);
#1883=VECTOR('',#13511,10.);
#1884=VECTOR('',#13512,10.);
#1885=VECTOR('',#13521,10.);
#1886=VECTOR('',#13522,10.);
#1887=VECTOR('',#13523,10.);
#1888=VECTOR('',#13524,10.);
#1889=VECTOR('',#13531,10.);
#1890=VECTOR('',#13534,10.);
#1891=VECTOR('',#13535,10.);
#1892=VECTOR('',#13536,10.);
#1893=VECTOR('',#13547,2.5);
#1894=VECTOR('',#13554,2.5);
#1895=VECTOR('',#13561,2.5);
#1896=VECTOR('',#13568,2.5);
#1897=VECTOR('',#13575,10.);
#1898=VECTOR('',#13580,10.);
#1899=VECTOR('',#13581,10.);
#1900=VECTOR('',#13582,10.);
#1901=VECTOR('',#13583,10.);
#1902=VECTOR('',#13590,10.);
#1903=VECTOR('',#13593,10.);
#1904=VECTOR('',#13594,10.);
#1905=VECTOR('',#13595,10.);
#1906=VECTOR('',#13604,10.);
#1907=VECTOR('',#13605,10.);
#1908=VECTOR('',#13606,10.);
#1909=VECTOR('',#13607,10.);
#1910=VECTOR('',#13614,10.);
#1911=VECTOR('',#13617,10.);
#1912=VECTOR('',#13618,10.);
#1913=VECTOR('',#13619,10.);
#1914=VECTOR('',#13630,2.5);
#1915=VECTOR('',#13637,2.5);
#1916=VECTOR('',#13644,2.5);
#1917=VECTOR('',#13651,2.5);
#1918=VECTOR('',#13658,10.);
#1919=VECTOR('',#13663,10.);
#1920=VECTOR('',#13664,10.);
#1921=VECTOR('',#13665,10.);
#1922=VECTOR('',#13666,10.);
#1923=VECTOR('',#13673,10.);
#1924=VECTOR('',#13676,10.);
#1925=VECTOR('',#13677,10.);
#1926=VECTOR('',#13678,10.);
#1927=VECTOR('',#13687,10.);
#1928=VECTOR('',#13688,10.);
#1929=VECTOR('',#13689,10.);
#1930=VECTOR('',#13690,10.);
#1931=VECTOR('',#13697,10.);
#1932=VECTOR('',#13700,10.);
#1933=VECTOR('',#13701,10.);
#1934=VECTOR('',#13702,10.);
#1935=VECTOR('',#13713,2.5);
#1936=VECTOR('',#13720,2.5);
#1937=VECTOR('',#13727,2.5);
#1938=VECTOR('',#13734,2.5);
#1939=VECTOR('',#13741,10.);
#1940=VECTOR('',#13746,10.);
#1941=VECTOR('',#13747,10.);
#1942=VECTOR('',#13748,10.);
#1943=VECTOR('',#13749,10.);
#1944=VECTOR('',#13756,10.);
#1945=VECTOR('',#13759,10.);
#1946=VECTOR('',#13760,10.);
#1947=VECTOR('',#13761,10.);
#1948=VECTOR('',#13770,10.);
#1949=VECTOR('',#13771,10.);
#1950=VECTOR('',#13772,10.);
#1951=VECTOR('',#13773,10.);
#1952=VECTOR('',#13780,10.);
#1953=VECTOR('',#13783,10.);
#1954=VECTOR('',#13784,10.);
#1955=VECTOR('',#13785,10.);
#1956=VECTOR('',#13796,2.5);
#1957=VECTOR('',#13803,2.5);
#1958=VECTOR('',#13810,2.5);
#1959=VECTOR('',#13817,2.5);
#1960=VECTOR('',#13824,10.);
#1961=VECTOR('',#13829,10.);
#1962=VECTOR('',#13830,10.);
#1963=VECTOR('',#13831,10.);
#1964=VECTOR('',#13832,10.);
#1965=VECTOR('',#13839,10.);
#1966=VECTOR('',#13842,10.);
#1967=VECTOR('',#13843,10.);
#1968=VECTOR('',#13844,10.);
#1969=VECTOR('',#13853,10.);
#1970=VECTOR('',#13854,10.);
#1971=VECTOR('',#13855,10.);
#1972=VECTOR('',#13856,10.);
#1973=VECTOR('',#13863,10.);
#1974=VECTOR('',#13866,10.);
#1975=VECTOR('',#13867,10.);
#1976=VECTOR('',#13868,10.);
#1977=VECTOR('',#13879,2.5);
#1978=VECTOR('',#13886,2.5);
#1979=VECTOR('',#13893,2.5);
#1980=VECTOR('',#13900,2.5);
#1981=VECTOR('',#13907,10.);
#1982=VECTOR('',#13912,10.);
#1983=VECTOR('',#13913,10.);
#1984=VECTOR('',#13914,10.);
#1985=VECTOR('',#13915,10.);
#1986=VECTOR('',#13922,10.);
#1987=VECTOR('',#13925,10.);
#1988=VECTOR('',#13926,10.);
#1989=VECTOR('',#13927,10.);
#1990=VECTOR('',#13936,10.);
#1991=VECTOR('',#13937,10.);
#1992=VECTOR('',#13938,10.);
#1993=VECTOR('',#13939,10.);
#1994=VECTOR('',#13946,10.);
#1995=VECTOR('',#13949,10.);
#1996=VECTOR('',#13950,10.);
#1997=VECTOR('',#13951,10.);
#1998=VECTOR('',#13962,2.5);
#1999=VECTOR('',#13969,2.5);
#2000=VECTOR('',#13976,2.5);
#2001=VECTOR('',#13983,2.5);
#2002=VECTOR('',#13990,10.);
#2003=VECTOR('',#13995,10.);
#2004=VECTOR('',#13996,10.);
#2005=VECTOR('',#13997,10.);
#2006=VECTOR('',#13998,10.);
#2007=VECTOR('',#14005,10.);
#2008=VECTOR('',#14008,10.);
#2009=VECTOR('',#14009,10.);
#2010=VECTOR('',#14010,10.);
#2011=VECTOR('',#14019,10.);
#2012=VECTOR('',#14020,10.);
#2013=VECTOR('',#14021,10.);
#2014=VECTOR('',#14022,10.);
#2015=VECTOR('',#14029,10.);
#2016=VECTOR('',#14032,10.);
#2017=VECTOR('',#14033,10.);
#2018=VECTOR('',#14034,10.);
#2019=VECTOR('',#14045,2.5);
#2020=VECTOR('',#14052,2.5);
#2021=VECTOR('',#14059,2.5);
#2022=VECTOR('',#14066,2.5);
#2023=VECTOR('',#14073,10.);
#2024=VECTOR('',#14078,10.);
#2025=VECTOR('',#14079,10.);
#2026=VECTOR('',#14080,10.);
#2027=VECTOR('',#14081,10.);
#2028=VECTOR('',#14088,10.);
#2029=VECTOR('',#14091,10.);
#2030=VECTOR('',#14092,10.);
#2031=VECTOR('',#14093,10.);
#2032=VECTOR('',#14102,10.);
#2033=VECTOR('',#14103,10.);
#2034=VECTOR('',#14104,10.);
#2035=VECTOR('',#14105,10.);
#2036=VECTOR('',#14112,10.);
#2037=VECTOR('',#14115,10.);
#2038=VECTOR('',#14116,10.);
#2039=VECTOR('',#14117,10.);
#2040=VECTOR('',#14128,2.5);
#2041=VECTOR('',#14135,2.5);
#2042=VECTOR('',#14142,2.5);
#2043=VECTOR('',#14149,2.5);
#2044=VECTOR('',#14156,10.);
#2045=VECTOR('',#14161,10.);
#2046=VECTOR('',#14162,10.);
#2047=VECTOR('',#14163,10.);
#2048=VECTOR('',#14164,10.);
#2049=VECTOR('',#14171,10.);
#2050=VECTOR('',#14174,10.);
#2051=VECTOR('',#14175,10.);
#2052=VECTOR('',#14176,10.);
#2053=VECTOR('',#14185,10.);
#2054=VECTOR('',#14186,10.);
#2055=VECTOR('',#14187,10.);
#2056=VECTOR('',#14188,10.);
#2057=VECTOR('',#14195,10.);
#2058=VECTOR('',#14198,10.);
#2059=VECTOR('',#14199,10.);
#2060=VECTOR('',#14200,10.);
#2061=VECTOR('',#14211,2.5);
#2062=VECTOR('',#14218,2.5);
#2063=VECTOR('',#14223,10.);
#2064=VECTOR('',#14224,10.);
#2065=VECTOR('',#14225,10.);
#2066=VECTOR('',#14226,10.);
#2067=VECTOR('',#14233,10.);
#2068=VECTOR('',#14236,10.);
#2069=VECTOR('',#14237,10.);
#2070=VECTOR('',#14238,10.);
#2071=VECTOR('',#14247,10.);
#2072=VECTOR('',#14248,10.);
#2073=VECTOR('',#14249,10.);
#2074=VECTOR('',#14250,10.);
#2075=VECTOR('',#14257,10.);
#2076=VECTOR('',#14260,10.);
#2077=VECTOR('',#14261,10.);
#2078=VECTOR('',#14262,10.);
#2079=VECTOR('',#14273,10.);
#2080=VECTOR('',#14280,2.5);
#2081=VECTOR('',#14287,2.5);
#2082=VECTOR('',#14294,10.);
#2083=VECTOR('',#14297,10.);
#2084=VECTOR('',#14300,10.);
#2085=VECTOR('',#14301,10.);
#2086=VECTOR('',#14302,10.);
#2087=VECTOR('',#14307,10.);
#2088=VECTOR('',#14312,10.);
#2089=VECTOR('',#14313,10.);
#2090=VECTOR('',#14314,10.);
#2091=VECTOR('',#14413,10.);
#2092=VECTOR('',#14416,10.);
#2093=VECTOR('',#14419,10.);
#2094=VECTOR('',#14420,10.);
#2095=VECTOR('',#14421,10.);
#2096=VECTOR('',#14424,10.);
#2097=VECTOR('',#14425,10.);
#2098=VECTOR('',#14426,10.);
#2099=VECTOR('',#14427,10.);
#2100=VECTOR('',#14428,10.);
#2101=VECTOR('',#14435,10.);
#2102=VECTOR('',#14440,2.);
#2103=VECTOR('',#14445,1.99999999999999);
#2104=VECTOR('',#14450,2.00000000000003);
#2105=VECTOR('',#14455,1.99999999999999);
#2106=VECTOR('',#14460,2.00000000000003);
#2107=VECTOR('',#14465,2.);
#2108=VECTOR('',#14470,1.99999999999999);
#2109=VECTOR('',#14475,1.99999999999999);
#2110=VECTOR('',#14480,1.99999999999999);
#2111=VECTOR('',#14485,1.99999999999999);
#2112=VECTOR('',#14490,1.99999999999999);
#2113=VECTOR('',#14495,1.99999999999999);
#2114=VECTOR('',#14500,2.);
#2115=VECTOR('',#14505,1.99999999999999);
#2116=VECTOR('',#14510,1.99999999999999);
#2117=VECTOR('',#14515,1.99999999999999);
#2118=VECTOR('',#14520,1.99999999999999);
#2119=VECTOR('',#14525,2.);
#2120=VECTOR('',#14530,2.);
#2121=VECTOR('',#14535,2.00000000000003);
#2122=VECTOR('',#14540,2.);
#2123=VECTOR('',#14545,1.99999999999999);
#2124=VECTOR('',#14550,2.);
#2125=VECTOR('',#14555,1.99999999999999);
#2126=VECTOR('',#14560,1.99999999999999);
#2127=VECTOR('',#14565,1.99999999999999);
#2128=VECTOR('',#14570,1.99999999999999);
#2129=VECTOR('',#14575,1.99999999999999);
#2130=VECTOR('',#14580,1.99999999999999);
#2131=VECTOR('',#14585,1.99999999999999);
#2132=VECTOR('',#14590,2.);
#2133=VECTOR('',#14595,2.00000000000003);
#2134=VECTOR('',#14600,1.99999999999999);
#2135=VECTOR('',#14605,1.99999999999999);
#2136=VECTOR('',#14610,1.99999999999999);
#2137=VECTOR('',#14615,1.99999999999999);
#2138=VECTOR('',#14620,2.);
#2139=VECTOR('',#14625,2.00000000000003);
#2140=VECTOR('',#14630,2.00000000000003);
#2141=VECTOR('',#14635,2.00000000000003);
#2142=VECTOR('',#14640,1.99999999999999);
#2143=VECTOR('',#14645,1.99999999999999);
#2144=VECTOR('',#14650,1.99999999999999);
#2145=VECTOR('',#14655,2.00000000000003);
#2146=VECTOR('',#14660,1.99999999999999);
#2147=VECTOR('',#14665,1.99999999999999);
#2148=VECTOR('',#14670,1.99999999999999);
#2149=VECTOR('',#14673,10.);
#2150=VECTOR('',#14674,10.);
#2151=VECTOR('',#14677,10.);
#2152=VECTOR('',#14682,2.);
#2153=VECTOR('',#14689,1.99999999999999);
#2154=VECTOR('',#14696,2.00000000000003);
#2155=VECTOR('',#14703,1.99999999999999);
#2156=VECTOR('',#14710,2.00000000000003);
#2157=VECTOR('',#14717,2.);
#2158=VECTOR('',#14724,1.99999999999999);
#2159=VECTOR('',#14731,1.99999999999999);
#2160=VECTOR('',#14738,1.99999999999999);
#2161=VECTOR('',#14745,1.99999999999999);
#2162=VECTOR('',#14752,1.99999999999999);
#2163=VECTOR('',#14759,1.99999999999999);
#2164=VECTOR('',#14766,2.);
#2165=VECTOR('',#14773,1.99999999999999);
#2166=VECTOR('',#14780,1.99999999999999);
#2167=VECTOR('',#14787,1.99999999999999);
#2168=VECTOR('',#14794,1.99999999999999);
#2169=VECTOR('',#14801,2.);
#2170=VECTOR('',#14808,2.);
#2171=VECTOR('',#14815,2.00000000000003);
#2172=VECTOR('',#14822,2.);
#2173=VECTOR('',#14829,1.99999999999999);
#2174=VECTOR('',#14836,2.);
#2175=VECTOR('',#14843,1.99999999999999);
#2176=VECTOR('',#14850,1.99999999999999);
#2177=VECTOR('',#14857,1.99999999999999);
#2178=VECTOR('',#14864,1.99999999999999);
#2179=VECTOR('',#14871,1.99999999999999);
#2180=VECTOR('',#14878,1.99999999999999);
#2181=VECTOR('',#14885,1.99999999999999);
#2182=VECTOR('',#14892,2.);
#2183=VECTOR('',#14899,2.00000000000003);
#2184=VECTOR('',#14906,1.99999999999999);
#2185=VECTOR('',#14913,1.99999999999999);
#2186=VECTOR('',#14920,1.99999999999999);
#2187=VECTOR('',#14927,1.99999999999999);
#2188=VECTOR('',#14934,2.);
#2189=VECTOR('',#14941,2.00000000000003);
#2190=VECTOR('',#14948,2.00000000000003);
#2191=VECTOR('',#14955,2.00000000000003);
#2192=VECTOR('',#14962,1.99999999999999);
#2193=VECTOR('',#14969,1.99999999999999);
#2194=VECTOR('',#14976,1.99999999999999);
#2195=VECTOR('',#14983,2.00000000000003);
#2196=VECTOR('',#14990,1.99999999999999);
#2197=VECTOR('',#14997,1.99999999999999);
#2198=VECTOR('',#15004,1.99999999999999);
#2199=VECTOR('',#15009,10.);
#2200=VECTOR('',#15010,10.);
#2201=VECTOR('',#15011,10.);
#2202=VECTOR('',#15014,10.);
#2203=VECTOR('',#15015,10.);
#2613=CYLINDRICAL_SURFACE('',#11760,2.5);
#2614=CYLINDRICAL_SURFACE('',#11763,2.5);
#2615=CYLINDRICAL_SURFACE('',#11766,2.5);
#2616=CYLINDRICAL_SURFACE('',#11769,2.5);
#2617=CYLINDRICAL_SURFACE('',#11772,10.);
#2618=CYLINDRICAL_SURFACE('',#11776,1.5);
#2619=CYLINDRICAL_SURFACE('',#11780,1.5);
#2620=CYLINDRICAL_SURFACE('',#11784,1.5);
#2621=CYLINDRICAL_SURFACE('',#11788,1.5);
#2622=CYLINDRICAL_SURFACE('',#11791,2.5);
#2623=CYLINDRICAL_SURFACE('',#11794,2.5);
#2624=CYLINDRICAL_SURFACE('',#11797,2.5);
#2625=CYLINDRICAL_SURFACE('',#11800,2.5);
#2626=CYLINDRICAL_SURFACE('',#11803,10.);
#2627=CYLINDRICAL_SURFACE('',#11807,1.5);
#2628=CYLINDRICAL_SURFACE('',#11811,1.5);
#2629=CYLINDRICAL_SURFACE('',#11815,1.5);
#2630=CYLINDRICAL_SURFACE('',#11819,1.5);
#2631=CYLINDRICAL_SURFACE('',#11822,2.5);
#2632=CYLINDRICAL_SURFACE('',#11825,2.5);
#2633=CYLINDRICAL_SURFACE('',#11828,2.5);
#2634=CYLINDRICAL_SURFACE('',#11831,2.5);
#2635=CYLINDRICAL_SURFACE('',#11834,10.);
#2636=CYLINDRICAL_SURFACE('',#11838,1.5);
#2637=CYLINDRICAL_SURFACE('',#11842,1.5);
#2638=CYLINDRICAL_SURFACE('',#11846,1.5);
#2639=CYLINDRICAL_SURFACE('',#11850,1.5);
#2640=CYLINDRICAL_SURFACE('',#11853,2.5);
#2641=CYLINDRICAL_SURFACE('',#11856,2.5);
#2642=CYLINDRICAL_SURFACE('',#11859,2.5);
#2643=CYLINDRICAL_SURFACE('',#11862,2.5);
#2644=CYLINDRICAL_SURFACE('',#11865,10.);
#2645=CYLINDRICAL_SURFACE('',#11869,1.5);
#2646=CYLINDRICAL_SURFACE('',#11873,1.5);
#2647=CYLINDRICAL_SURFACE('',#11877,1.5);
#2648=CYLINDRICAL_SURFACE('',#11881,1.5);
#2649=CYLINDRICAL_SURFACE('',#11884,2.5);
#2650=CYLINDRICAL_SURFACE('',#11887,2.5);
#2651=CYLINDRICAL_SURFACE('',#11890,2.5);
#2652=CYLINDRICAL_SURFACE('',#11893,2.5);
#2653=CYLINDRICAL_SURFACE('',#11896,10.);
#2654=CYLINDRICAL_SURFACE('',#11900,1.5);
#2655=CYLINDRICAL_SURFACE('',#11904,1.5);
#2656=CYLINDRICAL_SURFACE('',#11908,1.5);
#2657=CYLINDRICAL_SURFACE('',#11912,1.5);
#2658=CYLINDRICAL_SURFACE('',#11915,2.5);
#2659=CYLINDRICAL_SURFACE('',#11918,2.5);
#2660=CYLINDRICAL_SURFACE('',#11921,2.5);
#2661=CYLINDRICAL_SURFACE('',#11924,2.5);
#2662=CYLINDRICAL_SURFACE('',#11927,10.);
#2663=CYLINDRICAL_SURFACE('',#11931,1.5);
#2664=CYLINDRICAL_SURFACE('',#11935,1.5);
#2665=CYLINDRICAL_SURFACE('',#11939,1.5);
#2666=CYLINDRICAL_SURFACE('',#11943,1.5);
#2667=CYLINDRICAL_SURFACE('',#11946,2.5);
#2668=CYLINDRICAL_SURFACE('',#11949,2.5);
#2669=CYLINDRICAL_SURFACE('',#11952,2.5);
#2670=CYLINDRICAL_SURFACE('',#11955,2.5);
#2671=CYLINDRICAL_SURFACE('',#11958,10.);
#2672=CYLINDRICAL_SURFACE('',#11962,1.5);
#2673=CYLINDRICAL_SURFACE('',#11966,1.5);
#2674=CYLINDRICAL_SURFACE('',#11970,1.5);
#2675=CYLINDRICAL_SURFACE('',#11974,1.5);
#2676=CYLINDRICAL_SURFACE('',#11977,2.5);
#2677=CYLINDRICAL_SURFACE('',#11980,2.5);
#2678=CYLINDRICAL_SURFACE('',#11983,2.5);
#2679=CYLINDRICAL_SURFACE('',#11986,2.5);
#2680=CYLINDRICAL_SURFACE('',#11989,10.);
#2681=CYLINDRICAL_SURFACE('',#11993,1.5);
#2682=CYLINDRICAL_SURFACE('',#11997,1.5);
#2683=CYLINDRICAL_SURFACE('',#12001,1.5);
#2684=CYLINDRICAL_SURFACE('',#12005,1.5);
#2685=CYLINDRICAL_SURFACE('',#12008,2.5);
#2686=CYLINDRICAL_SURFACE('',#12011,2.5);
#2687=CYLINDRICAL_SURFACE('',#12014,2.5);
#2688=CYLINDRICAL_SURFACE('',#12017,2.5);
#2689=CYLINDRICAL_SURFACE('',#12020,10.);
#2690=CYLINDRICAL_SURFACE('',#12024,1.5);
#2691=CYLINDRICAL_SURFACE('',#12028,1.5);
#2692=CYLINDRICAL_SURFACE('',#12032,1.5);
#2693=CYLINDRICAL_SURFACE('',#12036,1.5);
#2694=CYLINDRICAL_SURFACE('',#12039,2.5);
#2695=CYLINDRICAL_SURFACE('',#12042,2.5);
#2696=CYLINDRICAL_SURFACE('',#12046,1.5);
#2697=CYLINDRICAL_SURFACE('',#12050,1.5);
#2698=CYLINDRICAL_SURFACE('',#12054,1.5);
#2699=CYLINDRICAL_SURFACE('',#12058,1.5);
#2700=CYLINDRICAL_SURFACE('',#12061,10.);
#2701=CYLINDRICAL_SURFACE('',#12064,2.5);
#2702=CYLINDRICAL_SURFACE('',#12067,2.5);
#2703=CYLINDRICAL_SURFACE('',#12070,0.5);
#2704=CYLINDRICAL_SURFACE('',#12074,0.5);
#2705=CYLINDRICAL_SURFACE('',#12125,2.);
#2706=CYLINDRICAL_SURFACE('',#12131,2.);
#2707=CYLINDRICAL_SURFACE('',#12133,2.);
#2708=CYLINDRICAL_SURFACE('',#12135,1.99999999999999);
#2709=CYLINDRICAL_SURFACE('',#12137,2.00000000000003);
#2710=CYLINDRICAL_SURFACE('',#12139,1.99999999999999);
#2711=CYLINDRICAL_SURFACE('',#12141,2.00000000000003);
#2712=CYLINDRICAL_SURFACE('',#12143,2.);
#2713=CYLINDRICAL_SURFACE('',#12145,1.99999999999999);
#2714=CYLINDRICAL_SURFACE('',#12147,1.99999999999999);
#2715=CYLINDRICAL_SURFACE('',#12149,1.99999999999999);
#2716=CYLINDRICAL_SURFACE('',#12151,1.99999999999999);
#2717=CYLINDRICAL_SURFACE('',#12153,1.99999999999999);
#2718=CYLINDRICAL_SURFACE('',#12155,1.99999999999999);
#2719=CYLINDRICAL_SURFACE('',#12157,2.);
#2720=CYLINDRICAL_SURFACE('',#12159,1.99999999999999);
#2721=CYLINDRICAL_SURFACE('',#12161,1.99999999999999);
#2722=CYLINDRICAL_SURFACE('',#12163,1.99999999999999);
#2723=CYLINDRICAL_SURFACE('',#12165,1.99999999999999);
#2724=CYLINDRICAL_SURFACE('',#12167,2.);
#2725=CYLINDRICAL_SURFACE('',#12169,2.);
#2726=CYLINDRICAL_SURFACE('',#12171,2.00000000000003);
#2727=CYLINDRICAL_SURFACE('',#12173,2.);
#2728=CYLINDRICAL_SURFACE('',#12175,1.99999999999999);
#2729=CYLINDRICAL_SURFACE('',#12177,2.);
#2730=CYLINDRICAL_SURFACE('',#12179,1.99999999999999);
#2731=CYLINDRICAL_SURFACE('',#12181,1.99999999999999);
#2732=CYLINDRICAL_SURFACE('',#12183,1.99999999999999);
#2733=CYLINDRICAL_SURFACE('',#12185,1.99999999999999);
#2734=CYLINDRICAL_SURFACE('',#12187,1.99999999999999);
#2735=CYLINDRICAL_SURFACE('',#12189,1.99999999999999);
#2736=CYLINDRICAL_SURFACE('',#12191,1.99999999999999);
#2737=CYLINDRICAL_SURFACE('',#12193,2.);
#2738=CYLINDRICAL_SURFACE('',#12195,2.00000000000003);
#2739=CYLINDRICAL_SURFACE('',#12197,1.99999999999999);
#2740=CYLINDRICAL_SURFACE('',#12199,1.99999999999999);
#2741=CYLINDRICAL_SURFACE('',#12201,1.99999999999999);
#2742=CYLINDRICAL_SURFACE('',#12203,1.99999999999999);
#2743=CYLINDRICAL_SURFACE('',#12205,2.);
#2744=CYLINDRICAL_SURFACE('',#12207,2.00000000000003);
#2745=CYLINDRICAL_SURFACE('',#12209,2.00000000000003);
#2746=CYLINDRICAL_SURFACE('',#12211,2.00000000000003);
#2747=CYLINDRICAL_SURFACE('',#12213,1.99999999999999);
#2748=CYLINDRICAL_SURFACE('',#12215,1.99999999999999);
#2749=CYLINDRICAL_SURFACE('',#12217,1.99999999999999);
#2750=CYLINDRICAL_SURFACE('',#12219,2.00000000000003);
#2751=CYLINDRICAL_SURFACE('',#12221,1.99999999999999);
#2752=CYLINDRICAL_SURFACE('',#12223,1.99999999999999);
#2753=CYLINDRICAL_SURFACE('',#12225,1.99999999999999);
#2754=CYLINDRICAL_SURFACE('',#12229,2.);
#2755=CYLINDRICAL_SURFACE('',#12232,1.99999999999999);
#2756=CYLINDRICAL_SURFACE('',#12235,2.00000000000003);
#2757=CYLINDRICAL_SURFACE('',#12238,1.99999999999999);
#2758=CYLINDRICAL_SURFACE('',#12241,2.00000000000003);
#2759=CYLINDRICAL_SURFACE('',#12244,2.);
#2760=CYLINDRICAL_SURFACE('',#12247,1.99999999999999);
#2761=CYLINDRICAL_SURFACE('',#12250,1.99999999999999);
#2762=CYLINDRICAL_SURFACE('',#12253,1.99999999999999);
#2763=CYLINDRICAL_SURFACE('',#12256,1.99999999999999);
#2764=CYLINDRICAL_SURFACE('',#12259,1.99999999999999);
#2765=CYLINDRICAL_SURFACE('',#12262,1.99999999999999);
#2766=CYLINDRICAL_SURFACE('',#12265,2.);
#2767=CYLINDRICAL_SURFACE('',#12268,1.99999999999999);
#2768=CYLINDRICAL_SURFACE('',#12271,1.99999999999999);
#2769=CYLINDRICAL_SURFACE('',#12274,1.99999999999999);
#2770=CYLINDRICAL_SURFACE('',#12277,1.99999999999999);
#2771=CYLINDRICAL_SURFACE('',#12280,2.);
#2772=CYLINDRICAL_SURFACE('',#12283,2.);
#2773=CYLINDRICAL_SURFACE('',#12286,2.00000000000003);
#2774=CYLINDRICAL_SURFACE('',#12289,2.);
#2775=CYLINDRICAL_SURFACE('',#12292,1.99999999999999);
#2776=CYLINDRICAL_SURFACE('',#12295,2.);
#2777=CYLINDRICAL_SURFACE('',#12298,1.99999999999999);
#2778=CYLINDRICAL_SURFACE('',#12301,1.99999999999999);
#2779=CYLINDRICAL_SURFACE('',#12304,1.99999999999999);
#2780=CYLINDRICAL_SURFACE('',#12307,1.99999999999999);
#2781=CYLINDRICAL_SURFACE('',#12310,1.99999999999999);
#2782=CYLINDRICAL_SURFACE('',#12313,1.99999999999999);
#2783=CYLINDRICAL_SURFACE('',#12316,1.99999999999999);
#2784=CYLINDRICAL_SURFACE('',#12319,2.);
#2785=CYLINDRICAL_SURFACE('',#12322,2.00000000000003);
#2786=CYLINDRICAL_SURFACE('',#12325,1.99999999999999);
#2787=CYLINDRICAL_SURFACE('',#12328,1.99999999999999);
#2788=CYLINDRICAL_SURFACE('',#12331,1.99999999999999);
#2789=CYLINDRICAL_SURFACE('',#12334,1.99999999999999);
#2790=CYLINDRICAL_SURFACE('',#12337,2.);
#2791=CYLINDRICAL_SURFACE('',#12340,2.00000000000003);
#2792=CYLINDRICAL_SURFACE('',#12343,2.00000000000003);
#2793=CYLINDRICAL_SURFACE('',#12346,2.00000000000003);
#2794=CYLINDRICAL_SURFACE('',#12349,1.99999999999999);
#2795=CYLINDRICAL_SURFACE('',#12352,1.99999999999999);
#2796=CYLINDRICAL_SURFACE('',#12355,1.99999999999999);
#2797=CYLINDRICAL_SURFACE('',#12358,2.00000000000003);
#2798=CYLINDRICAL_SURFACE('',#12361,1.99999999999999);
#2799=CYLINDRICAL_SURFACE('',#12364,1.99999999999999);
#2800=CYLINDRICAL_SURFACE('',#12367,1.99999999999999);
#2883=STYLED_ITEM('',(#19382),#100);
#3018=FACE_OUTER_BOUND('',#3642,.T.);
#3019=FACE_OUTER_BOUND('',#3643,.T.);
#3020=FACE_OUTER_BOUND('',#3644,.T.);
#3021=FACE_OUTER_BOUND('',#3645,.T.);
#3022=FACE_OUTER_BOUND('',#3646,.T.);
#3023=FACE_OUTER_BOUND('',#3647,.T.);
#3024=FACE_OUTER_BOUND('',#3648,.T.);
#3025=FACE_OUTER_BOUND('',#3649,.T.);
#3026=FACE_OUTER_BOUND('',#3650,.T.);
#3027=FACE_OUTER_BOUND('',#3651,.T.);
#3028=FACE_OUTER_BOUND('',#3652,.T.);
#3029=FACE_OUTER_BOUND('',#3653,.T.);
#3030=FACE_OUTER_BOUND('',#3654,.T.);
#3031=FACE_OUTER_BOUND('',#3655,.T.);
#3032=FACE_OUTER_BOUND('',#3656,.T.);
#3033=FACE_OUTER_BOUND('',#3657,.T.);
#3034=FACE_OUTER_BOUND('',#3658,.T.);
#3035=FACE_OUTER_BOUND('',#3659,.T.);
#3036=FACE_OUTER_BOUND('',#3660,.T.);
#3037=FACE_OUTER_BOUND('',#3661,.T.);
#3038=FACE_OUTER_BOUND('',#3662,.T.);
#3039=FACE_OUTER_BOUND('',#3663,.T.);
#3040=FACE_OUTER_BOUND('',#3664,.T.);
#3041=FACE_OUTER_BOUND('',#3665,.T.);
#3042=FACE_OUTER_BOUND('',#3666,.T.);
#3043=FACE_OUTER_BOUND('',#3667,.T.);
#3044=FACE_OUTER_BOUND('',#3668,.T.);
#3045=FACE_OUTER_BOUND('',#3669,.T.);
#3046=FACE_OUTER_BOUND('',#3670,.T.);
#3047=FACE_OUTER_BOUND('',#3671,.T.);
#3048=FACE_OUTER_BOUND('',#3672,.T.);
#3049=FACE_OUTER_BOUND('',#3673,.T.);
#3050=FACE_OUTER_BOUND('',#3674,.T.);
#3051=FACE_OUTER_BOUND('',#3675,.T.);
#3052=FACE_OUTER_BOUND('',#3676,.T.);
#3053=FACE_OUTER_BOUND('',#3677,.T.);
#3054=FACE_OUTER_BOUND('',#3678,.T.);
#3055=FACE_OUTER_BOUND('',#3679,.T.);
#3056=FACE_OUTER_BOUND('',#3680,.T.);
#3057=FACE_OUTER_BOUND('',#3681,.T.);
#3058=FACE_OUTER_BOUND('',#3682,.T.);
#3059=FACE_OUTER_BOUND('',#3683,.T.);
#3060=FACE_OUTER_BOUND('',#3684,.T.);
#3061=FACE_OUTER_BOUND('',#3685,.T.);
#3062=FACE_OUTER_BOUND('',#3686,.T.);
#3063=FACE_OUTER_BOUND('',#3687,.T.);
#3064=FACE_OUTER_BOUND('',#3688,.T.);
#3065=FACE_OUTER_BOUND('',#3689,.T.);
#3066=FACE_OUTER_BOUND('',#3690,.T.);
#3067=FACE_OUTER_BOUND('',#3691,.T.);
#3068=FACE_OUTER_BOUND('',#3692,.T.);
#3069=FACE_OUTER_BOUND('',#3693,.T.);
#3070=FACE_OUTER_BOUND('',#3694,.T.);
#3071=FACE_OUTER_BOUND('',#3695,.T.);
#3072=FACE_OUTER_BOUND('',#3696,.T.);
#3073=FACE_OUTER_BOUND('',#3697,.T.);
#3074=FACE_OUTER_BOUND('',#3698,.T.);
#3075=FACE_OUTER_BOUND('',#3699,.T.);
#3076=FACE_OUTER_BOUND('',#3700,.T.);
#3077=FACE_OUTER_BOUND('',#3701,.T.);
#3078=FACE_OUTER_BOUND('',#3702,.T.);
#3079=FACE_OUTER_BOUND('',#3703,.T.);
#3080=FACE_OUTER_BOUND('',#3704,.T.);
#3081=FACE_OUTER_BOUND('',#3705,.T.);
#3082=FACE_OUTER_BOUND('',#3706,.T.);
#3083=FACE_OUTER_BOUND('',#3707,.T.);
#3084=FACE_OUTER_BOUND('',#3708,.T.);
#3085=FACE_OUTER_BOUND('',#3709,.T.);
#3086=FACE_OUTER_BOUND('',#3710,.T.);
#3087=FACE_OUTER_BOUND('',#3711,.T.);
#3088=FACE_OUTER_BOUND('',#3712,.T.);
#3089=FACE_OUTER_BOUND('',#3713,.T.);
#3090=FACE_OUTER_BOUND('',#3714,.T.);
#3091=FACE_OUTER_BOUND('',#3715,.T.);
#3092=FACE_OUTER_BOUND('',#3716,.T.);
#3093=FACE_OUTER_BOUND('',#3717,.T.);
#3094=FACE_OUTER_BOUND('',#3718,.T.);
#3095=FACE_OUTER_BOUND('',#3719,.T.);
#3096=FACE_OUTER_BOUND('',#3720,.T.);
#3097=FACE_OUTER_BOUND('',#3721,.T.);
#3098=FACE_OUTER_BOUND('',#3722,.T.);
#3099=FACE_OUTER_BOUND('',#3723,.T.);
#3100=FACE_OUTER_BOUND('',#3724,.T.);
#3101=FACE_OUTER_BOUND('',#3725,.T.);
#3102=FACE_OUTER_BOUND('',#3726,.T.);
#3103=FACE_OUTER_BOUND('',#3727,.T.);
#3104=FACE_OUTER_BOUND('',#3728,.T.);
#3105=FACE_OUTER_BOUND('',#3729,.T.);
#3106=FACE_OUTER_BOUND('',#3730,.T.);
#3107=FACE_OUTER_BOUND('',#3731,.T.);
#3108=FACE_OUTER_BOUND('',#3732,.T.);
#3109=FACE_OUTER_BOUND('',#3733,.T.);
#3110=FACE_OUTER_BOUND('',#3734,.T.);
#3111=FACE_OUTER_BOUND('',#3735,.T.);
#3112=FACE_OUTER_BOUND('',#3736,.T.);
#3113=FACE_OUTER_BOUND('',#3737,.T.);
#3114=FACE_OUTER_BOUND('',#3738,.T.);
#3115=FACE_OUTER_BOUND('',#3739,.T.);
#3116=FACE_OUTER_BOUND('',#3740,.T.);
#3117=FACE_OUTER_BOUND('',#3741,.T.);
#3118=FACE_OUTER_BOUND('',#3742,.T.);
#3119=FACE_OUTER_BOUND('',#3743,.T.);
#3120=FACE_OUTER_BOUND('',#3744,.T.);
#3121=FACE_OUTER_BOUND('',#3745,.T.);
#3122=FACE_OUTER_BOUND('',#3746,.T.);
#3123=FACE_OUTER_BOUND('',#3747,.T.);
#3124=FACE_OUTER_BOUND('',#3748,.T.);
#3125=FACE_OUTER_BOUND('',#3749,.T.);
#3126=FACE_OUTER_BOUND('',#3750,.T.);
#3127=FACE_OUTER_BOUND('',#3751,.T.);
#3128=FACE_OUTER_BOUND('',#3752,.T.);
#3129=FACE_OUTER_BOUND('',#3753,.T.);
#3130=FACE_OUTER_BOUND('',#3754,.T.);
#3131=FACE_OUTER_BOUND('',#3755,.T.);
#3132=FACE_OUTER_BOUND('',#3756,.T.);
#3133=FACE_OUTER_BOUND('',#3757,.T.);
#3134=FACE_OUTER_BOUND('',#3758,.T.);
#3135=FACE_OUTER_BOUND('',#3759,.T.);
#3136=FACE_OUTER_BOUND('',#3760,.T.);
#3137=FACE_OUTER_BOUND('',#3761,.T.);
#3138=FACE_OUTER_BOUND('',#3762,.T.);
#3139=FACE_OUTER_BOUND('',#3763,.T.);
#3140=FACE_OUTER_BOUND('',#3764,.T.);
#3141=FACE_OUTER_BOUND('',#3765,.T.);
#3142=FACE_OUTER_BOUND('',#3766,.T.);
#3143=FACE_OUTER_BOUND('',#3767,.T.);
#3144=FACE_OUTER_BOUND('',#3768,.T.);
#3145=FACE_OUTER_BOUND('',#3769,.T.);
#3146=FACE_OUTER_BOUND('',#3770,.T.);
#3147=FACE_OUTER_BOUND('',#3771,.T.);
#3148=FACE_OUTER_BOUND('',#3772,.T.);
#3149=FACE_OUTER_BOUND('',#3773,.T.);
#3150=FACE_OUTER_BOUND('',#3844,.T.);
#3151=FACE_OUTER_BOUND('',#3845,.T.);
#3152=FACE_OUTER_BOUND('',#3893,.T.);
#3153=FACE_OUTER_BOUND('',#3894,.T.);
#3154=FACE_OUTER_BOUND('',#3965,.T.);
#3155=FACE_OUTER_BOUND('',#3966,.T.);
#3156=FACE_OUTER_BOUND('',#3967,.T.);
#3157=FACE_OUTER_BOUND('',#3968,.T.);
#3158=FACE_OUTER_BOUND('',#3969,.T.);
#3159=FACE_OUTER_BOUND('',#3970,.T.);
#3160=FACE_OUTER_BOUND('',#3971,.T.);
#3161=FACE_OUTER_BOUND('',#3972,.T.);
#3162=FACE_OUTER_BOUND('',#3973,.T.);
#3163=FACE_OUTER_BOUND('',#3974,.T.);
#3164=FACE_OUTER_BOUND('',#3975,.T.);
#3165=FACE_OUTER_BOUND('',#3976,.T.);
#3166=FACE_OUTER_BOUND('',#3977,.T.);
#3167=FACE_OUTER_BOUND('',#3978,.T.);
#3168=FACE_OUTER_BOUND('',#3979,.T.);
#3169=FACE_OUTER_BOUND('',#3980,.T.);
#3170=FACE_OUTER_BOUND('',#3981,.T.);
#3171=FACE_OUTER_BOUND('',#3982,.T.);
#3172=FACE_OUTER_BOUND('',#3983,.T.);
#3173=FACE_OUTER_BOUND('',#3984,.T.);
#3174=FACE_OUTER_BOUND('',#3985,.T.);
#3175=FACE_OUTER_BOUND('',#3986,.T.);
#3176=FACE_OUTER_BOUND('',#3987,.T.);
#3177=FACE_OUTER_BOUND('',#3988,.T.);
#3178=FACE_OUTER_BOUND('',#3989,.T.);
#3179=FACE_OUTER_BOUND('',#3990,.T.);
#3180=FACE_OUTER_BOUND('',#3991,.T.);
#3181=FACE_OUTER_BOUND('',#3992,.T.);
#3182=FACE_OUTER_BOUND('',#3993,.T.);
#3183=FACE_OUTER_BOUND('',#3994,.T.);
#3184=FACE_OUTER_BOUND('',#3995,.T.);
#3185=FACE_OUTER_BOUND('',#3996,.T.);
#3186=FACE_OUTER_BOUND('',#3997,.T.);
#3187=FACE_OUTER_BOUND('',#3998,.T.);
#3188=FACE_OUTER_BOUND('',#3999,.T.);
#3189=FACE_OUTER_BOUND('',#4000,.T.);
#3190=FACE_OUTER_BOUND('',#4001,.T.);
#3191=FACE_OUTER_BOUND('',#4002,.T.);
#3192=FACE_OUTER_BOUND('',#4003,.T.);
#3193=FACE_OUTER_BOUND('',#4004,.T.);
#3194=FACE_OUTER_BOUND('',#4005,.T.);
#3195=FACE_OUTER_BOUND('',#4006,.T.);
#3196=FACE_OUTER_BOUND('',#4007,.T.);
#3197=FACE_OUTER_BOUND('',#4008,.T.);
#3198=FACE_OUTER_BOUND('',#4009,.T.);
#3199=FACE_OUTER_BOUND('',#4010,.T.);
#3200=FACE_OUTER_BOUND('',#4011,.T.);
#3201=FACE_OUTER_BOUND('',#4012,.T.);
#3202=FACE_OUTER_BOUND('',#4013,.T.);
#3203=FACE_OUTER_BOUND('',#4014,.T.);
#3204=FACE_OUTER_BOUND('',#4015,.T.);
#3205=FACE_OUTER_BOUND('',#4063,.T.);
#3206=FACE_OUTER_BOUND('',#4064,.T.);
#3207=FACE_OUTER_BOUND('',#4065,.T.);
#3208=FACE_OUTER_BOUND('',#4066,.T.);
#3209=FACE_OUTER_BOUND('',#4067,.T.);
#3210=FACE_OUTER_BOUND('',#4068,.T.);
#3211=FACE_OUTER_BOUND('',#4069,.T.);
#3212=FACE_OUTER_BOUND('',#4070,.T.);
#3213=FACE_OUTER_BOUND('',#4071,.T.);
#3214=FACE_OUTER_BOUND('',#4072,.T.);
#3215=FACE_OUTER_BOUND('',#4073,.T.);
#3216=FACE_OUTER_BOUND('',#4074,.T.);
#3217=FACE_OUTER_BOUND('',#4075,.T.);
#3218=FACE_OUTER_BOUND('',#4076,.T.);
#3219=FACE_OUTER_BOUND('',#4077,.T.);
#3220=FACE_OUTER_BOUND('',#4078,.T.);
#3221=FACE_OUTER_BOUND('',#4079,.T.);
#3222=FACE_OUTER_BOUND('',#4080,.T.);
#3223=FACE_OUTER_BOUND('',#4081,.T.);
#3224=FACE_OUTER_BOUND('',#4082,.T.);
#3225=FACE_OUTER_BOUND('',#4083,.T.);
#3226=FACE_OUTER_BOUND('',#4084,.T.);
#3227=FACE_OUTER_BOUND('',#4085,.T.);
#3228=FACE_OUTER_BOUND('',#4086,.T.);
#3229=FACE_OUTER_BOUND('',#4087,.T.);
#3230=FACE_OUTER_BOUND('',#4088,.T.);
#3231=FACE_OUTER_BOUND('',#4089,.T.);
#3232=FACE_OUTER_BOUND('',#4090,.T.);
#3233=FACE_OUTER_BOUND('',#4091,.T.);
#3234=FACE_OUTER_BOUND('',#4092,.T.);
#3235=FACE_OUTER_BOUND('',#4093,.T.);
#3236=FACE_OUTER_BOUND('',#4094,.T.);
#3237=FACE_OUTER_BOUND('',#4095,.T.);
#3238=FACE_OUTER_BOUND('',#4096,.T.);
#3239=FACE_OUTER_BOUND('',#4097,.T.);
#3240=FACE_OUTER_BOUND('',#4098,.T.);
#3241=FACE_OUTER_BOUND('',#4099,.T.);
#3242=FACE_OUTER_BOUND('',#4100,.T.);
#3243=FACE_OUTER_BOUND('',#4101,.T.);
#3244=FACE_OUTER_BOUND('',#4102,.T.);
#3245=FACE_OUTER_BOUND('',#4103,.T.);
#3246=FACE_OUTER_BOUND('',#4104,.T.);
#3247=FACE_OUTER_BOUND('',#4105,.T.);
#3248=FACE_OUTER_BOUND('',#4106,.T.);
#3249=FACE_OUTER_BOUND('',#4107,.T.);
#3250=FACE_OUTER_BOUND('',#4108,.T.);
#3251=FACE_OUTER_BOUND('',#4109,.T.);
#3252=FACE_OUTER_BOUND('',#4110,.T.);
#3253=FACE_OUTER_BOUND('',#4111,.T.);
#3254=FACE_OUTER_BOUND('',#4112,.T.);
#3255=FACE_OUTER_BOUND('',#4160,.T.);
#3642=EDGE_LOOP('',(#8356,#8357,#8358,#8359));
#3643=EDGE_LOOP('',(#8360,#8361,#8362,#8363));
#3644=EDGE_LOOP('',(#8364,#8365,#8366,#8367));
#3645=EDGE_LOOP('',(#8368,#8369,#8370,#8371));
#3646=EDGE_LOOP('',(#8372,#8373,#8374,#8375));
#3647=EDGE_LOOP('',(#8376,#8377,#8378,#8379));
#3648=EDGE_LOOP('',(#8380,#8381,#8382,#8383));
#3649=EDGE_LOOP('',(#8384,#8385,#8386,#8387));
#3650=EDGE_LOOP('',(#8388,#8389,#8390,#8391));
#3651=EDGE_LOOP('',(#8392,#8393,#8394,#8395));
#3652=EDGE_LOOP('',(#8396,#8397,#8398,#8399));
#3653=EDGE_LOOP('',(#8400,#8401,#8402,#8403));
#3654=EDGE_LOOP('',(#8404,#8405,#8406,#8407));
#3655=EDGE_LOOP('',(#8408,#8409,#8410,#8411));
#3656=EDGE_LOOP('',(#8412,#8413,#8414,#8415));
#3657=EDGE_LOOP('',(#8416,#8417,#8418,#8419));
#3658=EDGE_LOOP('',(#8420,#8421,#8422,#8423));
#3659=EDGE_LOOP('',(#8424,#8425,#8426,#8427));
#3660=EDGE_LOOP('',(#8428,#8429,#8430,#8431));
#3661=EDGE_LOOP('',(#8432,#8433,#8434,#8435));
#3662=EDGE_LOOP('',(#8436,#8437,#8438,#8439));
#3663=EDGE_LOOP('',(#8440,#8441,#8442,#8443));
#3664=EDGE_LOOP('',(#8444,#8445,#8446,#8447));
#3665=EDGE_LOOP('',(#8448,#8449,#8450,#8451));
#3666=EDGE_LOOP('',(#8452,#8453,#8454,#8455));
#3667=EDGE_LOOP('',(#8456,#8457,#8458,#8459));
#3668=EDGE_LOOP('',(#8460,#8461,#8462,#8463));
#3669=EDGE_LOOP('',(#8464,#8465,#8466,#8467));
#3670=EDGE_LOOP('',(#8468,#8469,#8470,#8471));
#3671=EDGE_LOOP('',(#8472,#8473,#8474,#8475));
#3672=EDGE_LOOP('',(#8476,#8477,#8478,#8479));
#3673=EDGE_LOOP('',(#8480,#8481,#8482,#8483));
#3674=EDGE_LOOP('',(#8484,#8485,#8486,#8487));
#3675=EDGE_LOOP('',(#8488,#8489,#8490,#8491));
#3676=EDGE_LOOP('',(#8492,#8493,#8494,#8495));
#3677=EDGE_LOOP('',(#8496,#8497,#8498,#8499));
#3678=EDGE_LOOP('',(#8500,#8501,#8502,#8503));
#3679=EDGE_LOOP('',(#8504,#8505,#8506,#8507));
#3680=EDGE_LOOP('',(#8508,#8509,#8510,#8511));
#3681=EDGE_LOOP('',(#8512,#8513,#8514,#8515));
#3682=EDGE_LOOP('',(#8516,#8517,#8518,#8519));
#3683=EDGE_LOOP('',(#8520,#8521,#8522,#8523));
#3684=EDGE_LOOP('',(#8524,#8525,#8526,#8527));
#3685=EDGE_LOOP('',(#8528,#8529,#8530,#8531));
#3686=EDGE_LOOP('',(#8532,#8533,#8534,#8535));
#3687=EDGE_LOOP('',(#8536,#8537,#8538,#8539));
#3688=EDGE_LOOP('',(#8540,#8541,#8542,#8543));
#3689=EDGE_LOOP('',(#8544,#8545,#8546,#8547));
#3690=EDGE_LOOP('',(#8548,#8549,#8550,#8551));
#3691=EDGE_LOOP('',(#8552,#8553,#8554,#8555));
#3692=EDGE_LOOP('',(#8556,#8557,#8558,#8559));
#3693=EDGE_LOOP('',(#8560,#8561,#8562,#8563));
#3694=EDGE_LOOP('',(#8564,#8565,#8566,#8567));
#3695=EDGE_LOOP('',(#8568,#8569,#8570,#8571));
#3696=EDGE_LOOP('',(#8572,#8573,#8574,#8575));
#3697=EDGE_LOOP('',(#8576,#8577,#8578,#8579));
#3698=EDGE_LOOP('',(#8580,#8581,#8582,#8583));
#3699=EDGE_LOOP('',(#8584,#8585,#8586,#8587));
#3700=EDGE_LOOP('',(#8588,#8589,#8590,#8591));
#3701=EDGE_LOOP('',(#8592,#8593,#8594,#8595));
#3702=EDGE_LOOP('',(#8596,#8597,#8598,#8599));
#3703=EDGE_LOOP('',(#8600,#8601,#8602,#8603));
#3704=EDGE_LOOP('',(#8604,#8605,#8606,#8607));
#3705=EDGE_LOOP('',(#8608,#8609,#8610,#8611));
#3706=EDGE_LOOP('',(#8612,#8613,#8614,#8615));
#3707=EDGE_LOOP('',(#8616,#8617,#8618,#8619));
#3708=EDGE_LOOP('',(#8620,#8621,#8622,#8623));
#3709=EDGE_LOOP('',(#8624,#8625,#8626,#8627));
#3710=EDGE_LOOP('',(#8628,#8629,#8630,#8631));
#3711=EDGE_LOOP('',(#8632,#8633,#8634,#8635));
#3712=EDGE_LOOP('',(#8636,#8637,#8638,#8639));
#3713=EDGE_LOOP('',(#8640,#8641,#8642,#8643));
#3714=EDGE_LOOP('',(#8644,#8645,#8646,#8647));
#3715=EDGE_LOOP('',(#8648,#8649,#8650,#8651));
#3716=EDGE_LOOP('',(#8652,#8653,#8654,#8655));
#3717=EDGE_LOOP('',(#8656,#8657,#8658,#8659));
#3718=EDGE_LOOP('',(#8660,#8661,#8662,#8663));
#3719=EDGE_LOOP('',(#8664,#8665,#8666,#8667));
#3720=EDGE_LOOP('',(#8668,#8669,#8670,#8671));
#3721=EDGE_LOOP('',(#8672,#8673,#8674,#8675));
#3722=EDGE_LOOP('',(#8676,#8677,#8678,#8679));
#3723=EDGE_LOOP('',(#8680,#8681,#8682,#8683));
#3724=EDGE_LOOP('',(#8684,#8685,#8686,#8687));
#3725=EDGE_LOOP('',(#8688,#8689,#8690,#8691));
#3726=EDGE_LOOP('',(#8692,#8693,#8694,#8695));
#3727=EDGE_LOOP('',(#8696,#8697,#8698,#8699));
#3728=EDGE_LOOP('',(#8700,#8701,#8702,#8703));
#3729=EDGE_LOOP('',(#8704,#8705,#8706,#8707));
#3730=EDGE_LOOP('',(#8708,#8709,#8710,#8711));
#3731=EDGE_LOOP('',(#8712,#8713,#8714,#8715));
#3732=EDGE_LOOP('',(#8716,#8717,#8718,#8719));
#3733=EDGE_LOOP('',(#8720,#8721,#8722,#8723));
#3734=EDGE_LOOP('',(#8724,#8725,#8726,#8727));
#3735=EDGE_LOOP('',(#8728,#8729,#8730,#8731));
#3736=EDGE_LOOP('',(#8732,#8733,#8734,#8735));
#3737=EDGE_LOOP('',(#8736,#8737,#8738,#8739));
#3738=EDGE_LOOP('',(#8740,#8741,#8742,#8743));
#3739=EDGE_LOOP('',(#8744,#8745,#8746,#8747));
#3740=EDGE_LOOP('',(#8748,#8749,#8750,#8751));
#3741=EDGE_LOOP('',(#8752,#8753,#8754,#8755));
#3742=EDGE_LOOP('',(#8756,#8757,#8758,#8759));
#3743=EDGE_LOOP('',(#8760,#8761,#8762,#8763));
#3744=EDGE_LOOP('',(#8764,#8765,#8766,#8767));
#3745=EDGE_LOOP('',(#8768,#8769,#8770,#8771));
#3746=EDGE_LOOP('',(#8772,#8773,#8774,#8775));
#3747=EDGE_LOOP('',(#8776,#8777,#8778,#8779));
#3748=EDGE_LOOP('',(#8780,#8781,#8782,#8783));
#3749=EDGE_LOOP('',(#8784,#8785,#8786,#8787));
#3750=EDGE_LOOP('',(#8788,#8789,#8790,#8791));
#3751=EDGE_LOOP('',(#8792,#8793,#8794,#8795));
#3752=EDGE_LOOP('',(#8796,#8797,#8798,#8799));
#3753=EDGE_LOOP('',(#8800,#8801,#8802,#8803));
#3754=EDGE_LOOP('',(#8804,#8805,#8806,#8807));
#3755=EDGE_LOOP('',(#8808,#8809,#8810,#8811));
#3756=EDGE_LOOP('',(#8812,#8813,#8814,#8815));
#3757=EDGE_LOOP('',(#8816,#8817,#8818,#8819));
#3758=EDGE_LOOP('',(#8820,#8821,#8822,#8823));
#3759=EDGE_LOOP('',(#8824,#8825,#8826,#8827));
#3760=EDGE_LOOP('',(#8828,#8829,#8830,#8831));
#3761=EDGE_LOOP('',(#8832,#8833,#8834,#8835));
#3762=EDGE_LOOP('',(#8836,#8837,#8838,#8839));
#3763=EDGE_LOOP('',(#8840,#8841,#8842,#8843));
#3764=EDGE_LOOP('',(#8844,#8845,#8846,#8847));
#3765=EDGE_LOOP('',(#8848,#8849,#8850,#8851));
#3766=EDGE_LOOP('',(#8852,#8853,#8854,#8855));
#3767=EDGE_LOOP('',(#8856,#8857,#8858,#8859));
#3768=EDGE_LOOP('',(#8860,#8861,#8862,#8863));
#3769=EDGE_LOOP('',(#8864,#8865,#8866,#8867));
#3770=EDGE_LOOP('',(#8868,#8869,#8870,#8871));
#3771=EDGE_LOOP('',(#8872,#8873,#8874,#8875));
#3772=EDGE_LOOP('',(#8876,#8877,#8878,#8879));
#3773=EDGE_LOOP('',(#8880,#8881,#8882,#8883));
#3774=EDGE_LOOP('',(#8884));
#3775=EDGE_LOOP('',(#8885));
#3776=EDGE_LOOP('',(#8886,#8887,#8888,#8889));
#3777=EDGE_LOOP('',(#8890,#8891,#8892,#8893));
#3778=EDGE_LOOP('',(#8894));
#3779=EDGE_LOOP('',(#8895));
#3780=EDGE_LOOP('',(#8896));
#3781=EDGE_LOOP('',(#8897,#8898,#8899,#8900));
#3782=EDGE_LOOP('',(#8901,#8902,#8903,#8904));
#3783=EDGE_LOOP('',(#8905));
#3784=EDGE_LOOP('',(#8906));
#3785=EDGE_LOOP('',(#8907));
#3786=EDGE_LOOP('',(#8908));
#3787=EDGE_LOOP('',(#8909));
#3788=EDGE_LOOP('',(#8910,#8911,#8912,#8913));
#3789=EDGE_LOOP('',(#8914,#8915,#8916,#8917));
#3790=EDGE_LOOP('',(#8918));
#3791=EDGE_LOOP('',(#8919));
#3792=EDGE_LOOP('',(#8920));
#3793=EDGE_LOOP('',(#8921));
#3794=EDGE_LOOP('',(#8922));
#3795=EDGE_LOOP('',(#8923,#8924,#8925,#8926));
#3796=EDGE_LOOP('',(#8927,#8928,#8929,#8930));
#3797=EDGE_LOOP('',(#8931));
#3798=EDGE_LOOP('',(#8932));
#3799=EDGE_LOOP('',(#8933));
#3800=EDGE_LOOP('',(#8934));
#3801=EDGE_LOOP('',(#8935));
#3802=EDGE_LOOP('',(#8936,#8937,#8938,#8939));
#3803=EDGE_LOOP('',(#8940,#8941,#8942,#8943));
#3804=EDGE_LOOP('',(#8944));
#3805=EDGE_LOOP('',(#8945));
#3806=EDGE_LOOP('',(#8946));
#3807=EDGE_LOOP('',(#8947));
#3808=EDGE_LOOP('',(#8948));
#3809=EDGE_LOOP('',(#8949,#8950,#8951,#8952));
#3810=EDGE_LOOP('',(#8953,#8954,#8955,#8956));
#3811=EDGE_LOOP('',(#8957));
#3812=EDGE_LOOP('',(#8958));
#3813=EDGE_LOOP('',(#8959));
#3814=EDGE_LOOP('',(#8960));
#3815=EDGE_LOOP('',(#8961));
#3816=EDGE_LOOP('',(#8962,#8963,#8964,#8965));
#3817=EDGE_LOOP('',(#8966,#8967,#8968,#8969));
#3818=EDGE_LOOP('',(#8970));
#3819=EDGE_LOOP('',(#8971));
#3820=EDGE_LOOP('',(#8972));
#3821=EDGE_LOOP('',(#8973));
#3822=EDGE_LOOP('',(#8974));
#3823=EDGE_LOOP('',(#8975,#8976,#8977,#8978));
#3824=EDGE_LOOP('',(#8979,#8980,#8981,#8982));
#3825=EDGE_LOOP('',(#8983));
#3826=EDGE_LOOP('',(#8984));
#3827=EDGE_LOOP('',(#8985));
#3828=EDGE_LOOP('',(#8986));
#3829=EDGE_LOOP('',(#8987));
#3830=EDGE_LOOP('',(#8988,#8989,#8990,#8991));
#3831=EDGE_LOOP('',(#8992,#8993,#8994,#8995));
#3832=EDGE_LOOP('',(#8996));
#3833=EDGE_LOOP('',(#8997));
#3834=EDGE_LOOP('',(#8998));
#3835=EDGE_LOOP('',(#8999));
#3836=EDGE_LOOP('',(#9000));
#3837=EDGE_LOOP('',(#9001,#9002,#9003,#9004));
#3838=EDGE_LOOP('',(#9005,#9006,#9007,#9008));
#3839=EDGE_LOOP('',(#9009));
#3840=EDGE_LOOP('',(#9010));
#3841=EDGE_LOOP('',(#9011));
#3842=EDGE_LOOP('',(#9012));
#3843=EDGE_LOOP('',(#9013));
#3844=EDGE_LOOP('',(#9014,#9015,#9016,#9017));
#3845=EDGE_LOOP('',(#9018,#9019,#9020,#9021));
#3846=EDGE_LOOP('',(#9022));
#3847=EDGE_LOOP('',(#9023));
#3848=EDGE_LOOP('',(#9024));
#3849=EDGE_LOOP('',(#9025));
#3850=EDGE_LOOP('',(#9026));
#3851=EDGE_LOOP('',(#9027));
#3852=EDGE_LOOP('',(#9028));
#3853=EDGE_LOOP('',(#9029));
#3854=EDGE_LOOP('',(#9030));
#3855=EDGE_LOOP('',(#9031));
#3856=EDGE_LOOP('',(#9032));
#3857=EDGE_LOOP('',(#9033));
#3858=EDGE_LOOP('',(#9034));
#3859=EDGE_LOOP('',(#9035));
#3860=EDGE_LOOP('',(#9036));
#3861=EDGE_LOOP('',(#9037));
#3862=EDGE_LOOP('',(#9038));
#3863=EDGE_LOOP('',(#9039));
#3864=EDGE_LOOP('',(#9040));
#3865=EDGE_LOOP('',(#9041));
#3866=EDGE_LOOP('',(#9042));
#3867=EDGE_LOOP('',(#9043));
#3868=EDGE_LOOP('',(#9044));
#3869=EDGE_LOOP('',(#9045));
#3870=EDGE_LOOP('',(#9046));
#3871=EDGE_LOOP('',(#9047));
#3872=EDGE_LOOP('',(#9048));
#3873=EDGE_LOOP('',(#9049));
#3874=EDGE_LOOP('',(#9050));
#3875=EDGE_LOOP('',(#9051));
#3876=EDGE_LOOP('',(#9052));
#3877=EDGE_LOOP('',(#9053));
#3878=EDGE_LOOP('',(#9054));
#3879=EDGE_LOOP('',(#9055));
#3880=EDGE_LOOP('',(#9056));
#3881=EDGE_LOOP('',(#9057));
#3882=EDGE_LOOP('',(#9058));
#3883=EDGE_LOOP('',(#9059));
#3884=EDGE_LOOP('',(#9060));
#3885=EDGE_LOOP('',(#9061));
#3886=EDGE_LOOP('',(#9062));
#3887=EDGE_LOOP('',(#9063));
#3888=EDGE_LOOP('',(#9064));
#3889=EDGE_LOOP('',(#9065));
#3890=EDGE_LOOP('',(#9066));
#3891=EDGE_LOOP('',(#9067));
#3892=EDGE_LOOP('',(#9068));
#3893=EDGE_LOOP('',(#9069,#9070,#9071,#9072));
#3894=EDGE_LOOP('',(#9073,#9074,#9075,#9076));
#3895=EDGE_LOOP('',(#9077));
#3896=EDGE_LOOP('',(#9078));
#3897=EDGE_LOOP('',(#9079,#9080,#9081,#9082));
#3898=EDGE_LOOP('',(#9083,#9084,#9085,#9086));
#3899=EDGE_LOOP('',(#9087));
#3900=EDGE_LOOP('',(#9088));
#3901=EDGE_LOOP('',(#9089));
#3902=EDGE_LOOP('',(#9090,#9091,#9092,#9093));
#3903=EDGE_LOOP('',(#9094,#9095,#9096,#9097));
#3904=EDGE_LOOP('',(#9098));
#3905=EDGE_LOOP('',(#9099));
#3906=EDGE_LOOP('',(#9100));
#3907=EDGE_LOOP('',(#9101));
#3908=EDGE_LOOP('',(#9102));
#3909=EDGE_LOOP('',(#9103,#9104,#9105,#9106));
#3910=EDGE_LOOP('',(#9107,#9108,#9109,#9110));
#3911=EDGE_LOOP('',(#9111));
#3912=EDGE_LOOP('',(#9112));
#3913=EDGE_LOOP('',(#9113));
#3914=EDGE_LOOP('',(#9114));
#3915=EDGE_LOOP('',(#9115));
#3916=EDGE_LOOP('',(#9116,#9117,#9118,#9119));
#3917=EDGE_LOOP('',(#9120,#9121,#9122,#9123));
#3918=EDGE_LOOP('',(#9124));
#3919=EDGE_LOOP('',(#9125));
#3920=EDGE_LOOP('',(#9126));
#3921=EDGE_LOOP('',(#9127));
#3922=EDGE_LOOP('',(#9128));
#3923=EDGE_LOOP('',(#9129,#9130,#9131,#9132));
#3924=EDGE_LOOP('',(#9133,#9134,#9135,#9136));
#3925=EDGE_LOOP('',(#9137));
#3926=EDGE_LOOP('',(#9138));
#3927=EDGE_LOOP('',(#9139));
#3928=EDGE_LOOP('',(#9140));
#3929=EDGE_LOOP('',(#9141));
#3930=EDGE_LOOP('',(#9142,#9143,#9144,#9145));
#3931=EDGE_LOOP('',(#9146,#9147,#9148,#9149));
#3932=EDGE_LOOP('',(#9150));
#3933=EDGE_LOOP('',(#9151));
#3934=EDGE_LOOP('',(#9152));
#3935=EDGE_LOOP('',(#9153));
#3936=EDGE_LOOP('',(#9154));
#3937=EDGE_LOOP('',(#9155,#9156,#9157,#9158));
#3938=EDGE_LOOP('',(#9159,#9160,#9161,#9162));
#3939=EDGE_LOOP('',(#9163));
#3940=EDGE_LOOP('',(#9164));
#3941=EDGE_LOOP('',(#9165));
#3942=EDGE_LOOP('',(#9166));
#3943=EDGE_LOOP('',(#9167));
#3944=EDGE_LOOP('',(#9168,#9169,#9170,#9171));
#3945=EDGE_LOOP('',(#9172,#9173,#9174,#9175));
#3946=EDGE_LOOP('',(#9176));
#3947=EDGE_LOOP('',(#9177));
#3948=EDGE_LOOP('',(#9178));
#3949=EDGE_LOOP('',(#9179));
#3950=EDGE_LOOP('',(#9180));
#3951=EDGE_LOOP('',(#9181,#9182,#9183,#9184));
#3952=EDGE_LOOP('',(#9185,#9186,#9187,#9188));
#3953=EDGE_LOOP('',(#9189));
#3954=EDGE_LOOP('',(#9190));
#3955=EDGE_LOOP('',(#9191));
#3956=EDGE_LOOP('',(#9192));
#3957=EDGE_LOOP('',(#9193));
#3958=EDGE_LOOP('',(#9194,#9195,#9196,#9197));
#3959=EDGE_LOOP('',(#9198,#9199,#9200,#9201));
#3960=EDGE_LOOP('',(#9202));
#3961=EDGE_LOOP('',(#9203));
#3962=EDGE_LOOP('',(#9204));
#3963=EDGE_LOOP('',(#9205));
#3964=EDGE_LOOP('',(#9206));
#3965=EDGE_LOOP('',(#9207,#9208,#9209,#9210,#9211,#9212,#9213,#9214,#9215,
#9216,#9217,#9218));
#3966=EDGE_LOOP('',(#9219,#9220,#9221,#9222));
#3967=EDGE_LOOP('',(#9223,#9224,#9225,#9226));
#3968=EDGE_LOOP('',(#9227,#9228,#9229,#9230));
#3969=EDGE_LOOP('',(#9231,#9232,#9233,#9234));
#3970=EDGE_LOOP('',(#9235,#9236,#9237,#9238));
#3971=EDGE_LOOP('',(#9239,#9240,#9241,#9242));
#3972=EDGE_LOOP('',(#9243,#9244,#9245,#9246));
#3973=EDGE_LOOP('',(#9247,#9248,#9249,#9250));
#3974=EDGE_LOOP('',(#9251,#9252,#9253,#9254));
#3975=EDGE_LOOP('',(#9255,#9256,#9257,#9258));
#3976=EDGE_LOOP('',(#9259,#9260,#9261,#9262));
#3977=EDGE_LOOP('',(#9263,#9264,#9265,#9266));
#3978=EDGE_LOOP('',(#9267,#9268,#9269,#9270));
#3979=EDGE_LOOP('',(#9271,#9272,#9273,#9274));
#3980=EDGE_LOOP('',(#9275,#9276,#9277,#9278));
#3981=EDGE_LOOP('',(#9279,#9280,#9281,#9282));
#3982=EDGE_LOOP('',(#9283,#9284,#9285,#9286));
#3983=EDGE_LOOP('',(#9287,#9288,#9289,#9290));
#3984=EDGE_LOOP('',(#9291,#9292,#9293,#9294));
#3985=EDGE_LOOP('',(#9295,#9296,#9297,#9298));
#3986=EDGE_LOOP('',(#9299,#9300,#9301,#9302));
#3987=EDGE_LOOP('',(#9303,#9304,#9305,#9306));
#3988=EDGE_LOOP('',(#9307,#9308,#9309,#9310));
#3989=EDGE_LOOP('',(#9311,#9312,#9313,#9314));
#3990=EDGE_LOOP('',(#9315,#9316,#9317,#9318));
#3991=EDGE_LOOP('',(#9319,#9320,#9321,#9322));
#3992=EDGE_LOOP('',(#9323,#9324,#9325,#9326));
#3993=EDGE_LOOP('',(#9327,#9328,#9329,#9330));
#3994=EDGE_LOOP('',(#9331,#9332,#9333,#9334));
#3995=EDGE_LOOP('',(#9335,#9336,#9337,#9338));
#3996=EDGE_LOOP('',(#9339,#9340,#9341,#9342));
#3997=EDGE_LOOP('',(#9343,#9344,#9345,#9346));
#3998=EDGE_LOOP('',(#9347,#9348,#9349,#9350));
#3999=EDGE_LOOP('',(#9351,#9352,#9353,#9354));
#4000=EDGE_LOOP('',(#9355,#9356,#9357,#9358));
#4001=EDGE_LOOP('',(#9359,#9360,#9361,#9362));
#4002=EDGE_LOOP('',(#9363,#9364,#9365,#9366));
#4003=EDGE_LOOP('',(#9367,#9368,#9369,#9370));
#4004=EDGE_LOOP('',(#9371,#9372,#9373,#9374));
#4005=EDGE_LOOP('',(#9375,#9376,#9377,#9378));
#4006=EDGE_LOOP('',(#9379,#9380,#9381,#9382));
#4007=EDGE_LOOP('',(#9383,#9384,#9385,#9386));
#4008=EDGE_LOOP('',(#9387,#9388,#9389,#9390));
#4009=EDGE_LOOP('',(#9391,#9392,#9393,#9394));
#4010=EDGE_LOOP('',(#9395,#9396,#9397,#9398));
#4011=EDGE_LOOP('',(#9399,#9400,#9401,#9402));
#4012=EDGE_LOOP('',(#9403,#9404,#9405,#9406));
#4013=EDGE_LOOP('',(#9407,#9408,#9409,#9410));
#4014=EDGE_LOOP('',(#9411,#9412,#9413,#9414));
#4015=EDGE_LOOP('',(#9415,#9416,#9417,#9418));
#4016=EDGE_LOOP('',(#9419));
#4017=EDGE_LOOP('',(#9420));
#4018=EDGE_LOOP('',(#9421));
#4019=EDGE_LOOP('',(#9422));
#4020=EDGE_LOOP('',(#9423));
#4021=EDGE_LOOP('',(#9424));
#4022=EDGE_LOOP('',(#9425));
#4023=EDGE_LOOP('',(#9426));
#4024=EDGE_LOOP('',(#9427));
#4025=EDGE_LOOP('',(#9428));
#4026=EDGE_LOOP('',(#9429));
#4027=EDGE_LOOP('',(#9430));
#4028=EDGE_LOOP('',(#9431));
#4029=EDGE_LOOP('',(#9432));
#4030=EDGE_LOOP('',(#9433));
#4031=EDGE_LOOP('',(#9434));
#4032=EDGE_LOOP('',(#9435));
#4033=EDGE_LOOP('',(#9436));
#4034=EDGE_LOOP('',(#9437));
#4035=EDGE_LOOP('',(#9438));
#4036=EDGE_LOOP('',(#9439));
#4037=EDGE_LOOP('',(#9440));
#4038=EDGE_LOOP('',(#9441));
#4039=EDGE_LOOP('',(#9442));
#4040=EDGE_LOOP('',(#9443));
#4041=EDGE_LOOP('',(#9444));
#4042=EDGE_LOOP('',(#9445));
#4043=EDGE_LOOP('',(#9446));
#4044=EDGE_LOOP('',(#9447));
#4045=EDGE_LOOP('',(#9448));
#4046=EDGE_LOOP('',(#9449));
#4047=EDGE_LOOP('',(#9450));
#4048=EDGE_LOOP('',(#9451));
#4049=EDGE_LOOP('',(#9452));
#4050=EDGE_LOOP('',(#9453));
#4051=EDGE_LOOP('',(#9454));
#4052=EDGE_LOOP('',(#9455));
#4053=EDGE_LOOP('',(#9456));
#4054=EDGE_LOOP('',(#9457));
#4055=EDGE_LOOP('',(#9458));
#4056=EDGE_LOOP('',(#9459));
#4057=EDGE_LOOP('',(#9460));
#4058=EDGE_LOOP('',(#9461));
#4059=EDGE_LOOP('',(#9462));
#4060=EDGE_LOOP('',(#9463));
#4061=EDGE_LOOP('',(#9464));
#4062=EDGE_LOOP('',(#9465));
#4063=EDGE_LOOP('',(#9466,#9467,#9468,#9469));
#4064=EDGE_LOOP('',(#9470,#9471,#9472,#9473));
#4065=EDGE_LOOP('',(#9474,#9475,#9476,#9477));
#4066=EDGE_LOOP('',(#9478,#9479,#9480,#9481));
#4067=EDGE_LOOP('',(#9482,#9483,#9484,#9485));
#4068=EDGE_LOOP('',(#9486,#9487,#9488,#9489));
#4069=EDGE_LOOP('',(#9490,#9491,#9492,#9493));
#4070=EDGE_LOOP('',(#9494,#9495,#9496,#9497));
#4071=EDGE_LOOP('',(#9498,#9499,#9500,#9501));
#4072=EDGE_LOOP('',(#9502,#9503,#9504,#9505));
#4073=EDGE_LOOP('',(#9506,#9507,#9508,#9509));
#4074=EDGE_LOOP('',(#9510,#9511,#9512,#9513));
#4075=EDGE_LOOP('',(#9514,#9515,#9516,#9517));
#4076=EDGE_LOOP('',(#9518,#9519,#9520,#9521));
#4077=EDGE_LOOP('',(#9522,#9523,#9524,#9525));
#4078=EDGE_LOOP('',(#9526,#9527,#9528,#9529));
#4079=EDGE_LOOP('',(#9530,#9531,#9532,#9533));
#4080=EDGE_LOOP('',(#9534,#9535,#9536,#9537));
#4081=EDGE_LOOP('',(#9538,#9539,#9540,#9541));
#4082=EDGE_LOOP('',(#9542,#9543,#9544,#9545));
#4083=EDGE_LOOP('',(#9546,#9547,#9548,#9549));
#4084=EDGE_LOOP('',(#9550,#9551,#9552,#9553));
#4085=EDGE_LOOP('',(#9554,#9555,#9556,#9557));
#4086=EDGE_LOOP('',(#9558,#9559,#9560,#9561));
#4087=EDGE_LOOP('',(#9562,#9563,#9564,#9565));
#4088=EDGE_LOOP('',(#9566,#9567,#9568,#9569));
#4089=EDGE_LOOP('',(#9570,#9571,#9572,#9573));
#4090=EDGE_LOOP('',(#9574,#9575,#9576,#9577));
#4091=EDGE_LOOP('',(#9578,#9579,#9580,#9581));
#4092=EDGE_LOOP('',(#9582,#9583,#9584,#9585));
#4093=EDGE_LOOP('',(#9586,#9587,#9588,#9589));
#4094=EDGE_LOOP('',(#9590,#9591,#9592,#9593));
#4095=EDGE_LOOP('',(#9594,#9595,#9596,#9597));
#4096=EDGE_LOOP('',(#9598,#9599,#9600,#9601));
#4097=EDGE_LOOP('',(#9602,#9603,#9604,#9605));
#4098=EDGE_LOOP('',(#9606,#9607,#9608,#9609));
#4099=EDGE_LOOP('',(#9610,#9611,#9612,#9613));
#4100=EDGE_LOOP('',(#9614,#9615,#9616,#9617));
#4101=EDGE_LOOP('',(#9618,#9619,#9620,#9621));
#4102=EDGE_LOOP('',(#9622,#9623,#9624,#9625));
#4103=EDGE_LOOP('',(#9626,#9627,#9628,#9629));
#4104=EDGE_LOOP('',(#9630,#9631,#9632,#9633));
#4105=EDGE_LOOP('',(#9634,#9635,#9636,#9637));
#4106=EDGE_LOOP('',(#9638,#9639,#9640,#9641));
#4107=EDGE_LOOP('',(#9642,#9643,#9644,#9645));
#4108=EDGE_LOOP('',(#9646,#9647,#9648,#9649));
#4109=EDGE_LOOP('',(#9650,#9651,#9652,#9653));
#4110=EDGE_LOOP('',(#9654,#9655,#9656,#9657));
#4111=EDGE_LOOP('',(#9658,#9659,#9660,#9661,#9662,#9663,#9664,#9665,#9666,
#9667,#9668,#9669));
#4112=EDGE_LOOP('',(#9670,#9671,#9672,#9673));
#4113=EDGE_LOOP('',(#9674));
#4114=EDGE_LOOP('',(#9675));
#4115=EDGE_LOOP('',(#9676));
#4116=EDGE_LOOP('',(#9677));
#4117=EDGE_LOOP('',(#9678));
#4118=EDGE_LOOP('',(#9679));
#4119=EDGE_LOOP('',(#9680));
#4120=EDGE_LOOP('',(#9681));
#4121=EDGE_LOOP('',(#9682));
#4122=EDGE_LOOP('',(#9683));
#4123=EDGE_LOOP('',(#9684));
#4124=EDGE_LOOP('',(#9685));
#4125=EDGE_LOOP('',(#9686));
#4126=EDGE_LOOP('',(#9687));
#4127=EDGE_LOOP('',(#9688));
#4128=EDGE_LOOP('',(#9689));
#4129=EDGE_LOOP('',(#9690));
#4130=EDGE_LOOP('',(#9691));
#4131=EDGE_LOOP('',(#9692));
#4132=EDGE_LOOP('',(#9693));
#4133=EDGE_LOOP('',(#9694));
#4134=EDGE_LOOP('',(#9695));
#4135=EDGE_LOOP('',(#9696));
#4136=EDGE_LOOP('',(#9697));
#4137=EDGE_LOOP('',(#9698));
#4138=EDGE_LOOP('',(#9699));
#4139=EDGE_LOOP('',(#9700));
#4140=EDGE_LOOP('',(#9701));
#4141=EDGE_LOOP('',(#9702));
#4142=EDGE_LOOP('',(#9703));
#4143=EDGE_LOOP('',(#9704));
#4144=EDGE_LOOP('',(#9705));
#4145=EDGE_LOOP('',(#9706));
#4146=EDGE_LOOP('',(#9707));
#4147=EDGE_LOOP('',(#9708));
#4148=EDGE_LOOP('',(#9709));
#4149=EDGE_LOOP('',(#9710));
#4150=EDGE_LOOP('',(#9711));
#4151=EDGE_LOOP('',(#9712));
#4152=EDGE_LOOP('',(#9713));
#4153=EDGE_LOOP('',(#9714));
#4154=EDGE_LOOP('',(#9715));
#4155=EDGE_LOOP('',(#9716));
#4156=EDGE_LOOP('',(#9717));
#4157=EDGE_LOOP('',(#9718));
#4158=EDGE_LOOP('',(#9719));
#4159=EDGE_LOOP('',(#9720));
#4160=EDGE_LOOP('',(#9721,#9722,#9723,#9724));
#4161=EDGE_LOOP('',(#9725));
#4162=EDGE_LOOP('',(#9726));
#4163=EDGE_LOOP('',(#9727));
#4164=EDGE_LOOP('',(#9728));
#4165=EDGE_LOOP('',(#9729));
#4166=EDGE_LOOP('',(#9730));
#4167=EDGE_LOOP('',(#9731));
#4168=EDGE_LOOP('',(#9732));
#4169=EDGE_LOOP('',(#9733));
#4170=EDGE_LOOP('',(#9734));
#4171=EDGE_LOOP('',(#9735));
#4172=EDGE_LOOP('',(#9736));
#4173=EDGE_LOOP('',(#9737));
#4174=EDGE_LOOP('',(#9738));
#4175=EDGE_LOOP('',(#9739));
#4176=EDGE_LOOP('',(#9740));
#4177=EDGE_LOOP('',(#9741));
#4178=EDGE_LOOP('',(#9742));
#4179=EDGE_LOOP('',(#9743));
#4180=EDGE_LOOP('',(#9744));
#4181=EDGE_LOOP('',(#9745));
#4182=EDGE_LOOP('',(#9746));
#4183=EDGE_LOOP('',(#9747));
#4184=EDGE_LOOP('',(#9748));
#4185=EDGE_LOOP('',(#9749));
#4186=EDGE_LOOP('',(#9750));
#4187=EDGE_LOOP('',(#9751));
#4188=EDGE_LOOP('',(#9752));
#4189=EDGE_LOOP('',(#9753));
#4190=EDGE_LOOP('',(#9754));
#4191=EDGE_LOOP('',(#9755));
#4192=EDGE_LOOP('',(#9756));
#4193=EDGE_LOOP('',(#9757));
#4194=EDGE_LOOP('',(#9758));
#4195=EDGE_LOOP('',(#9759));
#4196=EDGE_LOOP('',(#9760));
#4197=EDGE_LOOP('',(#9761));
#4198=EDGE_LOOP('',(#9762));
#4199=EDGE_LOOP('',(#9763));
#4200=EDGE_LOOP('',(#9764));
#4201=EDGE_LOOP('',(#9765));
#4202=EDGE_LOOP('',(#9766));
#4203=EDGE_LOOP('',(#9767));
#4204=EDGE_LOOP('',(#9768));
#4205=EDGE_LOOP('',(#9769));
#4206=EDGE_LOOP('',(#9770));
#4207=EDGE_LOOP('',(#9771));
#4645=CIRCLE('',#11761,2.5);
#4646=CIRCLE('',#11762,2.5);
#4647=CIRCLE('',#11764,2.5);
#4648=CIRCLE('',#11765,2.5);
#4649=CIRCLE('',#11767,2.5);
#4650=CIRCLE('',#11768,2.5);
#4651=CIRCLE('',#11770,2.5);
#4652=CIRCLE('',#11771,2.5);
#4653=CIRCLE('',#11773,10.);
#4654=CIRCLE('',#11774,10.);
#4655=CIRCLE('',#11777,1.5);
#4656=CIRCLE('',#11778,1.5);
#4657=CIRCLE('',#11781,1.5);
#4658=CIRCLE('',#11782,1.5);
#4659=CIRCLE('',#11785,1.5);
#4660=CIRCLE('',#11786,1.5);
#4661=CIRCLE('',#11789,1.5);
#4662=CIRCLE('',#11790,1.5);
#4663=CIRCLE('',#11792,2.5);
#4664=CIRCLE('',#11793,2.5);
#4665=CIRCLE('',#11795,2.5);
#4666=CIRCLE('',#11796,2.5);
#4667=CIRCLE('',#11798,2.5);
#4668=CIRCLE('',#11799,2.5);
#4669=CIRCLE('',#11801,2.5);
#4670=CIRCLE('',#11802,2.5);
#4671=CIRCLE('',#11804,10.);
#4672=CIRCLE('',#11805,10.);
#4673=CIRCLE('',#11808,1.5);
#4674=CIRCLE('',#11809,1.5);
#4675=CIRCLE('',#11812,1.5);
#4676=CIRCLE('',#11813,1.5);
#4677=CIRCLE('',#11816,1.5);
#4678=CIRCLE('',#11817,1.5);
#4679=CIRCLE('',#11820,1.5);
#4680=CIRCLE('',#11821,1.5);
#4681=CIRCLE('',#11823,2.5);
#4682=CIRCLE('',#11824,2.5);
#4683=CIRCLE('',#11826,2.5);
#4684=CIRCLE('',#11827,2.5);
#4685=CIRCLE('',#11829,2.5);
#4686=CIRCLE('',#11830,2.5);
#4687=CIRCLE('',#11832,2.5);
#4688=CIRCLE('',#11833,2.5);
#4689=CIRCLE('',#11835,10.);
#4690=CIRCLE('',#11836,10.);
#4691=CIRCLE('',#11839,1.5);
#4692=CIRCLE('',#11840,1.5);
#4693=CIRCLE('',#11843,1.5);
#4694=CIRCLE('',#11844,1.5);
#4695=CIRCLE('',#11847,1.5);
#4696=CIRCLE('',#11848,1.5);
#4697=CIRCLE('',#11851,1.5);
#4698=CIRCLE('',#11852,1.5);
#4699=CIRCLE('',#11854,2.5);
#4700=CIRCLE('',#11855,2.5);
#4701=CIRCLE('',#11857,2.5);
#4702=CIRCLE('',#11858,2.5);
#4703=CIRCLE('',#11860,2.5);
#4704=CIRCLE('',#11861,2.5);
#4705=CIRCLE('',#11863,2.5);
#4706=CIRCLE('',#11864,2.5);
#4707=CIRCLE('',#11866,10.);
#4708=CIRCLE('',#11867,10.);
#4709=CIRCLE('',#11870,1.5);
#4710=CIRCLE('',#11871,1.5);
#4711=CIRCLE('',#11874,1.5);
#4712=CIRCLE('',#11875,1.5);
#4713=CIRCLE('',#11878,1.5);
#4714=CIRCLE('',#11879,1.5);
#4715=CIRCLE('',#11882,1.5);
#4716=CIRCLE('',#11883,1.5);
#4717=CIRCLE('',#11885,2.5);
#4718=CIRCLE('',#11886,2.5);
#4719=CIRCLE('',#11888,2.5);
#4720=CIRCLE('',#11889,2.5);
#4721=CIRCLE('',#11891,2.5);
#4722=CIRCLE('',#11892,2.5);
#4723=CIRCLE('',#11894,2.5);
#4724=CIRCLE('',#11895,2.5);
#4725=CIRCLE('',#11897,10.);
#4726=CIRCLE('',#11898,10.);
#4727=CIRCLE('',#11901,1.5);
#4728=CIRCLE('',#11902,1.5);
#4729=CIRCLE('',#11905,1.5);
#4730=CIRCLE('',#11906,1.5);
#4731=CIRCLE('',#11909,1.5);
#4732=CIRCLE('',#11910,1.5);
#4733=CIRCLE('',#11913,1.5);
#4734=CIRCLE('',#11914,1.5);
#4735=CIRCLE('',#11916,2.5);
#4736=CIRCLE('',#11917,2.5);
#4737=CIRCLE('',#11919,2.5);
#4738=CIRCLE('',#11920,2.5);
#4739=CIRCLE('',#11922,2.5);
#4740=CIRCLE('',#11923,2.5);
#4741=CIRCLE('',#11925,2.5);
#4742=CIRCLE('',#11926,2.5);
#4743=CIRCLE('',#11928,10.);
#4744=CIRCLE('',#11929,10.);
#4745=CIRCLE('',#11932,1.5);
#4746=CIRCLE('',#11933,1.5);
#4747=CIRCLE('',#11936,1.5);
#4748=CIRCLE('',#11937,1.5);
#4749=CIRCLE('',#11940,1.5);
#4750=CIRCLE('',#11941,1.5);
#4751=CIRCLE('',#11944,1.5);
#4752=CIRCLE('',#11945,1.5);
#4753=CIRCLE('',#11947,2.5);
#4754=CIRCLE('',#11948,2.5);
#4755=CIRCLE('',#11950,2.5);
#4756=CIRCLE('',#11951,2.5);
#4757=CIRCLE('',#11953,2.5);
#4758=CIRCLE('',#11954,2.5);
#4759=CIRCLE('',#11956,2.5);
#4760=CIRCLE('',#11957,2.5);
#4761=CIRCLE('',#11959,10.);
#4762=CIRCLE('',#11960,10.);
#4763=CIRCLE('',#11963,1.5);
#4764=CIRCLE('',#11964,1.5);
#4765=CIRCLE('',#11967,1.5);
#4766=CIRCLE('',#11968,1.5);
#4767=CIRCLE('',#11971,1.5);
#4768=CIRCLE('',#11972,1.5);
#4769=CIRCLE('',#11975,1.5);
#4770=CIRCLE('',#11976,1.5);
#4771=CIRCLE('',#11978,2.5);
#4772=CIRCLE('',#11979,2.5);
#4773=CIRCLE('',#11981,2.5);
#4774=CIRCLE('',#11982,2.5);
#4775=CIRCLE('',#11984,2.5);
#4776=CIRCLE('',#11985,2.5);
#4777=CIRCLE('',#11987,2.5);
#4778=CIRCLE('',#11988,2.5);
#4779=CIRCLE('',#11990,10.);
#4780=CIRCLE('',#11991,10.);
#4781=CIRCLE('',#11994,1.5);
#4782=CIRCLE('',#11995,1.5);
#4783=CIRCLE('',#11998,1.5);
#4784=CIRCLE('',#11999,1.5);
#4785=CIRCLE('',#12002,1.5);
#4786=CIRCLE('',#12003,1.5);
#4787=CIRCLE('',#12006,1.5);
#4788=CIRCLE('',#12007,1.5);
#4789=CIRCLE('',#12009,2.5);
#4790=CIRCLE('',#12010,2.5);
#4791=CIRCLE('',#12012,2.5);
#4792=CIRCLE('',#12013,2.5);
#4793=CIRCLE('',#12015,2.5);
#4794=CIRCLE('',#12016,2.5);
#4795=CIRCLE('',#12018,2.5);
#4796=CIRCLE('',#12019,2.5);
#4797=CIRCLE('',#12021,10.);
#4798=CIRCLE('',#12022,10.);
#4799=CIRCLE('',#12025,1.5);
#4800=CIRCLE('',#12026,1.5);
#4801=CIRCLE('',#12029,1.5);
#4802=CIRCLE('',#12030,1.5);
#4803=CIRCLE('',#12033,1.5);
#4804=CIRCLE('',#12034,1.5);
#4805=CIRCLE('',#12037,1.5);
#4806=CIRCLE('',#12038,1.5);
#4807=CIRCLE('',#12040,2.5);
#4808=CIRCLE('',#12041,2.5);
#4809=CIRCLE('',#12043,2.5);
#4810=CIRCLE('',#12044,2.5);
#4811=CIRCLE('',#12047,1.5);
#4812=CIRCLE('',#12048,1.5);
#4813=CIRCLE('',#12051,1.5);
#4814=CIRCLE('',#12052,1.5);
#4815=CIRCLE('',#12055,1.5);
#4816=CIRCLE('',#12056,1.5);
#4817=CIRCLE('',#12059,1.5);
#4818=CIRCLE('',#12060,1.5);
#4819=CIRCLE('',#12062,10.);
#4820=CIRCLE('',#12063,10.);
#4821=CIRCLE('',#12065,2.5);
#4822=CIRCLE('',#12066,2.5);
#4823=CIRCLE('',#12068,2.5);
#4824=CIRCLE('',#12069,2.5);
#4825=CIRCLE('',#12071,0.5);
#4826=CIRCLE('',#12072,0.5);
#4827=CIRCLE('',#12075,0.5);
#4828=CIRCLE('',#12076,0.5);
#4829=CIRCLE('',#12078,2.);
#4830=CIRCLE('',#12079,1.99999999999999);
#4831=CIRCLE('',#12080,2.00000000000003);
#4832=CIRCLE('',#12081,1.99999999999999);
#4833=CIRCLE('',#12082,2.00000000000003);
#4834=CIRCLE('',#12083,2.);
#4835=CIRCLE('',#12084,1.99999999999999);
#4836=CIRCLE('',#12085,1.99999999999999);
#4837=CIRCLE('',#12086,1.99999999999999);
#4838=CIRCLE('',#12087,1.99999999999999);
#4839=CIRCLE('',#12088,1.99999999999999);
#4840=CIRCLE('',#12089,1.99999999999999);
#4841=CIRCLE('',#12090,2.);
#4842=CIRCLE('',#12091,1.99999999999999);
#4843=CIRCLE('',#12092,1.99999999999999);
#4844=CIRCLE('',#12093,1.99999999999999);
#4845=CIRCLE('',#12094,1.99999999999999);
#4846=CIRCLE('',#12095,2.);
#4847=CIRCLE('',#12096,2.);
#4848=CIRCLE('',#12097,2.00000000000003);
#4849=CIRCLE('',#12098,2.);
#4850=CIRCLE('',#12099,1.99999999999999);
#4851=CIRCLE('',#12100,2.);
#4852=CIRCLE('',#12101,1.99999999999999);
#4853=CIRCLE('',#12102,1.99999999999999);
#4854=CIRCLE('',#12103,1.99999999999999);
#4855=CIRCLE('',#12104,1.99999999999999);
#4856=CIRCLE('',#12105,1.99999999999999);
#4857=CIRCLE('',#12106,1.99999999999999);
#4858=CIRCLE('',#12107,1.99999999999999);
#4859=CIRCLE('',#12108,2.);
#4860=CIRCLE('',#12109,2.00000000000003);
#4861=CIRCLE('',#12110,1.99999999999999);
#4862=CIRCLE('',#12111,1.99999999999999);
#4863=CIRCLE('',#12112,1.99999999999999);
#4864=CIRCLE('',#12113,1.99999999999999);
#4865=CIRCLE('',#12114,2.);
#4866=CIRCLE('',#12115,2.00000000000003);
#4867=CIRCLE('',#12116,2.00000000000003);
#4868=CIRCLE('',#12117,2.00000000000003);
#4869=CIRCLE('',#12118,1.99999999999999);
#4870=CIRCLE('',#12119,1.99999999999999);
#4871=CIRCLE('',#12120,1.99999999999999);
#4872=CIRCLE('',#12121,2.00000000000003);
#4873=CIRCLE('',#12122,1.99999999999999);
#4874=CIRCLE('',#12123,1.99999999999999);
#4875=CIRCLE('',#12124,1.99999999999999);
#4876=CIRCLE('',#12126,2.);
#4877=CIRCLE('',#12127,2.);
#4878=CIRCLE('',#12130,2.);
#4879=CIRCLE('',#12132,2.);
#4880=CIRCLE('',#12134,2.);
#4881=CIRCLE('',#12136,1.99999999999999);
#4882=CIRCLE('',#12138,2.00000000000003);
#4883=CIRCLE('',#12140,1.99999999999999);
#4884=CIRCLE('',#12142,2.00000000000003);
#4885=CIRCLE('',#12144,2.);
#4886=CIRCLE('',#12146,1.99999999999999);
#4887=CIRCLE('',#12148,1.99999999999999);
#4888=CIRCLE('',#12150,1.99999999999999);
#4889=CIRCLE('',#12152,1.99999999999999);
#4890=CIRCLE('',#12154,1.99999999999999);
#4891=CIRCLE('',#12156,1.99999999999999);
#4892=CIRCLE('',#12158,2.);
#4893=CIRCLE('',#12160,1.99999999999999);
#4894=CIRCLE('',#12162,1.99999999999999);
#4895=CIRCLE('',#12164,1.99999999999999);
#4896=CIRCLE('',#12166,1.99999999999999);
#4897=CIRCLE('',#12168,2.);
#4898=CIRCLE('',#12170,2.);
#4899=CIRCLE('',#12172,2.00000000000003);
#4900=CIRCLE('',#12174,2.);
#4901=CIRCLE('',#12176,1.99999999999999);
#4902=CIRCLE('',#12178,2.);
#4903=CIRCLE('',#12180,1.99999999999999);
#4904=CIRCLE('',#12182,1.99999999999999);
#4905=CIRCLE('',#12184,1.99999999999999);
#4906=CIRCLE('',#12186,1.99999999999999);
#4907=CIRCLE('',#12188,1.99999999999999);
#4908=CIRCLE('',#12190,1.99999999999999);
#4909=CIRCLE('',#12192,1.99999999999999);
#4910=CIRCLE('',#12194,2.);
#4911=CIRCLE('',#12196,2.00000000000003);
#4912=CIRCLE('',#12198,1.99999999999999);
#4913=CIRCLE('',#12200,1.99999999999999);
#4914=CIRCLE('',#12202,1.99999999999999);
#4915=CIRCLE('',#12204,1.99999999999999);
#4916=CIRCLE('',#12206,2.);
#4917=CIRCLE('',#12208,2.00000000000003);
#4918=CIRCLE('',#12210,2.00000000000003);
#4919=CIRCLE('',#12212,2.00000000000003);
#4920=CIRCLE('',#12214,1.99999999999999);
#4921=CIRCLE('',#12216,1.99999999999999);
#4922=CIRCLE('',#12218,1.99999999999999);
#4923=CIRCLE('',#12220,2.00000000000003);
#4924=CIRCLE('',#12222,1.99999999999999);
#4925=CIRCLE('',#12224,1.99999999999999);
#4926=CIRCLE('',#12226,1.99999999999999);
#4927=CIRCLE('',#12230,2.);
#4928=CIRCLE('',#12231,2.);
#4929=CIRCLE('',#12233,1.99999999999999);
#4930=CIRCLE('',#12234,1.99999999999999);
#4931=CIRCLE('',#12236,2.00000000000003);
#4932=CIRCLE('',#12237,2.00000000000003);
#4933=CIRCLE('',#12239,1.99999999999999);
#4934=CIRCLE('',#12240,1.99999999999999);
#4935=CIRCLE('',#12242,2.00000000000003);
#4936=CIRCLE('',#12243,2.00000000000003);
#4937=CIRCLE('',#12245,2.);
#4938=CIRCLE('',#12246,2.);
#4939=CIRCLE('',#12248,1.99999999999999);
#4940=CIRCLE('',#12249,1.99999999999999);
#4941=CIRCLE('',#12251,1.99999999999999);
#4942=CIRCLE('',#12252,1.99999999999999);
#4943=CIRCLE('',#12254,1.99999999999999);
#4944=CIRCLE('',#12255,1.99999999999999);
#4945=CIRCLE('',#12257,1.99999999999999);
#4946=CIRCLE('',#12258,1.99999999999999);
#4947=CIRCLE('',#12260,1.99999999999999);
#4948=CIRCLE('',#12261,1.99999999999999);
#4949=CIRCLE('',#12263,1.99999999999999);
#4950=CIRCLE('',#12264,1.99999999999999);
#4951=CIRCLE('',#12266,2.);
#4952=CIRCLE('',#12267,2.);
#4953=CIRCLE('',#12269,1.99999999999999);
#4954=CIRCLE('',#12270,1.99999999999999);
#4955=CIRCLE('',#12272,1.99999999999999);
#4956=CIRCLE('',#12273,1.99999999999999);
#4957=CIRCLE('',#12275,1.99999999999999);
#4958=CIRCLE('',#12276,1.99999999999999);
#4959=CIRCLE('',#12278,1.99999999999999);
#4960=CIRCLE('',#12279,1.99999999999999);
#4961=CIRCLE('',#12281,2.);
#4962=CIRCLE('',#12282,2.);
#4963=CIRCLE('',#12284,2.);
#4964=CIRCLE('',#12285,2.);
#4965=CIRCLE('',#12287,2.00000000000003);
#4966=CIRCLE('',#12288,2.00000000000003);
#4967=CIRCLE('',#12290,2.);
#4968=CIRCLE('',#12291,2.);
#4969=CIRCLE('',#12293,1.99999999999999);
#4970=CIRCLE('',#12294,1.99999999999999);
#4971=CIRCLE('',#12296,2.);
#4972=CIRCLE('',#12297,2.);
#4973=CIRCLE('',#12299,1.99999999999999);
#4974=CIRCLE('',#12300,1.99999999999999);
#4975=CIRCLE('',#12302,1.99999999999999);
#4976=CIRCLE('',#12303,1.99999999999999);
#4977=CIRCLE('',#12305,1.99999999999999);
#4978=CIRCLE('',#12306,1.99999999999999);
#4979=CIRCLE('',#12308,1.99999999999999);
#4980=CIRCLE('',#12309,1.99999999999999);
#4981=CIRCLE('',#12311,1.99999999999999);
#4982=CIRCLE('',#12312,1.99999999999999);
#4983=CIRCLE('',#12314,1.99999999999999);
#4984=CIRCLE('',#12315,1.99999999999999);
#4985=CIRCLE('',#12317,1.99999999999999);
#4986=CIRCLE('',#12318,1.99999999999999);
#4987=CIRCLE('',#12320,2.);
#4988=CIRCLE('',#12321,2.);
#4989=CIRCLE('',#12323,2.00000000000003);
#4990=CIRCLE('',#12324,2.00000000000003);
#4991=CIRCLE('',#12326,1.99999999999999);
#4992=CIRCLE('',#12327,1.99999999999999);
#4993=CIRCLE('',#12329,1.99999999999999);
#4994=CIRCLE('',#12330,1.99999999999999);
#4995=CIRCLE('',#12332,1.99999999999999);
#4996=CIRCLE('',#12333,1.99999999999999);
#4997=CIRCLE('',#12335,1.99999999999999);
#4998=CIRCLE('',#12336,1.99999999999999);
#4999=CIRCLE('',#12338,2.);
#5000=CIRCLE('',#12339,2.);
#5001=CIRCLE('',#12341,2.00000000000003);
#5002=CIRCLE('',#12342,2.00000000000003);
#5003=CIRCLE('',#12344,2.00000000000003);
#5004=CIRCLE('',#12345,2.00000000000003);
#5005=CIRCLE('',#12347,2.00000000000003);
#5006=CIRCLE('',#12348,2.00000000000003);
#5007=CIRCLE('',#12350,1.99999999999999);
#5008=CIRCLE('',#12351,1.99999999999999);
#5009=CIRCLE('',#12353,1.99999999999999);
#5010=CIRCLE('',#12354,1.99999999999999);
#5011=CIRCLE('',#12356,1.99999999999999);
#5012=CIRCLE('',#12357,1.99999999999999);
#5013=CIRCLE('',#12359,2.00000000000003);
#5014=CIRCLE('',#12360,2.00000000000003);
#5015=CIRCLE('',#12362,1.99999999999999);
#5016=CIRCLE('',#12363,1.99999999999999);
#5017=CIRCLE('',#12365,1.99999999999999);
#5018=CIRCLE('',#12366,1.99999999999999);
#5019=CIRCLE('',#12368,1.99999999999999);
#5020=CIRCLE('',#12369,1.99999999999999);
#5385=VERTEX_POINT('',#16743);
#5386=VERTEX_POINT('',#16745);
#5387=VERTEX_POINT('',#16749);
#5388=VERTEX_POINT('',#16751);
#5389=VERTEX_POINT('',#16755);
#5390=VERTEX_POINT('',#16757);
#5391=VERTEX_POINT('',#16761);
#5392=VERTEX_POINT('',#16763);
#5393=VERTEX_POINT('',#16767);
#5394=VERTEX_POINT('',#16769);
#5395=VERTEX_POINT('',#16773);
#5396=VERTEX_POINT('',#16774);
#5397=VERTEX_POINT('',#16776);
#5398=VERTEX_POINT('',#16778);
#5399=VERTEX_POINT('',#16782);
#5400=VERTEX_POINT('',#16784);
#5401=VERTEX_POINT('',#16788);
#5402=VERTEX_POINT('',#16790);
#5403=VERTEX_POINT('',#16797);
#5404=VERTEX_POINT('',#16798);
#5405=VERTEX_POINT('',#16800);
#5406=VERTEX_POINT('',#16802);
#5407=VERTEX_POINT('',#16806);
#5408=VERTEX_POINT('',#16808);
#5409=VERTEX_POINT('',#16812);
#5410=VERTEX_POINT('',#16814);
#5411=VERTEX_POINT('',#16821);
#5412=VERTEX_POINT('',#16823);
#5413=VERTEX_POINT('',#16827);
#5414=VERTEX_POINT('',#16829);
#5415=VERTEX_POINT('',#16833);
#5416=VERTEX_POINT('',#16835);
#5417=VERTEX_POINT('',#16839);
#5418=VERTEX_POINT('',#16841);
#5419=VERTEX_POINT('',#16845);
#5420=VERTEX_POINT('',#16847);
#5421=VERTEX_POINT('',#16851);
#5422=VERTEX_POINT('',#16852);
#5423=VERTEX_POINT('',#16854);
#5424=VERTEX_POINT('',#16856);
#5425=VERTEX_POINT('',#16860);
#5426=VERTEX_POINT('',#16862);
#5427=VERTEX_POINT('',#16866);
#5428=VERTEX_POINT('',#16868);
#5429=VERTEX_POINT('',#16875);
#5430=VERTEX_POINT('',#16876);
#5431=VERTEX_POINT('',#16878);
#5432=VERTEX_POINT('',#16880);
#5433=VERTEX_POINT('',#16884);
#5434=VERTEX_POINT('',#16886);
#5435=VERTEX_POINT('',#16890);
#5436=VERTEX_POINT('',#16892);
#5437=VERTEX_POINT('',#16899);
#5438=VERTEX_POINT('',#16901);
#5439=VERTEX_POINT('',#16905);
#5440=VERTEX_POINT('',#16907);
#5441=VERTEX_POINT('',#16911);
#5442=VERTEX_POINT('',#16913);
#5443=VERTEX_POINT('',#16917);
#5444=VERTEX_POINT('',#16919);
#5445=VERTEX_POINT('',#16923);
#5446=VERTEX_POINT('',#16925);
#5447=VERTEX_POINT('',#16929);
#5448=VERTEX_POINT('',#16930);
#5449=VERTEX_POINT('',#16932);
#5450=VERTEX_POINT('',#16934);
#5451=VERTEX_POINT('',#16938);
#5452=VERTEX_POINT('',#16940);
#5453=VERTEX_POINT('',#16944);
#5454=VERTEX_POINT('',#16946);
#5455=VERTEX_POINT('',#16953);
#5456=VERTEX_POINT('',#16954);
#5457=VERTEX_POINT('',#16956);
#5458=VERTEX_POINT('',#16958);
#5459=VERTEX_POINT('',#16962);
#5460=VERTEX_POINT('',#16964);
#5461=VERTEX_POINT('',#16968);
#5462=VERTEX_POINT('',#16970);
#5463=VERTEX_POINT('',#16977);
#5464=VERTEX_POINT('',#16979);
#5465=VERTEX_POINT('',#16983);
#5466=VERTEX_POINT('',#16985);
#5467=VERTEX_POINT('',#16989);
#5468=VERTEX_POINT('',#16991);
#5469=VERTEX_POINT('',#16995);
#5470=VERTEX_POINT('',#16997);
#5471=VERTEX_POINT('',#17001);
#5472=VERTEX_POINT('',#17003);
#5473=VERTEX_POINT('',#17007);
#5474=VERTEX_POINT('',#17008);
#5475=VERTEX_POINT('',#17010);
#5476=VERTEX_POINT('',#17012);
#5477=VERTEX_POINT('',#17016);
#5478=VERTEX_POINT('',#17018);
#5479=VERTEX_POINT('',#17022);
#5480=VERTEX_POINT('',#17024);
#5481=VERTEX_POINT('',#17031);
#5482=VERTEX_POINT('',#17032);
#5483=VERTEX_POINT('',#17034);
#5484=VERTEX_POINT('',#17036);
#5485=VERTEX_POINT('',#17040);
#5486=VERTEX_POINT('',#17042);
#5487=VERTEX_POINT('',#17046);
#5488=VERTEX_POINT('',#17048);
#5489=VERTEX_POINT('',#17055);
#5490=VERTEX_POINT('',#17057);
#5491=VERTEX_POINT('',#17061);
#5492=VERTEX_POINT('',#17063);
#5493=VERTEX_POINT('',#17067);
#5494=VERTEX_POINT('',#17069);
#5495=VERTEX_POINT('',#17073);
#5496=VERTEX_POINT('',#17075);
#5497=VERTEX_POINT('',#17079);
#5498=VERTEX_POINT('',#17081);
#5499=VERTEX_POINT('',#17085);
#5500=VERTEX_POINT('',#17086);
#5501=VERTEX_POINT('',#17088);
#5502=VERTEX_POINT('',#17090);
#5503=VERTEX_POINT('',#17094);
#5504=VERTEX_POINT('',#17096);
#5505=VERTEX_POINT('',#17100);
#5506=VERTEX_POINT('',#17102);
#5507=VERTEX_POINT('',#17109);
#5508=VERTEX_POINT('',#17110);
#5509=VERTEX_POINT('',#17112);
#5510=VERTEX_POINT('',#17114);
#5511=VERTEX_POINT('',#17118);
#5512=VERTEX_POINT('',#17120);
#5513=VERTEX_POINT('',#17124);
#5514=VERTEX_POINT('',#17126);
#5515=VERTEX_POINT('',#17133);
#5516=VERTEX_POINT('',#17135);
#5517=VERTEX_POINT('',#17139);
#5518=VERTEX_POINT('',#17141);
#5519=VERTEX_POINT('',#17145);
#5520=VERTEX_POINT('',#17147);
#5521=VERTEX_POINT('',#17151);
#5522=VERTEX_POINT('',#17153);
#5523=VERTEX_POINT('',#17157);
#5524=VERTEX_POINT('',#17159);
#5525=VERTEX_POINT('',#17163);
#5526=VERTEX_POINT('',#17164);
#5527=VERTEX_POINT('',#17166);
#5528=VERTEX_POINT('',#17168);
#5529=VERTEX_POINT('',#17172);
#5530=VERTEX_POINT('',#17174);
#5531=VERTEX_POINT('',#17178);
#5532=VERTEX_POINT('',#17180);
#5533=VERTEX_POINT('',#17187);
#5534=VERTEX_POINT('',#17188);
#5535=VERTEX_POINT('',#17190);
#5536=VERTEX_POINT('',#17192);
#5537=VERTEX_POINT('',#17196);
#5538=VERTEX_POINT('',#17198);
#5539=VERTEX_POINT('',#17202);
#5540=VERTEX_POINT('',#17204);
#5541=VERTEX_POINT('',#17211);
#5542=VERTEX_POINT('',#17213);
#5543=VERTEX_POINT('',#17217);
#5544=VERTEX_POINT('',#17219);
#5545=VERTEX_POINT('',#17223);
#5546=VERTEX_POINT('',#17225);
#5547=VERTEX_POINT('',#17229);
#5548=VERTEX_POINT('',#17231);
#5549=VERTEX_POINT('',#17235);
#5550=VERTEX_POINT('',#17237);
#5551=VERTEX_POINT('',#17241);
#5552=VERTEX_POINT('',#17242);
#5553=VERTEX_POINT('',#17244);
#5554=VERTEX_POINT('',#17246);
#5555=VERTEX_POINT('',#17250);
#5556=VERTEX_POINT('',#17252);
#5557=VERTEX_POINT('',#17256);
#5558=VERTEX_POINT('',#17258);
#5559=VERTEX_POINT('',#17265);
#5560=VERTEX_POINT('',#17266);
#5561=VERTEX_POINT('',#17268);
#5562=VERTEX_POINT('',#17270);
#5563=VERTEX_POINT('',#17274);
#5564=VERTEX_POINT('',#17276);
#5565=VERTEX_POINT('',#17280);
#5566=VERTEX_POINT('',#17282);
#5567=VERTEX_POINT('',#17289);
#5568=VERTEX_POINT('',#17291);
#5569=VERTEX_POINT('',#17295);
#5570=VERTEX_POINT('',#17297);
#5571=VERTEX_POINT('',#17301);
#5572=VERTEX_POINT('',#17303);
#5573=VERTEX_POINT('',#17307);
#5574=VERTEX_POINT('',#17309);
#5575=VERTEX_POINT('',#17313);
#5576=VERTEX_POINT('',#17315);
#5577=VERTEX_POINT('',#17319);
#5578=VERTEX_POINT('',#17320);
#5579=VERTEX_POINT('',#17322);
#5580=VERTEX_POINT('',#17324);
#5581=VERTEX_POINT('',#17328);
#5582=VERTEX_POINT('',#17330);
#5583=VERTEX_POINT('',#17334);
#5584=VERTEX_POINT('',#17336);
#5585=VERTEX_POINT('',#17343);
#5586=VERTEX_POINT('',#17344);
#5587=VERTEX_POINT('',#17346);
#5588=VERTEX_POINT('',#17348);
#5589=VERTEX_POINT('',#17352);
#5590=VERTEX_POINT('',#17354);
#5591=VERTEX_POINT('',#17358);
#5592=VERTEX_POINT('',#17360);
#5593=VERTEX_POINT('',#17367);
#5594=VERTEX_POINT('',#17369);
#5595=VERTEX_POINT('',#17373);
#5596=VERTEX_POINT('',#17375);
#5597=VERTEX_POINT('',#17379);
#5598=VERTEX_POINT('',#17381);
#5599=VERTEX_POINT('',#17385);
#5600=VERTEX_POINT('',#17387);
#5601=VERTEX_POINT('',#17391);
#5602=VERTEX_POINT('',#17393);
#5603=VERTEX_POINT('',#17397);
#5604=VERTEX_POINT('',#17398);
#5605=VERTEX_POINT('',#17400);
#5606=VERTEX_POINT('',#17402);
#5607=VERTEX_POINT('',#17406);
#5608=VERTEX_POINT('',#17408);
#5609=VERTEX_POINT('',#17412);
#5610=VERTEX_POINT('',#17414);
#5611=VERTEX_POINT('',#17421);
#5612=VERTEX_POINT('',#17422);
#5613=VERTEX_POINT('',#17424);
#5614=VERTEX_POINT('',#17426);
#5615=VERTEX_POINT('',#17430);
#5616=VERTEX_POINT('',#17432);
#5617=VERTEX_POINT('',#17436);
#5618=VERTEX_POINT('',#17438);
#5619=VERTEX_POINT('',#17445);
#5620=VERTEX_POINT('',#17447);
#5621=VERTEX_POINT('',#17451);
#5622=VERTEX_POINT('',#17453);
#5623=VERTEX_POINT('',#17457);
#5624=VERTEX_POINT('',#17458);
#5625=VERTEX_POINT('',#17460);
#5626=VERTEX_POINT('',#17462);
#5627=VERTEX_POINT('',#17466);
#5628=VERTEX_POINT('',#17468);
#5629=VERTEX_POINT('',#17472);
#5630=VERTEX_POINT('',#17474);
#5631=VERTEX_POINT('',#17481);
#5632=VERTEX_POINT('',#17482);
#5633=VERTEX_POINT('',#17484);
#5634=VERTEX_POINT('',#17486);
#5635=VERTEX_POINT('',#17490);
#5636=VERTEX_POINT('',#17492);
#5637=VERTEX_POINT('',#17496);
#5638=VERTEX_POINT('',#17498);
#5639=VERTEX_POINT('',#17505);
#5640=VERTEX_POINT('',#17507);
#5641=VERTEX_POINT('',#17511);
#5642=VERTEX_POINT('',#17513);
#5643=VERTEX_POINT('',#17517);
#5644=VERTEX_POINT('',#17519);
#5645=VERTEX_POINT('',#17523);
#5646=VERTEX_POINT('',#17524);
#5647=VERTEX_POINT('',#17526);
#5648=VERTEX_POINT('',#17528);
#5649=VERTEX_POINT('',#17532);
#5650=VERTEX_POINT('',#17534);
#5651=VERTEX_POINT('',#17538);
#5652=VERTEX_POINT('',#17540);
#5653=VERTEX_POINT('',#17544);
#5654=VERTEX_POINT('',#17546);
#5655=VERTEX_POINT('',#17549);
#5656=VERTEX_POINT('',#17551);
#5657=VERTEX_POINT('',#17553);
#5658=VERTEX_POINT('',#17555);
#5659=VERTEX_POINT('',#17557);
#5660=VERTEX_POINT('',#17559);
#5661=VERTEX_POINT('',#17561);
#5662=VERTEX_POINT('',#17563);
#5663=VERTEX_POINT('',#17565);
#5664=VERTEX_POINT('',#17567);
#5665=VERTEX_POINT('',#17569);
#5666=VERTEX_POINT('',#17571);
#5667=VERTEX_POINT('',#17573);
#5668=VERTEX_POINT('',#17575);
#5669=VERTEX_POINT('',#17577);
#5670=VERTEX_POINT('',#17579);
#5671=VERTEX_POINT('',#17581);
#5672=VERTEX_POINT('',#17583);
#5673=VERTEX_POINT('',#17585);
#5674=VERTEX_POINT('',#17587);
#5675=VERTEX_POINT('',#17589);
#5676=VERTEX_POINT('',#17591);
#5677=VERTEX_POINT('',#17593);
#5678=VERTEX_POINT('',#17595);
#5679=VERTEX_POINT('',#17597);
#5680=VERTEX_POINT('',#17599);
#5681=VERTEX_POINT('',#17601);
#5682=VERTEX_POINT('',#17603);
#5683=VERTEX_POINT('',#17605);
#5684=VERTEX_POINT('',#17607);
#5685=VERTEX_POINT('',#17609);
#5686=VERTEX_POINT('',#17611);
#5687=VERTEX_POINT('',#17613);
#5688=VERTEX_POINT('',#17615);
#5689=VERTEX_POINT('',#17617);
#5690=VERTEX_POINT('',#17619);
#5691=VERTEX_POINT('',#17621);
#5692=VERTEX_POINT('',#17623);
#5693=VERTEX_POINT('',#17625);
#5694=VERTEX_POINT('',#17627);
#5695=VERTEX_POINT('',#17629);
#5696=VERTEX_POINT('',#17631);
#5697=VERTEX_POINT('',#17633);
#5698=VERTEX_POINT('',#17635);
#5699=VERTEX_POINT('',#17637);
#5700=VERTEX_POINT('',#17639);
#5701=VERTEX_POINT('',#17641);
#5702=VERTEX_POINT('',#17644);
#5703=VERTEX_POINT('',#17645);
#5704=VERTEX_POINT('',#17647);
#5705=VERTEX_POINT('',#17649);
#5706=VERTEX_POINT('',#17653);
#5707=VERTEX_POINT('',#17655);
#5708=VERTEX_POINT('',#17659);
#5709=VERTEX_POINT('',#17662);
#5710=VERTEX_POINT('',#17664);
#5711=VERTEX_POINT('',#17666);
#5712=VERTEX_POINT('',#17670);
#5713=VERTEX_POINT('',#17674);
#5714=VERTEX_POINT('',#17678);
#5715=VERTEX_POINT('',#17682);
#5716=VERTEX_POINT('',#17686);
#5717=VERTEX_POINT('',#17690);
#5718=VERTEX_POINT('',#17694);
#5719=VERTEX_POINT('',#17698);
#5720=VERTEX_POINT('',#17702);
#5721=VERTEX_POINT('',#17706);
#5722=VERTEX_POINT('',#17710);
#5723=VERTEX_POINT('',#17714);
#5724=VERTEX_POINT('',#17718);
#5725=VERTEX_POINT('',#17722);
#5726=VERTEX_POINT('',#17726);
#5727=VERTEX_POINT('',#17730);
#5728=VERTEX_POINT('',#17734);
#5729=VERTEX_POINT('',#17738);
#5730=VERTEX_POINT('',#17742);
#5731=VERTEX_POINT('',#17746);
#5732=VERTEX_POINT('',#17750);
#5733=VERTEX_POINT('',#17754);
#5734=VERTEX_POINT('',#17758);
#5735=VERTEX_POINT('',#17762);
#5736=VERTEX_POINT('',#17766);
#5737=VERTEX_POINT('',#17770);
#5738=VERTEX_POINT('',#17774);
#5739=VERTEX_POINT('',#17778);
#5740=VERTEX_POINT('',#17782);
#5741=VERTEX_POINT('',#17786);
#5742=VERTEX_POINT('',#17790);
#5743=VERTEX_POINT('',#17794);
#5744=VERTEX_POINT('',#17798);
#5745=VERTEX_POINT('',#17802);
#5746=VERTEX_POINT('',#17806);
#5747=VERTEX_POINT('',#17810);
#5748=VERTEX_POINT('',#17814);
#5749=VERTEX_POINT('',#17818);
#5750=VERTEX_POINT('',#17822);
#5751=VERTEX_POINT('',#17826);
#5752=VERTEX_POINT('',#17830);
#5753=VERTEX_POINT('',#17834);
#5754=VERTEX_POINT('',#17838);
#5755=VERTEX_POINT('',#17842);
#5756=VERTEX_POINT('',#17846);
#5757=VERTEX_POINT('',#17850);
#5758=VERTEX_POINT('',#17854);
#5759=VERTEX_POINT('',#17858);
#5760=VERTEX_POINT('',#17862);
#5761=VERTEX_POINT('',#17868);
#5762=VERTEX_POINT('',#17870);
#5763=VERTEX_POINT('',#17874);
#5764=VERTEX_POINT('',#17876);
#5765=VERTEX_POINT('',#17880);
#5766=VERTEX_POINT('',#17882);
#5767=VERTEX_POINT('',#17886);
#5768=VERTEX_POINT('',#17888);
#5769=VERTEX_POINT('',#17892);
#5770=VERTEX_POINT('',#17894);
#5771=VERTEX_POINT('',#17898);
#5772=VERTEX_POINT('',#17900);
#5773=VERTEX_POINT('',#17904);
#5774=VERTEX_POINT('',#17906);
#5775=VERTEX_POINT('',#17910);
#5776=VERTEX_POINT('',#17912);
#5777=VERTEX_POINT('',#17916);
#5778=VERTEX_POINT('',#17918);
#5779=VERTEX_POINT('',#17922);
#5780=VERTEX_POINT('',#17924);
#5781=VERTEX_POINT('',#17928);
#5782=VERTEX_POINT('',#17930);
#5783=VERTEX_POINT('',#17934);
#5784=VERTEX_POINT('',#17936);
#5785=VERTEX_POINT('',#17940);
#5786=VERTEX_POINT('',#17942);
#5787=VERTEX_POINT('',#17946);
#5788=VERTEX_POINT('',#17948);
#5789=VERTEX_POINT('',#17952);
#5790=VERTEX_POINT('',#17954);
#5791=VERTEX_POINT('',#17958);
#5792=VERTEX_POINT('',#17960);
#5793=VERTEX_POINT('',#17964);
#5794=VERTEX_POINT('',#17966);
#5795=VERTEX_POINT('',#17970);
#5796=VERTEX_POINT('',#17972);
#5797=VERTEX_POINT('',#17976);
#5798=VERTEX_POINT('',#17978);
#5799=VERTEX_POINT('',#17982);
#5800=VERTEX_POINT('',#17984);
#5801=VERTEX_POINT('',#17988);
#5802=VERTEX_POINT('',#17990);
#5803=VERTEX_POINT('',#17994);
#5804=VERTEX_POINT('',#17996);
#5805=VERTEX_POINT('',#18000);
#5806=VERTEX_POINT('',#18002);
#5807=VERTEX_POINT('',#18006);
#5808=VERTEX_POINT('',#18008);
#5809=VERTEX_POINT('',#18012);
#5810=VERTEX_POINT('',#18014);
#5811=VERTEX_POINT('',#18018);
#5812=VERTEX_POINT('',#18020);
#5813=VERTEX_POINT('',#18024);
#5814=VERTEX_POINT('',#18026);
#5815=VERTEX_POINT('',#18030);
#5816=VERTEX_POINT('',#18032);
#5817=VERTEX_POINT('',#18036);
#5818=VERTEX_POINT('',#18038);
#5819=VERTEX_POINT('',#18042);
#5820=VERTEX_POINT('',#18044);
#5821=VERTEX_POINT('',#18048);
#5822=VERTEX_POINT('',#18050);
#5823=VERTEX_POINT('',#18054);
#5824=VERTEX_POINT('',#18056);
#5825=VERTEX_POINT('',#18060);
#5826=VERTEX_POINT('',#18062);
#5827=VERTEX_POINT('',#18066);
#5828=VERTEX_POINT('',#18068);
#5829=VERTEX_POINT('',#18072);
#5830=VERTEX_POINT('',#18074);
#5831=VERTEX_POINT('',#18078);
#5832=VERTEX_POINT('',#18080);
#5833=VERTEX_POINT('',#18084);
#5834=VERTEX_POINT('',#18086);
#5835=VERTEX_POINT('',#18090);
#5836=VERTEX_POINT('',#18092);
#5837=VERTEX_POINT('',#18096);
#5838=VERTEX_POINT('',#18098);
#5839=VERTEX_POINT('',#18102);
#5840=VERTEX_POINT('',#18104);
#5841=VERTEX_POINT('',#18108);
#5842=VERTEX_POINT('',#18110);
#5843=VERTEX_POINT('',#18114);
#5844=VERTEX_POINT('',#18116);
#5845=VERTEX_POINT('',#18120);
#5846=VERTEX_POINT('',#18122);
#5847=VERTEX_POINT('',#18126);
#5848=VERTEX_POINT('',#18128);
#5849=VERTEX_POINT('',#18132);
#5850=VERTEX_POINT('',#18134);
#5851=VERTEX_POINT('',#18138);
#5852=VERTEX_POINT('',#18140);
#5853=VERTEX_POINT('',#18144);
#5854=VERTEX_POINT('',#18146);
#5855=VERTEX_POINT('',#18150);
#5856=VERTEX_POINT('',#18152);
#6509=EDGE_CURVE('',#5385,#5385,#4645,.T.);
#6510=EDGE_CURVE('',#5385,#5386,#1017,.T.);
#6511=EDGE_CURVE('',#5386,#5386,#4646,.T.);
#6512=EDGE_CURVE('',#5387,#5387,#4647,.T.);
#6513=EDGE_CURVE('',#5387,#5388,#1018,.T.);
#6514=EDGE_CURVE('',#5388,#5388,#4648,.T.);
#6515=EDGE_CURVE('',#5389,#5389,#4649,.T.);
#6516=EDGE_CURVE('',#5389,#5390,#1019,.T.);
#6517=EDGE_CURVE('',#5390,#5390,#4650,.T.);
#6518=EDGE_CURVE('',#5391,#5391,#4651,.T.);
#6519=EDGE_CURVE('',#5391,#5392,#1020,.T.);
#6520=EDGE_CURVE('',#5392,#5392,#4652,.T.);
#6521=EDGE_CURVE('',#5393,#5393,#4653,.T.);
#6522=EDGE_CURVE('',#5393,#5394,#1021,.T.);
#6523=EDGE_CURVE('',#5394,#5394,#4654,.T.);
#6524=EDGE_CURVE('',#5395,#5396,#1022,.T.);
#6525=EDGE_CURVE('',#5397,#5395,#1023,.T.);
#6526=EDGE_CURVE('',#5398,#5397,#1024,.T.);
#6527=EDGE_CURVE('',#5398,#5396,#1025,.T.);
#6528=EDGE_CURVE('',#5396,#5399,#4655,.T.);
#6529=EDGE_CURVE('',#5400,#5398,#4656,.T.);
#6530=EDGE_CURVE('',#5400,#5399,#1026,.T.);
#6531=EDGE_CURVE('',#5399,#5401,#1027,.T.);
#6532=EDGE_CURVE('',#5402,#5400,#1028,.T.);
#6533=EDGE_CURVE('',#5402,#5401,#1029,.T.);
#6534=EDGE_CURVE('',#5401,#5395,#4657,.T.);
#6535=EDGE_CURVE('',#5397,#5402,#4658,.T.);
#6536=EDGE_CURVE('',#5403,#5404,#1030,.T.);
#6537=EDGE_CURVE('',#5405,#5403,#1031,.T.);
#6538=EDGE_CURVE('',#5406,#5405,#1032,.T.);
#6539=EDGE_CURVE('',#5406,#5404,#1033,.T.);
#6540=EDGE_CURVE('',#5404,#5407,#4659,.T.);
#6541=EDGE_CURVE('',#5408,#5406,#4660,.T.);
#6542=EDGE_CURVE('',#5408,#5407,#1034,.T.);
#6543=EDGE_CURVE('',#5407,#5409,#1035,.T.);
#6544=EDGE_CURVE('',#5410,#5408,#1036,.T.);
#6545=EDGE_CURVE('',#5410,#5409,#1037,.T.);
#6546=EDGE_CURVE('',#5409,#5403,#4661,.T.);
#6547=EDGE_CURVE('',#5405,#5410,#4662,.T.);
#6548=EDGE_CURVE('',#5411,#5411,#4663,.T.);
#6549=EDGE_CURVE('',#5411,#5412,#1038,.T.);
#6550=EDGE_CURVE('',#5412,#5412,#4664,.T.);
#6551=EDGE_CURVE('',#5413,#5413,#4665,.T.);
#6552=EDGE_CURVE('',#5413,#5414,#1039,.T.);
#6553=EDGE_CURVE('',#5414,#5414,#4666,.T.);
#6554=EDGE_CURVE('',#5415,#5415,#4667,.T.);
#6555=EDGE_CURVE('',#5415,#5416,#1040,.T.);
#6556=EDGE_CURVE('',#5416,#5416,#4668,.T.);
#6557=EDGE_CURVE('',#5417,#5417,#4669,.T.);
#6558=EDGE_CURVE('',#5417,#5418,#1041,.T.);
#6559=EDGE_CURVE('',#5418,#5418,#4670,.T.);
#6560=EDGE_CURVE('',#5419,#5419,#4671,.T.);
#6561=EDGE_CURVE('',#5419,#5420,#1042,.T.);
#6562=EDGE_CURVE('',#5420,#5420,#4672,.T.);
#6563=EDGE_CURVE('',#5421,#5422,#1043,.T.);
#6564=EDGE_CURVE('',#5423,#5421,#1044,.T.);
#6565=EDGE_CURVE('',#5424,#5423,#1045,.T.);
#6566=EDGE_CURVE('',#5424,#5422,#1046,.T.);
#6567=EDGE_CURVE('',#5422,#5425,#4673,.T.);
#6568=EDGE_CURVE('',#5426,#5424,#4674,.T.);
#6569=EDGE_CURVE('',#5426,#5425,#1047,.T.);
#6570=EDGE_CURVE('',#5425,#5427,#1048,.T.);
#6571=EDGE_CURVE('',#5428,#5426,#1049,.T.);
#6572=EDGE_CURVE('',#5428,#5427,#1050,.T.);
#6573=EDGE_CURVE('',#5427,#5421,#4675,.T.);
#6574=EDGE_CURVE('',#5423,#5428,#4676,.T.);
#6575=EDGE_CURVE('',#5429,#5430,#1051,.T.);
#6576=EDGE_CURVE('',#5431,#5429,#1052,.T.);
#6577=EDGE_CURVE('',#5432,#5431,#1053,.T.);
#6578=EDGE_CURVE('',#5432,#5430,#1054,.T.);
#6579=EDGE_CURVE('',#5430,#5433,#4677,.T.);
#6580=EDGE_CURVE('',#5434,#5432,#4678,.T.);
#6581=EDGE_CURVE('',#5434,#5433,#1055,.T.);
#6582=EDGE_CURVE('',#5433,#5435,#1056,.T.);
#6583=EDGE_CURVE('',#5436,#5434,#1057,.T.);
#6584=EDGE_CURVE('',#5436,#5435,#1058,.T.);
#6585=EDGE_CURVE('',#5435,#5429,#4679,.T.);
#6586=EDGE_CURVE('',#5431,#5436,#4680,.T.);
#6587=EDGE_CURVE('',#5437,#5437,#4681,.T.);
#6588=EDGE_CURVE('',#5437,#5438,#1059,.T.);
#6589=EDGE_CURVE('',#5438,#5438,#4682,.T.);
#6590=EDGE_CURVE('',#5439,#5439,#4683,.T.);
#6591=EDGE_CURVE('',#5439,#5440,#1060,.T.);
#6592=EDGE_CURVE('',#5440,#5440,#4684,.T.);
#6593=EDGE_CURVE('',#5441,#5441,#4685,.T.);
#6594=EDGE_CURVE('',#5441,#5442,#1061,.T.);
#6595=EDGE_CURVE('',#5442,#5442,#4686,.T.);
#6596=EDGE_CURVE('',#5443,#5443,#4687,.T.);
#6597=EDGE_CURVE('',#5443,#5444,#1062,.T.);
#6598=EDGE_CURVE('',#5444,#5444,#4688,.T.);
#6599=EDGE_CURVE('',#5445,#5445,#4689,.T.);
#6600=EDGE_CURVE('',#5445,#5446,#1063,.T.);
#6601=EDGE_CURVE('',#5446,#5446,#4690,.T.);
#6602=EDGE_CURVE('',#5447,#5448,#1064,.T.);
#6603=EDGE_CURVE('',#5449,#5447,#1065,.T.);
#6604=EDGE_CURVE('',#5450,#5449,#1066,.T.);
#6605=EDGE_CURVE('',#5450,#5448,#1067,.T.);
#6606=EDGE_CURVE('',#5448,#5451,#4691,.T.);
#6607=EDGE_CURVE('',#5452,#5450,#4692,.T.);
#6608=EDGE_CURVE('',#5452,#5451,#1068,.T.);
#6609=EDGE_CURVE('',#5451,#5453,#1069,.T.);
#6610=EDGE_CURVE('',#5454,#5452,#1070,.T.);
#6611=EDGE_CURVE('',#5454,#5453,#1071,.T.);
#6612=EDGE_CURVE('',#5453,#5447,#4693,.T.);
#6613=EDGE_CURVE('',#5449,#5454,#4694,.T.);
#6614=EDGE_CURVE('',#5455,#5456,#1072,.T.);
#6615=EDGE_CURVE('',#5457,#5455,#1073,.T.);
#6616=EDGE_CURVE('',#5458,#5457,#1074,.T.);
#6617=EDGE_CURVE('',#5458,#5456,#1075,.T.);
#6618=EDGE_CURVE('',#5456,#5459,#4695,.T.);
#6619=EDGE_CURVE('',#5460,#5458,#4696,.T.);
#6620=EDGE_CURVE('',#5460,#5459,#1076,.T.);
#6621=EDGE_CURVE('',#5459,#5461,#1077,.T.);
#6622=EDGE_CURVE('',#5462,#5460,#1078,.T.);
#6623=EDGE_CURVE('',#5462,#5461,#1079,.T.);
#6624=EDGE_CURVE('',#5461,#5455,#4697,.T.);
#6625=EDGE_CURVE('',#5457,#5462,#4698,.T.);
#6626=EDGE_CURVE('',#5463,#5463,#4699,.T.);
#6627=EDGE_CURVE('',#5463,#5464,#1080,.T.);
#6628=EDGE_CURVE('',#5464,#5464,#4700,.T.);
#6629=EDGE_CURVE('',#5465,#5465,#4701,.T.);
#6630=EDGE_CURVE('',#5465,#5466,#1081,.T.);
#6631=EDGE_CURVE('',#5466,#5466,#4702,.T.);
#6632=EDGE_CURVE('',#5467,#5467,#4703,.T.);
#6633=EDGE_CURVE('',#5467,#5468,#1082,.T.);
#6634=EDGE_CURVE('',#5468,#5468,#4704,.T.);
#6635=EDGE_CURVE('',#5469,#5469,#4705,.T.);
#6636=EDGE_CURVE('',#5469,#5470,#1083,.T.);
#6637=EDGE_CURVE('',#5470,#5470,#4706,.T.);
#6638=EDGE_CURVE('',#5471,#5471,#4707,.T.);
#6639=EDGE_CURVE('',#5471,#5472,#1084,.T.);
#6640=EDGE_CURVE('',#5472,#5472,#4708,.T.);
#6641=EDGE_CURVE('',#5473,#5474,#1085,.T.);
#6642=EDGE_CURVE('',#5475,#5473,#1086,.T.);
#6643=EDGE_CURVE('',#5476,#5475,#1087,.T.);
#6644=EDGE_CURVE('',#5476,#5474,#1088,.T.);
#6645=EDGE_CURVE('',#5474,#5477,#4709,.T.);
#6646=EDGE_CURVE('',#5478,#5476,#4710,.T.);
#6647=EDGE_CURVE('',#5478,#5477,#1089,.T.);
#6648=EDGE_CURVE('',#5477,#5479,#1090,.T.);
#6649=EDGE_CURVE('',#5480,#5478,#1091,.T.);
#6650=EDGE_CURVE('',#5480,#5479,#1092,.T.);
#6651=EDGE_CURVE('',#5479,#5473,#4711,.T.);
#6652=EDGE_CURVE('',#5475,#5480,#4712,.T.);
#6653=EDGE_CURVE('',#5481,#5482,#1093,.T.);
#6654=EDGE_CURVE('',#5483,#5481,#1094,.T.);
#6655=EDGE_CURVE('',#5484,#5483,#1095,.T.);
#6656=EDGE_CURVE('',#5484,#5482,#1096,.T.);
#6657=EDGE_CURVE('',#5482,#5485,#4713,.T.);
#6658=EDGE_CURVE('',#5486,#5484,#4714,.T.);
#6659=EDGE_CURVE('',#5486,#5485,#1097,.T.);
#6660=EDGE_CURVE('',#5485,#5487,#1098,.T.);
#6661=EDGE_CURVE('',#5488,#5486,#1099,.T.);
#6662=EDGE_CURVE('',#5488,#5487,#1100,.T.);
#6663=EDGE_CURVE('',#5487,#5481,#4715,.T.);
#6664=EDGE_CURVE('',#5483,#5488,#4716,.T.);
#6665=EDGE_CURVE('',#5489,#5489,#4717,.T.);
#6666=EDGE_CURVE('',#5489,#5490,#1101,.T.);
#6667=EDGE_CURVE('',#5490,#5490,#4718,.T.);
#6668=EDGE_CURVE('',#5491,#5491,#4719,.T.);
#6669=EDGE_CURVE('',#5491,#5492,#1102,.T.);
#6670=EDGE_CURVE('',#5492,#5492,#4720,.T.);
#6671=EDGE_CURVE('',#5493,#5493,#4721,.T.);
#6672=EDGE_CURVE('',#5493,#5494,#1103,.T.);
#6673=EDGE_CURVE('',#5494,#5494,#4722,.T.);
#6674=EDGE_CURVE('',#5495,#5495,#4723,.T.);
#6675=EDGE_CURVE('',#5495,#5496,#1104,.T.);
#6676=EDGE_CURVE('',#5496,#5496,#4724,.T.);
#6677=EDGE_CURVE('',#5497,#5497,#4725,.T.);
#6678=EDGE_CURVE('',#5497,#5498,#1105,.T.);
#6679=EDGE_CURVE('',#5498,#5498,#4726,.T.);
#6680=EDGE_CURVE('',#5499,#5500,#1106,.T.);
#6681=EDGE_CURVE('',#5501,#5499,#1107,.T.);
#6682=EDGE_CURVE('',#5502,#5501,#1108,.T.);
#6683=EDGE_CURVE('',#5502,#5500,#1109,.T.);
#6684=EDGE_CURVE('',#5500,#5503,#4727,.T.);
#6685=EDGE_CURVE('',#5504,#5502,#4728,.T.);
#6686=EDGE_CURVE('',#5504,#5503,#1110,.T.);
#6687=EDGE_CURVE('',#5503,#5505,#1111,.T.);
#6688=EDGE_CURVE('',#5506,#5504,#1112,.T.);
#6689=EDGE_CURVE('',#5506,#5505,#1113,.T.);
#6690=EDGE_CURVE('',#5505,#5499,#4729,.T.);
#6691=EDGE_CURVE('',#5501,#5506,#4730,.T.);
#6692=EDGE_CURVE('',#5507,#5508,#1114,.T.);
#6693=EDGE_CURVE('',#5509,#5507,#1115,.T.);
#6694=EDGE_CURVE('',#5510,#5509,#1116,.T.);
#6695=EDGE_CURVE('',#5510,#5508,#1117,.T.);
#6696=EDGE_CURVE('',#5508,#5511,#4731,.T.);
#6697=EDGE_CURVE('',#5512,#5510,#4732,.T.);
#6698=EDGE_CURVE('',#5512,#5511,#1118,.T.);
#6699=EDGE_CURVE('',#5511,#5513,#1119,.T.);
#6700=EDGE_CURVE('',#5514,#5512,#1120,.T.);
#6701=EDGE_CURVE('',#5514,#5513,#1121,.T.);
#6702=EDGE_CURVE('',#5513,#5507,#4733,.T.);
#6703=EDGE_CURVE('',#5509,#5514,#4734,.T.);
#6704=EDGE_CURVE('',#5515,#5515,#4735,.T.);
#6705=EDGE_CURVE('',#5515,#5516,#1122,.T.);
#6706=EDGE_CURVE('',#5516,#5516,#4736,.T.);
#6707=EDGE_CURVE('',#5517,#5517,#4737,.T.);
#6708=EDGE_CURVE('',#5517,#5518,#1123,.T.);
#6709=EDGE_CURVE('',#5518,#5518,#4738,.T.);
#6710=EDGE_CURVE('',#5519,#5519,#4739,.T.);
#6711=EDGE_CURVE('',#5519,#5520,#1124,.T.);
#6712=EDGE_CURVE('',#5520,#5520,#4740,.T.);
#6713=EDGE_CURVE('',#5521,#5521,#4741,.T.);
#6714=EDGE_CURVE('',#5521,#5522,#1125,.T.);
#6715=EDGE_CURVE('',#5522,#5522,#4742,.T.);
#6716=EDGE_CURVE('',#5523,#5523,#4743,.T.);
#6717=EDGE_CURVE('',#5523,#5524,#1126,.T.);
#6718=EDGE_CURVE('',#5524,#5524,#4744,.T.);
#6719=EDGE_CURVE('',#5525,#5526,#1127,.T.);
#6720=EDGE_CURVE('',#5527,#5525,#1128,.T.);
#6721=EDGE_CURVE('',#5528,#5527,#1129,.T.);
#6722=EDGE_CURVE('',#5528,#5526,#1130,.T.);
#6723=EDGE_CURVE('',#5526,#5529,#4745,.T.);
#6724=EDGE_CURVE('',#5530,#5528,#4746,.T.);
#6725=EDGE_CURVE('',#5530,#5529,#1131,.T.);
#6726=EDGE_CURVE('',#5529,#5531,#1132,.T.);
#6727=EDGE_CURVE('',#5532,#5530,#1133,.T.);
#6728=EDGE_CURVE('',#5532,#5531,#1134,.T.);
#6729=EDGE_CURVE('',#5531,#5525,#4747,.T.);
#6730=EDGE_CURVE('',#5527,#5532,#4748,.T.);
#6731=EDGE_CURVE('',#5533,#5534,#1135,.T.);
#6732=EDGE_CURVE('',#5535,#5533,#1136,.T.);
#6733=EDGE_CURVE('',#5536,#5535,#1137,.T.);
#6734=EDGE_CURVE('',#5536,#5534,#1138,.T.);
#6735=EDGE_CURVE('',#5534,#5537,#4749,.T.);
#6736=EDGE_CURVE('',#5538,#5536,#4750,.T.);
#6737=EDGE_CURVE('',#5538,#5537,#1139,.T.);
#6738=EDGE_CURVE('',#5537,#5539,#1140,.T.);
#6739=EDGE_CURVE('',#5540,#5538,#1141,.T.);
#6740=EDGE_CURVE('',#5540,#5539,#1142,.T.);
#6741=EDGE_CURVE('',#5539,#5533,#4751,.T.);
#6742=EDGE_CURVE('',#5535,#5540,#4752,.T.);
#6743=EDGE_CURVE('',#5541,#5541,#4753,.T.);
#6744=EDGE_CURVE('',#5541,#5542,#1143,.T.);
#6745=EDGE_CURVE('',#5542,#5542,#4754,.T.);
#6746=EDGE_CURVE('',#5543,#5543,#4755,.T.);
#6747=EDGE_CURVE('',#5543,#5544,#1144,.T.);
#6748=EDGE_CURVE('',#5544,#5544,#4756,.T.);
#6749=EDGE_CURVE('',#5545,#5545,#4757,.T.);
#6750=EDGE_CURVE('',#5545,#5546,#1145,.T.);
#6751=EDGE_CURVE('',#5546,#5546,#4758,.T.);
#6752=EDGE_CURVE('',#5547,#5547,#4759,.T.);
#6753=EDGE_CURVE('',#5547,#5548,#1146,.T.);
#6754=EDGE_CURVE('',#5548,#5548,#4760,.T.);
#6755=EDGE_CURVE('',#5549,#5549,#4761,.T.);
#6756=EDGE_CURVE('',#5549,#5550,#1147,.T.);
#6757=EDGE_CURVE('',#5550,#5550,#4762,.T.);
#6758=EDGE_CURVE('',#5551,#5552,#1148,.T.);
#6759=EDGE_CURVE('',#5553,#5551,#1149,.T.);
#6760=EDGE_CURVE('',#5554,#5553,#1150,.T.);
#6761=EDGE_CURVE('',#5554,#5552,#1151,.T.);
#6762=EDGE_CURVE('',#5552,#5555,#4763,.T.);
#6763=EDGE_CURVE('',#5556,#5554,#4764,.T.);
#6764=EDGE_CURVE('',#5556,#5555,#1152,.T.);
#6765=EDGE_CURVE('',#5555,#5557,#1153,.T.);
#6766=EDGE_CURVE('',#5558,#5556,#1154,.T.);
#6767=EDGE_CURVE('',#5558,#5557,#1155,.T.);
#6768=EDGE_CURVE('',#5557,#5551,#4765,.T.);
#6769=EDGE_CURVE('',#5553,#5558,#4766,.T.);
#6770=EDGE_CURVE('',#5559,#5560,#1156,.T.);
#6771=EDGE_CURVE('',#5561,#5559,#1157,.T.);
#6772=EDGE_CURVE('',#5562,#5561,#1158,.T.);
#6773=EDGE_CURVE('',#5562,#5560,#1159,.T.);
#6774=EDGE_CURVE('',#5560,#5563,#4767,.T.);
#6775=EDGE_CURVE('',#5564,#5562,#4768,.T.);
#6776=EDGE_CURVE('',#5564,#5563,#1160,.T.);
#6777=EDGE_CURVE('',#5563,#5565,#1161,.T.);
#6778=EDGE_CURVE('',#5566,#5564,#1162,.T.);
#6779=EDGE_CURVE('',#5566,#5565,#1163,.T.);
#6780=EDGE_CURVE('',#5565,#5559,#4769,.T.);
#6781=EDGE_CURVE('',#5561,#5566,#4770,.T.);
#6782=EDGE_CURVE('',#5567,#5567,#4771,.T.);
#6783=EDGE_CURVE('',#5567,#5568,#1164,.T.);
#6784=EDGE_CURVE('',#5568,#5568,#4772,.T.);
#6785=EDGE_CURVE('',#5569,#5569,#4773,.T.);
#6786=EDGE_CURVE('',#5569,#5570,#1165,.T.);
#6787=EDGE_CURVE('',#5570,#5570,#4774,.T.);
#6788=EDGE_CURVE('',#5571,#5571,#4775,.T.);
#6789=EDGE_CURVE('',#5571,#5572,#1166,.T.);
#6790=EDGE_CURVE('',#5572,#5572,#4776,.T.);
#6791=EDGE_CURVE('',#5573,#5573,#4777,.T.);
#6792=EDGE_CURVE('',#5573,#5574,#1167,.T.);
#6793=EDGE_CURVE('',#5574,#5574,#4778,.T.);
#6794=EDGE_CURVE('',#5575,#5575,#4779,.T.);
#6795=EDGE_CURVE('',#5575,#5576,#1168,.T.);
#6796=EDGE_CURVE('',#5576,#5576,#4780,.T.);
#6797=EDGE_CURVE('',#5577,#5578,#1169,.T.);
#6798=EDGE_CURVE('',#5579,#5577,#1170,.T.);
#6799=EDGE_CURVE('',#5580,#5579,#1171,.T.);
#6800=EDGE_CURVE('',#5580,#5578,#1172,.T.);
#6801=EDGE_CURVE('',#5578,#5581,#4781,.T.);
#6802=EDGE_CURVE('',#5582,#5580,#4782,.T.);
#6803=EDGE_CURVE('',#5582,#5581,#1173,.T.);
#6804=EDGE_CURVE('',#5581,#5583,#1174,.T.);
#6805=EDGE_CURVE('',#5584,#5582,#1175,.T.);
#6806=EDGE_CURVE('',#5584,#5583,#1176,.T.);
#6807=EDGE_CURVE('',#5583,#5577,#4783,.T.);
#6808=EDGE_CURVE('',#5579,#5584,#4784,.T.);
#6809=EDGE_CURVE('',#5585,#5586,#1177,.T.);
#6810=EDGE_CURVE('',#5587,#5585,#1178,.T.);
#6811=EDGE_CURVE('',#5588,#5587,#1179,.T.);
#6812=EDGE_CURVE('',#5588,#5586,#1180,.T.);
#6813=EDGE_CURVE('',#5586,#5589,#4785,.T.);
#6814=EDGE_CURVE('',#5590,#5588,#4786,.T.);
#6815=EDGE_CURVE('',#5590,#5589,#1181,.T.);
#6816=EDGE_CURVE('',#5589,#5591,#1182,.T.);
#6817=EDGE_CURVE('',#5592,#5590,#1183,.T.);
#6818=EDGE_CURVE('',#5592,#5591,#1184,.T.);
#6819=EDGE_CURVE('',#5591,#5585,#4787,.T.);
#6820=EDGE_CURVE('',#5587,#5592,#4788,.T.);
#6821=EDGE_CURVE('',#5593,#5593,#4789,.T.);
#6822=EDGE_CURVE('',#5593,#5594,#1185,.T.);
#6823=EDGE_CURVE('',#5594,#5594,#4790,.T.);
#6824=EDGE_CURVE('',#5595,#5595,#4791,.T.);
#6825=EDGE_CURVE('',#5595,#5596,#1186,.T.);
#6826=EDGE_CURVE('',#5596,#5596,#4792,.T.);
#6827=EDGE_CURVE('',#5597,#5597,#4793,.T.);
#6828=EDGE_CURVE('',#5597,#5598,#1187,.T.);
#6829=EDGE_CURVE('',#5598,#5598,#4794,.T.);
#6830=EDGE_CURVE('',#5599,#5599,#4795,.T.);
#6831=EDGE_CURVE('',#5599,#5600,#1188,.T.);
#6832=EDGE_CURVE('',#5600,#5600,#4796,.T.);
#6833=EDGE_CURVE('',#5601,#5601,#4797,.T.);
#6834=EDGE_CURVE('',#5601,#5602,#1189,.T.);
#6835=EDGE_CURVE('',#5602,#5602,#4798,.T.);
#6836=EDGE_CURVE('',#5603,#5604,#1190,.T.);
#6837=EDGE_CURVE('',#5605,#5603,#1191,.T.);
#6838=EDGE_CURVE('',#5606,#5605,#1192,.T.);
#6839=EDGE_CURVE('',#5606,#5604,#1193,.T.);
#6840=EDGE_CURVE('',#5604,#5607,#4799,.T.);
#6841=EDGE_CURVE('',#5608,#5606,#4800,.T.);
#6842=EDGE_CURVE('',#5608,#5607,#1194,.T.);
#6843=EDGE_CURVE('',#5607,#5609,#1195,.T.);
#6844=EDGE_CURVE('',#5610,#5608,#1196,.T.);
#6845=EDGE_CURVE('',#5610,#5609,#1197,.T.);
#6846=EDGE_CURVE('',#5609,#5603,#4801,.T.);
#6847=EDGE_CURVE('',#5605,#5610,#4802,.T.);
#6848=EDGE_CURVE('',#5611,#5612,#1198,.T.);
#6849=EDGE_CURVE('',#5613,#5611,#1199,.T.);
#6850=EDGE_CURVE('',#5614,#5613,#1200,.T.);
#6851=EDGE_CURVE('',#5614,#5612,#1201,.T.);
#6852=EDGE_CURVE('',#5612,#5615,#4803,.T.);
#6853=EDGE_CURVE('',#5616,#5614,#4804,.T.);
#6854=EDGE_CURVE('',#5616,#5615,#1202,.T.);
#6855=EDGE_CURVE('',#5615,#5617,#1203,.T.);
#6856=EDGE_CURVE('',#5618,#5616,#1204,.T.);
#6857=EDGE_CURVE('',#5618,#5617,#1205,.T.);
#6858=EDGE_CURVE('',#5617,#5611,#4805,.T.);
#6859=EDGE_CURVE('',#5613,#5618,#4806,.T.);
#6860=EDGE_CURVE('',#5619,#5619,#4807,.T.);
#6861=EDGE_CURVE('',#5619,#5620,#1206,.T.);
#6862=EDGE_CURVE('',#5620,#5620,#4808,.T.);
#6863=EDGE_CURVE('',#5621,#5621,#4809,.T.);
#6864=EDGE_CURVE('',#5621,#5622,#1207,.T.);
#6865=EDGE_CURVE('',#5622,#5622,#4810,.T.);
#6866=EDGE_CURVE('',#5623,#5624,#1208,.T.);
#6867=EDGE_CURVE('',#5625,#5623,#1209,.T.);
#6868=EDGE_CURVE('',#5626,#5625,#1210,.T.);
#6869=EDGE_CURVE('',#5626,#5624,#1211,.T.);
#6870=EDGE_CURVE('',#5624,#5627,#4811,.T.);
#6871=EDGE_CURVE('',#5628,#5626,#4812,.T.);
#6872=EDGE_CURVE('',#5628,#5627,#1212,.T.);
#6873=EDGE_CURVE('',#5627,#5629,#1213,.T.);
#6874=EDGE_CURVE('',#5630,#5628,#1214,.T.);
#6875=EDGE_CURVE('',#5630,#5629,#1215,.T.);
#6876=EDGE_CURVE('',#5629,#5623,#4813,.T.);
#6877=EDGE_CURVE('',#5625,#5630,#4814,.T.);
#6878=EDGE_CURVE('',#5631,#5632,#1216,.T.);
#6879=EDGE_CURVE('',#5633,#5631,#1217,.T.);
#6880=EDGE_CURVE('',#5634,#5633,#1218,.T.);
#6881=EDGE_CURVE('',#5634,#5632,#1219,.T.);
#6882=EDGE_CURVE('',#5632,#5635,#4815,.T.);
#6883=EDGE_CURVE('',#5636,#5634,#4816,.T.);
#6884=EDGE_CURVE('',#5636,#5635,#1220,.T.);
#6885=EDGE_CURVE('',#5635,#5637,#1221,.T.);
#6886=EDGE_CURVE('',#5638,#5636,#1222,.T.);
#6887=EDGE_CURVE('',#5638,#5637,#1223,.T.);
#6888=EDGE_CURVE('',#5637,#5631,#4817,.T.);
#6889=EDGE_CURVE('',#5633,#5638,#4818,.T.);
#6890=EDGE_CURVE('',#5639,#5639,#4819,.T.);
#6891=EDGE_CURVE('',#5639,#5640,#1224,.T.);
#6892=EDGE_CURVE('',#5640,#5640,#4820,.T.);
#6893=EDGE_CURVE('',#5641,#5641,#4821,.T.);
#6894=EDGE_CURVE('',#5641,#5642,#1225,.T.);
#6895=EDGE_CURVE('',#5642,#5642,#4822,.T.);
#6896=EDGE_CURVE('',#5643,#5643,#4823,.T.);
#6897=EDGE_CURVE('',#5643,#5644,#1226,.T.);
#6898=EDGE_CURVE('',#5644,#5644,#4824,.T.);
#6899=EDGE_CURVE('',#5645,#5646,#4825,.T.);
#6900=EDGE_CURVE('',#5646,#5647,#1227,.T.);
#6901=EDGE_CURVE('',#5647,#5648,#4826,.T.);
#6902=EDGE_CURVE('',#5648,#5645,#1228,.T.);
#6903=EDGE_CURVE('',#5646,#5649,#1229,.T.);
#6904=EDGE_CURVE('',#5650,#5649,#1230,.T.);
#6905=EDGE_CURVE('',#5647,#5650,#1231,.T.);
#6906=EDGE_CURVE('',#5649,#5651,#4827,.T.);
#6907=EDGE_CURVE('',#5651,#5652,#1232,.T.);
#6908=EDGE_CURVE('',#5652,#5650,#4828,.T.);
#6909=EDGE_CURVE('',#5651,#5653,#1233,.T.);
#6910=EDGE_CURVE('',#5653,#5654,#1234,.T.);
#6911=EDGE_CURVE('',#5654,#5652,#1235,.T.);
#6912=EDGE_CURVE('',#5655,#5655,#4829,.T.);
#6913=EDGE_CURVE('',#5656,#5656,#4830,.T.);
#6914=EDGE_CURVE('',#5657,#5657,#4831,.T.);
#6915=EDGE_CURVE('',#5658,#5658,#4832,.T.);
#6916=EDGE_CURVE('',#5659,#5659,#4833,.T.);
#6917=EDGE_CURVE('',#5660,#5660,#4834,.T.);
#6918=EDGE_CURVE('',#5661,#5661,#4835,.T.);
#6919=EDGE_CURVE('',#5662,#5662,#4836,.T.);
#6920=EDGE_CURVE('',#5663,#5663,#4837,.T.);
#6921=EDGE_CURVE('',#5664,#5664,#4838,.T.);
#6922=EDGE_CURVE('',#5665,#5665,#4839,.T.);
#6923=EDGE_CURVE('',#5666,#5666,#4840,.T.);
#6924=EDGE_CURVE('',#5667,#5667,#4841,.T.);
#6925=EDGE_CURVE('',#5668,#5668,#4842,.T.);
#6926=EDGE_CURVE('',#5669,#5669,#4843,.T.);
#6927=EDGE_CURVE('',#5670,#5670,#4844,.T.);
#6928=EDGE_CURVE('',#5671,#5671,#4845,.T.);
#6929=EDGE_CURVE('',#5672,#5672,#4846,.T.);
#6930=EDGE_CURVE('',#5673,#5673,#4847,.T.);
#6931=EDGE_CURVE('',#5674,#5674,#4848,.T.);
#6932=EDGE_CURVE('',#5675,#5675,#4849,.T.);
#6933=EDGE_CURVE('',#5676,#5676,#4850,.T.);
#6934=EDGE_CURVE('',#5677,#5677,#4851,.T.);
#6935=EDGE_CURVE('',#5678,#5678,#4852,.T.);
#6936=EDGE_CURVE('',#5679,#5679,#4853,.T.);
#6937=EDGE_CURVE('',#5680,#5680,#4854,.T.);
#6938=EDGE_CURVE('',#5681,#5681,#4855,.T.);
#6939=EDGE_CURVE('',#5682,#5682,#4856,.T.);
#6940=EDGE_CURVE('',#5683,#5683,#4857,.T.);
#6941=EDGE_CURVE('',#5684,#5684,#4858,.T.);
#6942=EDGE_CURVE('',#5685,#5685,#4859,.T.);
#6943=EDGE_CURVE('',#5686,#5686,#4860,.T.);
#6944=EDGE_CURVE('',#5687,#5687,#4861,.T.);
#6945=EDGE_CURVE('',#5688,#5688,#4862,.T.);
#6946=EDGE_CURVE('',#5689,#5689,#4863,.T.);
#6947=EDGE_CURVE('',#5690,#5690,#4864,.T.);
#6948=EDGE_CURVE('',#5691,#5691,#4865,.T.);
#6949=EDGE_CURVE('',#5692,#5692,#4866,.T.);
#6950=EDGE_CURVE('',#5693,#5693,#4867,.T.);
#6951=EDGE_CURVE('',#5694,#5694,#4868,.T.);
#6952=EDGE_CURVE('',#5695,#5695,#4869,.T.);
#6953=EDGE_CURVE('',#5696,#5696,#4870,.T.);
#6954=EDGE_CURVE('',#5697,#5697,#4871,.T.);
#6955=EDGE_CURVE('',#5698,#5698,#4872,.T.);
#6956=EDGE_CURVE('',#5699,#5699,#4873,.T.);
#6957=EDGE_CURVE('',#5700,#5700,#4874,.T.);
#6958=EDGE_CURVE('',#5701,#5701,#4875,.T.);
#6959=EDGE_CURVE('',#5702,#5703,#4876,.T.);
#6960=EDGE_CURVE('',#5703,#5704,#1236,.T.);
#6961=EDGE_CURVE('',#5704,#5705,#4877,.T.);
#6962=EDGE_CURVE('',#5705,#5702,#1237,.T.);
#6963=EDGE_CURVE('',#5706,#5705,#1238,.T.);
#6964=EDGE_CURVE('',#5707,#5706,#1239,.T.);
#6965=EDGE_CURVE('',#5707,#5702,#1240,.T.);
#6966=EDGE_CURVE('',#5708,#5704,#1241,.T.);
#6967=EDGE_CURVE('',#5653,#5708,#1242,.T.);
#6968=EDGE_CURVE('',#5709,#5645,#1243,.T.);
#6969=EDGE_CURVE('',#5710,#5709,#1244,.T.);
#6970=EDGE_CURVE('',#5711,#5710,#1245,.T.);
#6971=EDGE_CURVE('',#5706,#5711,#4878,.T.);
#6972=EDGE_CURVE('',#5712,#5707,#4879,.T.);
#6973=EDGE_CURVE('',#5711,#5712,#1246,.T.);
#6974=EDGE_CURVE('',#5713,#5713,#4880,.T.);
#6975=EDGE_CURVE('',#5713,#5655,#1247,.T.);
#6976=EDGE_CURVE('',#5714,#5714,#4881,.T.);
#6977=EDGE_CURVE('',#5714,#5656,#1248,.T.);
#6978=EDGE_CURVE('',#5715,#5715,#4882,.T.);
#6979=EDGE_CURVE('',#5715,#5657,#1249,.T.);
#6980=EDGE_CURVE('',#5716,#5716,#4883,.T.);
#6981=EDGE_CURVE('',#5716,#5658,#1250,.T.);
#6982=EDGE_CURVE('',#5717,#5717,#4884,.T.);
#6983=EDGE_CURVE('',#5717,#5659,#1251,.T.);
#6984=EDGE_CURVE('',#5718,#5718,#4885,.T.);
#6985=EDGE_CURVE('',#5718,#5660,#1252,.T.);
#6986=EDGE_CURVE('',#5719,#5719,#4886,.T.);
#6987=EDGE_CURVE('',#5719,#5661,#1253,.T.);
#6988=EDGE_CURVE('',#5720,#5720,#4887,.T.);
#6989=EDGE_CURVE('',#5720,#5662,#1254,.T.);
#6990=EDGE_CURVE('',#5721,#5721,#4888,.T.);
#6991=EDGE_CURVE('',#5721,#5663,#1255,.T.);
#6992=EDGE_CURVE('',#5722,#5722,#4889,.T.);
#6993=EDGE_CURVE('',#5722,#5664,#1256,.T.);
#6994=EDGE_CURVE('',#5723,#5723,#4890,.T.);
#6995=EDGE_CURVE('',#5723,#5665,#1257,.T.);
#6996=EDGE_CURVE('',#5724,#5724,#4891,.T.);
#6997=EDGE_CURVE('',#5724,#5666,#1258,.T.);
#6998=EDGE_CURVE('',#5725,#5725,#4892,.T.);
#6999=EDGE_CURVE('',#5725,#5667,#1259,.T.);
#7000=EDGE_CURVE('',#5726,#5726,#4893,.T.);
#7001=EDGE_CURVE('',#5726,#5668,#1260,.T.);
#7002=EDGE_CURVE('',#5727,#5727,#4894,.T.);
#7003=EDGE_CURVE('',#5727,#5669,#1261,.T.);
#7004=EDGE_CURVE('',#5728,#5728,#4895,.T.);
#7005=EDGE_CURVE('',#5728,#5670,#1262,.T.);
#7006=EDGE_CURVE('',#5729,#5729,#4896,.T.);
#7007=EDGE_CURVE('',#5729,#5671,#1263,.T.);
#7008=EDGE_CURVE('',#5730,#5730,#4897,.T.);
#7009=EDGE_CURVE('',#5730,#5672,#1264,.T.);
#7010=EDGE_CURVE('',#5731,#5731,#4898,.T.);
#7011=EDGE_CURVE('',#5731,#5673,#1265,.T.);
#7012=EDGE_CURVE('',#5732,#5732,#4899,.T.);
#7013=EDGE_CURVE('',#5732,#5674,#1266,.T.);
#7014=EDGE_CURVE('',#5733,#5733,#4900,.T.);
#7015=EDGE_CURVE('',#5733,#5675,#1267,.T.);
#7016=EDGE_CURVE('',#5734,#5734,#4901,.T.);
#7017=EDGE_CURVE('',#5734,#5676,#1268,.T.);
#7018=EDGE_CURVE('',#5735,#5735,#4902,.T.);
#7019=EDGE_CURVE('',#5735,#5677,#1269,.T.);
#7020=EDGE_CURVE('',#5736,#5736,#4903,.T.);
#7021=EDGE_CURVE('',#5736,#5678,#1270,.T.);
#7022=EDGE_CURVE('',#5737,#5737,#4904,.T.);
#7023=EDGE_CURVE('',#5737,#5679,#1271,.T.);
#7024=EDGE_CURVE('',#5738,#5738,#4905,.T.);
#7025=EDGE_CURVE('',#5738,#5680,#1272,.T.);
#7026=EDGE_CURVE('',#5739,#5739,#4906,.T.);
#7027=EDGE_CURVE('',#5739,#5681,#1273,.T.);
#7028=EDGE_CURVE('',#5740,#5740,#4907,.T.);
#7029=EDGE_CURVE('',#5740,#5682,#1274,.T.);
#7030=EDGE_CURVE('',#5741,#5741,#4908,.T.);
#7031=EDGE_CURVE('',#5741,#5683,#1275,.T.);
#7032=EDGE_CURVE('',#5742,#5742,#4909,.T.);
#7033=EDGE_CURVE('',#5742,#5684,#1276,.T.);
#7034=EDGE_CURVE('',#5743,#5743,#4910,.T.);
#7035=EDGE_CURVE('',#5743,#5685,#1277,.T.);
#7036=EDGE_CURVE('',#5744,#5744,#4911,.T.);
#7037=EDGE_CURVE('',#5744,#5686,#1278,.T.);
#7038=EDGE_CURVE('',#5745,#5745,#4912,.T.);
#7039=EDGE_CURVE('',#5745,#5687,#1279,.T.);
#7040=EDGE_CURVE('',#5746,#5746,#4913,.T.);
#7041=EDGE_CURVE('',#5746,#5688,#1280,.T.);
#7042=EDGE_CURVE('',#5747,#5747,#4914,.T.);
#7043=EDGE_CURVE('',#5747,#5689,#1281,.T.);
#7044=EDGE_CURVE('',#5748,#5748,#4915,.T.);
#7045=EDGE_CURVE('',#5748,#5690,#1282,.T.);
#7046=EDGE_CURVE('',#5749,#5749,#4916,.T.);
#7047=EDGE_CURVE('',#5749,#5691,#1283,.T.);
#7048=EDGE_CURVE('',#5750,#5750,#4917,.T.);
#7049=EDGE_CURVE('',#5750,#5692,#1284,.T.);
#7050=EDGE_CURVE('',#5751,#5751,#4918,.T.);
#7051=EDGE_CURVE('',#5751,#5693,#1285,.T.);
#7052=EDGE_CURVE('',#5752,#5752,#4919,.T.);
#7053=EDGE_CURVE('',#5752,#5694,#1286,.T.);
#7054=EDGE_CURVE('',#5753,#5753,#4920,.T.);
#7055=EDGE_CURVE('',#5753,#5695,#1287,.T.);
#7056=EDGE_CURVE('',#5754,#5754,#4921,.T.);
#7057=EDGE_CURVE('',#5754,#5696,#1288,.T.);
#7058=EDGE_CURVE('',#5755,#5755,#4922,.T.);
#7059=EDGE_CURVE('',#5755,#5697,#1289,.T.);
#7060=EDGE_CURVE('',#5756,#5756,#4923,.T.);
#7061=EDGE_CURVE('',#5756,#5698,#1290,.T.);
#7062=EDGE_CURVE('',#5757,#5757,#4924,.T.);
#7063=EDGE_CURVE('',#5757,#5699,#1291,.T.);
#7064=EDGE_CURVE('',#5758,#5758,#4925,.T.);
#7065=EDGE_CURVE('',#5758,#5700,#1292,.T.);
#7066=EDGE_CURVE('',#5759,#5759,#4926,.T.);
#7067=EDGE_CURVE('',#5759,#5701,#1293,.T.);
#7068=EDGE_CURVE('',#5760,#5708,#1294,.T.);
#7069=EDGE_CURVE('',#5654,#5760,#1295,.T.);
#7070=EDGE_CURVE('',#5703,#5760,#1296,.T.);
#7071=EDGE_CURVE('',#5761,#5761,#4927,.T.);
#7072=EDGE_CURVE('',#5761,#5762,#1297,.T.);
#7073=EDGE_CURVE('',#5762,#5762,#4928,.T.);
#7074=EDGE_CURVE('',#5763,#5763,#4929,.T.);
#7075=EDGE_CURVE('',#5763,#5764,#1298,.T.);
#7076=EDGE_CURVE('',#5764,#5764,#4930,.T.);
#7077=EDGE_CURVE('',#5765,#5765,#4931,.T.);
#7078=EDGE_CURVE('',#5765,#5766,#1299,.T.);
#7079=EDGE_CURVE('',#5766,#5766,#4932,.T.);
#7080=EDGE_CURVE('',#5767,#5767,#4933,.T.);
#7081=EDGE_CURVE('',#5767,#5768,#1300,.T.);
#7082=EDGE_CURVE('',#5768,#5768,#4934,.T.);
#7083=EDGE_CURVE('',#5769,#5769,#4935,.T.);
#7084=EDGE_CURVE('',#5769,#5770,#1301,.T.);
#7085=EDGE_CURVE('',#5770,#5770,#4936,.T.);
#7086=EDGE_CURVE('',#5771,#5771,#4937,.T.);
#7087=EDGE_CURVE('',#5771,#5772,#1302,.T.);
#7088=EDGE_CURVE('',#5772,#5772,#4938,.T.);
#7089=EDGE_CURVE('',#5773,#5773,#4939,.T.);
#7090=EDGE_CURVE('',#5773,#5774,#1303,.T.);
#7091=EDGE_CURVE('',#5774,#5774,#4940,.T.);
#7092=EDGE_CURVE('',#5775,#5775,#4941,.T.);
#7093=EDGE_CURVE('',#5775,#5776,#1304,.T.);
#7094=EDGE_CURVE('',#5776,#5776,#4942,.T.);
#7095=EDGE_CURVE('',#5777,#5777,#4943,.T.);
#7096=EDGE_CURVE('',#5777,#5778,#1305,.T.);
#7097=EDGE_CURVE('',#5778,#5778,#4944,.T.);
#7098=EDGE_CURVE('',#5779,#5779,#4945,.T.);
#7099=EDGE_CURVE('',#5779,#5780,#1306,.T.);
#7100=EDGE_CURVE('',#5780,#5780,#4946,.T.);
#7101=EDGE_CURVE('',#5781,#5781,#4947,.T.);
#7102=EDGE_CURVE('',#5781,#5782,#1307,.T.);
#7103=EDGE_CURVE('',#5782,#5782,#4948,.T.);
#7104=EDGE_CURVE('',#5783,#5783,#4949,.T.);
#7105=EDGE_CURVE('',#5783,#5784,#1308,.T.);
#7106=EDGE_CURVE('',#5784,#5784,#4950,.T.);
#7107=EDGE_CURVE('',#5785,#5785,#4951,.T.);
#7108=EDGE_CURVE('',#5785,#5786,#1309,.T.);
#7109=EDGE_CURVE('',#5786,#5786,#4952,.T.);
#7110=EDGE_CURVE('',#5787,#5787,#4953,.T.);
#7111=EDGE_CURVE('',#5787,#5788,#1310,.T.);
#7112=EDGE_CURVE('',#5788,#5788,#4954,.T.);
#7113=EDGE_CURVE('',#5789,#5789,#4955,.T.);
#7114=EDGE_CURVE('',#5789,#5790,#1311,.T.);
#7115=EDGE_CURVE('',#5790,#5790,#4956,.T.);
#7116=EDGE_CURVE('',#5791,#5791,#4957,.T.);
#7117=EDGE_CURVE('',#5791,#5792,#1312,.T.);
#7118=EDGE_CURVE('',#5792,#5792,#4958,.T.);
#7119=EDGE_CURVE('',#5793,#5793,#4959,.T.);
#7120=EDGE_CURVE('',#5793,#5794,#1313,.T.);
#7121=EDGE_CURVE('',#5794,#5794,#4960,.T.);
#7122=EDGE_CURVE('',#5795,#5795,#4961,.T.);
#7123=EDGE_CURVE('',#5795,#5796,#1314,.T.);
#7124=EDGE_CURVE('',#5796,#5796,#4962,.T.);
#7125=EDGE_CURVE('',#5797,#5797,#4963,.T.);
#7126=EDGE_CURVE('',#5797,#5798,#1315,.T.);
#7127=EDGE_CURVE('',#5798,#5798,#4964,.T.);
#7128=EDGE_CURVE('',#5799,#5799,#4965,.T.);
#7129=EDGE_CURVE('',#5799,#5800,#1316,.T.);
#7130=EDGE_CURVE('',#5800,#5800,#4966,.T.);
#7131=EDGE_CURVE('',#5801,#5801,#4967,.T.);
#7132=EDGE_CURVE('',#5801,#5802,#1317,.T.);
#7133=EDGE_CURVE('',#5802,#5802,#4968,.T.);
#7134=EDGE_CURVE('',#5803,#5803,#4969,.T.);
#7135=EDGE_CURVE('',#5803,#5804,#1318,.T.);
#7136=EDGE_CURVE('',#5804,#5804,#4970,.T.);
#7137=EDGE_CURVE('',#5805,#5805,#4971,.T.);
#7138=EDGE_CURVE('',#5805,#5806,#1319,.T.);
#7139=EDGE_CURVE('',#5806,#5806,#4972,.T.);
#7140=EDGE_CURVE('',#5807,#5807,#4973,.T.);
#7141=EDGE_CURVE('',#5807,#5808,#1320,.T.);
#7142=EDGE_CURVE('',#5808,#5808,#4974,.T.);
#7143=EDGE_CURVE('',#5809,#5809,#4975,.T.);
#7144=EDGE_CURVE('',#5809,#5810,#1321,.T.);
#7145=EDGE_CURVE('',#5810,#5810,#4976,.T.);
#7146=EDGE_CURVE('',#5811,#5811,#4977,.T.);
#7147=EDGE_CURVE('',#5811,#5812,#1322,.T.);
#7148=EDGE_CURVE('',#5812,#5812,#4978,.T.);
#7149=EDGE_CURVE('',#5813,#5813,#4979,.T.);
#7150=EDGE_CURVE('',#5813,#5814,#1323,.T.);
#7151=EDGE_CURVE('',#5814,#5814,#4980,.T.);
#7152=EDGE_CURVE('',#5815,#5815,#4981,.T.);
#7153=EDGE_CURVE('',#5815,#5816,#1324,.T.);
#7154=EDGE_CURVE('',#5816,#5816,#4982,.T.);
#7155=EDGE_CURVE('',#5817,#5817,#4983,.T.);
#7156=EDGE_CURVE('',#5817,#5818,#1325,.T.);
#7157=EDGE_CURVE('',#5818,#5818,#4984,.T.);
#7158=EDGE_CURVE('',#5819,#5819,#4985,.T.);
#7159=EDGE_CURVE('',#5819,#5820,#1326,.T.);
#7160=EDGE_CURVE('',#5820,#5820,#4986,.T.);
#7161=EDGE_CURVE('',#5821,#5821,#4987,.T.);
#7162=EDGE_CURVE('',#5821,#5822,#1327,.T.);
#7163=EDGE_CURVE('',#5822,#5822,#4988,.T.);
#7164=EDGE_CURVE('',#5823,#5823,#4989,.T.);
#7165=EDGE_CURVE('',#5823,#5824,#1328,.T.);
#7166=EDGE_CURVE('',#5824,#5824,#4990,.T.);
#7167=EDGE_CURVE('',#5825,#5825,#4991,.T.);
#7168=EDGE_CURVE('',#5825,#5826,#1329,.T.);
#7169=EDGE_CURVE('',#5826,#5826,#4992,.T.);
#7170=EDGE_CURVE('',#5827,#5827,#4993,.T.);
#7171=EDGE_CURVE('',#5827,#5828,#1330,.T.);
#7172=EDGE_CURVE('',#5828,#5828,#4994,.T.);
#7173=EDGE_CURVE('',#5829,#5829,#4995,.T.);
#7174=EDGE_CURVE('',#5829,#5830,#1331,.T.);
#7175=EDGE_CURVE('',#5830,#5830,#4996,.T.);
#7176=EDGE_CURVE('',#5831,#5831,#4997,.T.);
#7177=EDGE_CURVE('',#5831,#5832,#1332,.T.);
#7178=EDGE_CURVE('',#5832,#5832,#4998,.T.);
#7179=EDGE_CURVE('',#5833,#5833,#4999,.T.);
#7180=EDGE_CURVE('',#5833,#5834,#1333,.T.);
#7181=EDGE_CURVE('',#5834,#5834,#5000,.T.);
#7182=EDGE_CURVE('',#5835,#5835,#5001,.T.);
#7183=EDGE_CURVE('',#5835,#5836,#1334,.T.);
#7184=EDGE_CURVE('',#5836,#5836,#5002,.T.);
#7185=EDGE_CURVE('',#5837,#5837,#5003,.T.);
#7186=EDGE_CURVE('',#5837,#5838,#1335,.T.);
#7187=EDGE_CURVE('',#5838,#5838,#5004,.T.);
#7188=EDGE_CURVE('',#5839,#5839,#5005,.T.);
#7189=EDGE_CURVE('',#5839,#5840,#1336,.T.);
#7190=EDGE_CURVE('',#5840,#5840,#5006,.T.);
#7191=EDGE_CURVE('',#5841,#5841,#5007,.T.);
#7192=EDGE_CURVE('',#5841,#5842,#1337,.T.);
#7193=EDGE_CURVE('',#5842,#5842,#5008,.T.);
#7194=EDGE_CURVE('',#5843,#5843,#5009,.T.);
#7195=EDGE_CURVE('',#5843,#5844,#1338,.T.);
#7196=EDGE_CURVE('',#5844,#5844,#5010,.T.);
#7197=EDGE_CURVE('',#5845,#5845,#5011,.T.);
#7198=EDGE_CURVE('',#5845,#5846,#1339,.T.);
#7199=EDGE_CURVE('',#5846,#5846,#5012,.T.);
#7200=EDGE_CURVE('',#5847,#5847,#5013,.T.);
#7201=EDGE_CURVE('',#5847,#5848,#1340,.T.);
#7202=EDGE_CURVE('',#5848,#5848,#5014,.T.);
#7203=EDGE_CURVE('',#5849,#5849,#5015,.T.);
#7204=EDGE_CURVE('',#5849,#5850,#1341,.T.);
#7205=EDGE_CURVE('',#5850,#5850,#5016,.T.);
#7206=EDGE_CURVE('',#5851,#5851,#5017,.T.);
#7207=EDGE_CURVE('',#5851,#5852,#1342,.T.);
#7208=EDGE_CURVE('',#5852,#5852,#5018,.T.);
#7209=EDGE_CURVE('',#5853,#5853,#5019,.T.);
#7210=EDGE_CURVE('',#5853,#5854,#1343,.T.);
#7211=EDGE_CURVE('',#5854,#5854,#5020,.T.);
#7212=EDGE_CURVE('',#5710,#5855,#1344,.T.);
#7213=EDGE_CURVE('',#5856,#5709,#1345,.T.);
#7214=EDGE_CURVE('',#5855,#5856,#1346,.T.);
#7215=EDGE_CURVE('',#5855,#5712,#1347,.T.);
#7216=EDGE_CURVE('',#5648,#5856,#1348,.T.);
#8356=ORIENTED_EDGE('',*,*,#6509,.F.);
#8357=ORIENTED_EDGE('',*,*,#6510,.T.);
#8358=ORIENTED_EDGE('',*,*,#6511,.F.);
#8359=ORIENTED_EDGE('',*,*,#6510,.F.);
#8360=ORIENTED_EDGE('',*,*,#6512,.F.);
#8361=ORIENTED_EDGE('',*,*,#6513,.T.);
#8362=ORIENTED_EDGE('',*,*,#6514,.F.);
#8363=ORIENTED_EDGE('',*,*,#6513,.F.);
#8364=ORIENTED_EDGE('',*,*,#6515,.F.);
#8365=ORIENTED_EDGE('',*,*,#6516,.T.);
#8366=ORIENTED_EDGE('',*,*,#6517,.F.);
#8367=ORIENTED_EDGE('',*,*,#6516,.F.);
#8368=ORIENTED_EDGE('',*,*,#6518,.F.);
#8369=ORIENTED_EDGE('',*,*,#6519,.T.);
#8370=ORIENTED_EDGE('',*,*,#6520,.F.);
#8371=ORIENTED_EDGE('',*,*,#6519,.F.);
#8372=ORIENTED_EDGE('',*,*,#6521,.F.);
#8373=ORIENTED_EDGE('',*,*,#6522,.T.);
#8374=ORIENTED_EDGE('',*,*,#6523,.F.);
#8375=ORIENTED_EDGE('',*,*,#6522,.F.);
#8376=ORIENTED_EDGE('',*,*,#6524,.F.);
#8377=ORIENTED_EDGE('',*,*,#6525,.F.);
#8378=ORIENTED_EDGE('',*,*,#6526,.F.);
#8379=ORIENTED_EDGE('',*,*,#6527,.T.);
#8380=ORIENTED_EDGE('',*,*,#6528,.F.);
#8381=ORIENTED_EDGE('',*,*,#6527,.F.);
#8382=ORIENTED_EDGE('',*,*,#6529,.F.);
#8383=ORIENTED_EDGE('',*,*,#6530,.T.);
#8384=ORIENTED_EDGE('',*,*,#6531,.F.);
#8385=ORIENTED_EDGE('',*,*,#6530,.F.);
#8386=ORIENTED_EDGE('',*,*,#6532,.F.);
#8387=ORIENTED_EDGE('',*,*,#6533,.T.);
#8388=ORIENTED_EDGE('',*,*,#6534,.F.);
#8389=ORIENTED_EDGE('',*,*,#6533,.F.);
#8390=ORIENTED_EDGE('',*,*,#6535,.F.);
#8391=ORIENTED_EDGE('',*,*,#6525,.T.);
#8392=ORIENTED_EDGE('',*,*,#6536,.F.);
#8393=ORIENTED_EDGE('',*,*,#6537,.F.);
#8394=ORIENTED_EDGE('',*,*,#6538,.F.);
#8395=ORIENTED_EDGE('',*,*,#6539,.T.);
#8396=ORIENTED_EDGE('',*,*,#6540,.F.);
#8397=ORIENTED_EDGE('',*,*,#6539,.F.);
#8398=ORIENTED_EDGE('',*,*,#6541,.F.);
#8399=ORIENTED_EDGE('',*,*,#6542,.T.);
#8400=ORIENTED_EDGE('',*,*,#6543,.F.);
#8401=ORIENTED_EDGE('',*,*,#6542,.F.);
#8402=ORIENTED_EDGE('',*,*,#6544,.F.);
#8403=ORIENTED_EDGE('',*,*,#6545,.T.);
#8404=ORIENTED_EDGE('',*,*,#6546,.F.);
#8405=ORIENTED_EDGE('',*,*,#6545,.F.);
#8406=ORIENTED_EDGE('',*,*,#6547,.F.);
#8407=ORIENTED_EDGE('',*,*,#6537,.T.);
#8408=ORIENTED_EDGE('',*,*,#6548,.F.);
#8409=ORIENTED_EDGE('',*,*,#6549,.T.);
#8410=ORIENTED_EDGE('',*,*,#6550,.F.);
#8411=ORIENTED_EDGE('',*,*,#6549,.F.);
#8412=ORIENTED_EDGE('',*,*,#6551,.F.);
#8413=ORIENTED_EDGE('',*,*,#6552,.T.);
#8414=ORIENTED_EDGE('',*,*,#6553,.F.);
#8415=ORIENTED_EDGE('',*,*,#6552,.F.);
#8416=ORIENTED_EDGE('',*,*,#6554,.F.);
#8417=ORIENTED_EDGE('',*,*,#6555,.T.);
#8418=ORIENTED_EDGE('',*,*,#6556,.F.);
#8419=ORIENTED_EDGE('',*,*,#6555,.F.);
#8420=ORIENTED_EDGE('',*,*,#6557,.F.);
#8421=ORIENTED_EDGE('',*,*,#6558,.T.);
#8422=ORIENTED_EDGE('',*,*,#6559,.F.);
#8423=ORIENTED_EDGE('',*,*,#6558,.F.);
#8424=ORIENTED_EDGE('',*,*,#6560,.F.);
#8425=ORIENTED_EDGE('',*,*,#6561,.T.);
#8426=ORIENTED_EDGE('',*,*,#6562,.F.);
#8427=ORIENTED_EDGE('',*,*,#6561,.F.);
#8428=ORIENTED_EDGE('',*,*,#6563,.F.);
#8429=ORIENTED_EDGE('',*,*,#6564,.F.);
#8430=ORIENTED_EDGE('',*,*,#6565,.F.);
#8431=ORIENTED_EDGE('',*,*,#6566,.T.);
#8432=ORIENTED_EDGE('',*,*,#6567,.F.);
#8433=ORIENTED_EDGE('',*,*,#6566,.F.);
#8434=ORIENTED_EDGE('',*,*,#6568,.F.);
#8435=ORIENTED_EDGE('',*,*,#6569,.T.);
#8436=ORIENTED_EDGE('',*,*,#6570,.F.);
#8437=ORIENTED_EDGE('',*,*,#6569,.F.);
#8438=ORIENTED_EDGE('',*,*,#6571,.F.);
#8439=ORIENTED_EDGE('',*,*,#6572,.T.);
#8440=ORIENTED_EDGE('',*,*,#6573,.F.);
#8441=ORIENTED_EDGE('',*,*,#6572,.F.);
#8442=ORIENTED_EDGE('',*,*,#6574,.F.);
#8443=ORIENTED_EDGE('',*,*,#6564,.T.);
#8444=ORIENTED_EDGE('',*,*,#6575,.F.);
#8445=ORIENTED_EDGE('',*,*,#6576,.F.);
#8446=ORIENTED_EDGE('',*,*,#6577,.F.);
#8447=ORIENTED_EDGE('',*,*,#6578,.T.);
#8448=ORIENTED_EDGE('',*,*,#6579,.F.);
#8449=ORIENTED_EDGE('',*,*,#6578,.F.);
#8450=ORIENTED_EDGE('',*,*,#6580,.F.);
#8451=ORIENTED_EDGE('',*,*,#6581,.T.);
#8452=ORIENTED_EDGE('',*,*,#6582,.F.);
#8453=ORIENTED_EDGE('',*,*,#6581,.F.);
#8454=ORIENTED_EDGE('',*,*,#6583,.F.);
#8455=ORIENTED_EDGE('',*,*,#6584,.T.);
#8456=ORIENTED_EDGE('',*,*,#6585,.F.);
#8457=ORIENTED_EDGE('',*,*,#6584,.F.);
#8458=ORIENTED_EDGE('',*,*,#6586,.F.);
#8459=ORIENTED_EDGE('',*,*,#6576,.T.);
#8460=ORIENTED_EDGE('',*,*,#6587,.F.);
#8461=ORIENTED_EDGE('',*,*,#6588,.T.);
#8462=ORIENTED_EDGE('',*,*,#6589,.F.);
#8463=ORIENTED_EDGE('',*,*,#6588,.F.);
#8464=ORIENTED_EDGE('',*,*,#6590,.F.);
#8465=ORIENTED_EDGE('',*,*,#6591,.T.);
#8466=ORIENTED_EDGE('',*,*,#6592,.F.);
#8467=ORIENTED_EDGE('',*,*,#6591,.F.);
#8468=ORIENTED_EDGE('',*,*,#6593,.F.);
#8469=ORIENTED_EDGE('',*,*,#6594,.T.);
#8470=ORIENTED_EDGE('',*,*,#6595,.F.);
#8471=ORIENTED_EDGE('',*,*,#6594,.F.);
#8472=ORIENTED_EDGE('',*,*,#6596,.F.);
#8473=ORIENTED_EDGE('',*,*,#6597,.T.);
#8474=ORIENTED_EDGE('',*,*,#6598,.F.);
#8475=ORIENTED_EDGE('',*,*,#6597,.F.);
#8476=ORIENTED_EDGE('',*,*,#6599,.F.);
#8477=ORIENTED_EDGE('',*,*,#6600,.T.);
#8478=ORIENTED_EDGE('',*,*,#6601,.F.);
#8479=ORIENTED_EDGE('',*,*,#6600,.F.);
#8480=ORIENTED_EDGE('',*,*,#6602,.F.);
#8481=ORIENTED_EDGE('',*,*,#6603,.F.);
#8482=ORIENTED_EDGE('',*,*,#6604,.F.);
#8483=ORIENTED_EDGE('',*,*,#6605,.T.);
#8484=ORIENTED_EDGE('',*,*,#6606,.F.);
#8485=ORIENTED_EDGE('',*,*,#6605,.F.);
#8486=ORIENTED_EDGE('',*,*,#6607,.F.);
#8487=ORIENTED_EDGE('',*,*,#6608,.T.);
#8488=ORIENTED_EDGE('',*,*,#6609,.F.);
#8489=ORIENTED_EDGE('',*,*,#6608,.F.);
#8490=ORIENTED_EDGE('',*,*,#6610,.F.);
#8491=ORIENTED_EDGE('',*,*,#6611,.T.);
#8492=ORIENTED_EDGE('',*,*,#6612,.F.);
#8493=ORIENTED_EDGE('',*,*,#6611,.F.);
#8494=ORIENTED_EDGE('',*,*,#6613,.F.);
#8495=ORIENTED_EDGE('',*,*,#6603,.T.);
#8496=ORIENTED_EDGE('',*,*,#6614,.F.);
#8497=ORIENTED_EDGE('',*,*,#6615,.F.);
#8498=ORIENTED_EDGE('',*,*,#6616,.F.);
#8499=ORIENTED_EDGE('',*,*,#6617,.T.);
#8500=ORIENTED_EDGE('',*,*,#6618,.F.);
#8501=ORIENTED_EDGE('',*,*,#6617,.F.);
#8502=ORIENTED_EDGE('',*,*,#6619,.F.);
#8503=ORIENTED_EDGE('',*,*,#6620,.T.);
#8504=ORIENTED_EDGE('',*,*,#6621,.F.);
#8505=ORIENTED_EDGE('',*,*,#6620,.F.);
#8506=ORIENTED_EDGE('',*,*,#6622,.F.);
#8507=ORIENTED_EDGE('',*,*,#6623,.T.);
#8508=ORIENTED_EDGE('',*,*,#6624,.F.);
#8509=ORIENTED_EDGE('',*,*,#6623,.F.);
#8510=ORIENTED_EDGE('',*,*,#6625,.F.);
#8511=ORIENTED_EDGE('',*,*,#6615,.T.);
#8512=ORIENTED_EDGE('',*,*,#6626,.F.);
#8513=ORIENTED_EDGE('',*,*,#6627,.T.);
#8514=ORIENTED_EDGE('',*,*,#6628,.F.);
#8515=ORIENTED_EDGE('',*,*,#6627,.F.);
#8516=ORIENTED_EDGE('',*,*,#6629,.F.);
#8517=ORIENTED_EDGE('',*,*,#6630,.T.);
#8518=ORIENTED_EDGE('',*,*,#6631,.F.);
#8519=ORIENTED_EDGE('',*,*,#6630,.F.);
#8520=ORIENTED_EDGE('',*,*,#6632,.F.);
#8521=ORIENTED_EDGE('',*,*,#6633,.T.);
#8522=ORIENTED_EDGE('',*,*,#6634,.F.);
#8523=ORIENTED_EDGE('',*,*,#6633,.F.);
#8524=ORIENTED_EDGE('',*,*,#6635,.F.);
#8525=ORIENTED_EDGE('',*,*,#6636,.T.);
#8526=ORIENTED_EDGE('',*,*,#6637,.F.);
#8527=ORIENTED_EDGE('',*,*,#6636,.F.);
#8528=ORIENTED_EDGE('',*,*,#6638,.F.);
#8529=ORIENTED_EDGE('',*,*,#6639,.T.);
#8530=ORIENTED_EDGE('',*,*,#6640,.F.);
#8531=ORIENTED_EDGE('',*,*,#6639,.F.);
#8532=ORIENTED_EDGE('',*,*,#6641,.F.);
#8533=ORIENTED_EDGE('',*,*,#6642,.F.);
#8534=ORIENTED_EDGE('',*,*,#6643,.F.);
#8535=ORIENTED_EDGE('',*,*,#6644,.T.);
#8536=ORIENTED_EDGE('',*,*,#6645,.F.);
#8537=ORIENTED_EDGE('',*,*,#6644,.F.);
#8538=ORIENTED_EDGE('',*,*,#6646,.F.);
#8539=ORIENTED_EDGE('',*,*,#6647,.T.);
#8540=ORIENTED_EDGE('',*,*,#6648,.F.);
#8541=ORIENTED_EDGE('',*,*,#6647,.F.);
#8542=ORIENTED_EDGE('',*,*,#6649,.F.);
#8543=ORIENTED_EDGE('',*,*,#6650,.T.);
#8544=ORIENTED_EDGE('',*,*,#6651,.F.);
#8545=ORIENTED_EDGE('',*,*,#6650,.F.);
#8546=ORIENTED_EDGE('',*,*,#6652,.F.);
#8547=ORIENTED_EDGE('',*,*,#6642,.T.);
#8548=ORIENTED_EDGE('',*,*,#6653,.F.);
#8549=ORIENTED_EDGE('',*,*,#6654,.F.);
#8550=ORIENTED_EDGE('',*,*,#6655,.F.);
#8551=ORIENTED_EDGE('',*,*,#6656,.T.);
#8552=ORIENTED_EDGE('',*,*,#6657,.F.);
#8553=ORIENTED_EDGE('',*,*,#6656,.F.);
#8554=ORIENTED_EDGE('',*,*,#6658,.F.);
#8555=ORIENTED_EDGE('',*,*,#6659,.T.);
#8556=ORIENTED_EDGE('',*,*,#6660,.F.);
#8557=ORIENTED_EDGE('',*,*,#6659,.F.);
#8558=ORIENTED_EDGE('',*,*,#6661,.F.);
#8559=ORIENTED_EDGE('',*,*,#6662,.T.);
#8560=ORIENTED_EDGE('',*,*,#6663,.F.);
#8561=ORIENTED_EDGE('',*,*,#6662,.F.);
#8562=ORIENTED_EDGE('',*,*,#6664,.F.);
#8563=ORIENTED_EDGE('',*,*,#6654,.T.);
#8564=ORIENTED_EDGE('',*,*,#6665,.F.);
#8565=ORIENTED_EDGE('',*,*,#6666,.T.);
#8566=ORIENTED_EDGE('',*,*,#6667,.F.);
#8567=ORIENTED_EDGE('',*,*,#6666,.F.);
#8568=ORIENTED_EDGE('',*,*,#6668,.F.);
#8569=ORIENTED_EDGE('',*,*,#6669,.T.);
#8570=ORIENTED_EDGE('',*,*,#6670,.F.);
#8571=ORIENTED_EDGE('',*,*,#6669,.F.);
#8572=ORIENTED_EDGE('',*,*,#6671,.F.);
#8573=ORIENTED_EDGE('',*,*,#6672,.T.);
#8574=ORIENTED_EDGE('',*,*,#6673,.F.);
#8575=ORIENTED_EDGE('',*,*,#6672,.F.);
#8576=ORIENTED_EDGE('',*,*,#6674,.F.);
#8577=ORIENTED_EDGE('',*,*,#6675,.T.);
#8578=ORIENTED_EDGE('',*,*,#6676,.F.);
#8579=ORIENTED_EDGE('',*,*,#6675,.F.);
#8580=ORIENTED_EDGE('',*,*,#6677,.F.);
#8581=ORIENTED_EDGE('',*,*,#6678,.T.);
#8582=ORIENTED_EDGE('',*,*,#6679,.F.);
#8583=ORIENTED_EDGE('',*,*,#6678,.F.);
#8584=ORIENTED_EDGE('',*,*,#6680,.F.);
#8585=ORIENTED_EDGE('',*,*,#6681,.F.);
#8586=ORIENTED_EDGE('',*,*,#6682,.F.);
#8587=ORIENTED_EDGE('',*,*,#6683,.T.);
#8588=ORIENTED_EDGE('',*,*,#6684,.F.);
#8589=ORIENTED_EDGE('',*,*,#6683,.F.);
#8590=ORIENTED_EDGE('',*,*,#6685,.F.);
#8591=ORIENTED_EDGE('',*,*,#6686,.T.);
#8592=ORIENTED_EDGE('',*,*,#6687,.F.);
#8593=ORIENTED_EDGE('',*,*,#6686,.F.);
#8594=ORIENTED_EDGE('',*,*,#6688,.F.);
#8595=ORIENTED_EDGE('',*,*,#6689,.T.);
#8596=ORIENTED_EDGE('',*,*,#6690,.F.);
#8597=ORIENTED_EDGE('',*,*,#6689,.F.);
#8598=ORIENTED_EDGE('',*,*,#6691,.F.);
#8599=ORIENTED_EDGE('',*,*,#6681,.T.);
#8600=ORIENTED_EDGE('',*,*,#6692,.F.);
#8601=ORIENTED_EDGE('',*,*,#6693,.F.);
#8602=ORIENTED_EDGE('',*,*,#6694,.F.);
#8603=ORIENTED_EDGE('',*,*,#6695,.T.);
#8604=ORIENTED_EDGE('',*,*,#6696,.F.);
#8605=ORIENTED_EDGE('',*,*,#6695,.F.);
#8606=ORIENTED_EDGE('',*,*,#6697,.F.);
#8607=ORIENTED_EDGE('',*,*,#6698,.T.);
#8608=ORIENTED_EDGE('',*,*,#6699,.F.);
#8609=ORIENTED_EDGE('',*,*,#6698,.F.);
#8610=ORIENTED_EDGE('',*,*,#6700,.F.);
#8611=ORIENTED_EDGE('',*,*,#6701,.T.);
#8612=ORIENTED_EDGE('',*,*,#6702,.F.);
#8613=ORIENTED_EDGE('',*,*,#6701,.F.);
#8614=ORIENTED_EDGE('',*,*,#6703,.F.);
#8615=ORIENTED_EDGE('',*,*,#6693,.T.);
#8616=ORIENTED_EDGE('',*,*,#6704,.F.);
#8617=ORIENTED_EDGE('',*,*,#6705,.T.);
#8618=ORIENTED_EDGE('',*,*,#6706,.F.);
#8619=ORIENTED_EDGE('',*,*,#6705,.F.);
#8620=ORIENTED_EDGE('',*,*,#6707,.F.);
#8621=ORIENTED_EDGE('',*,*,#6708,.T.);
#8622=ORIENTED_EDGE('',*,*,#6709,.F.);
#8623=ORIENTED_EDGE('',*,*,#6708,.F.);
#8624=ORIENTED_EDGE('',*,*,#6710,.F.);
#8625=ORIENTED_EDGE('',*,*,#6711,.T.);
#8626=ORIENTED_EDGE('',*,*,#6712,.F.);
#8627=ORIENTED_EDGE('',*,*,#6711,.F.);
#8628=ORIENTED_EDGE('',*,*,#6713,.F.);
#8629=ORIENTED_EDGE('',*,*,#6714,.T.);
#8630=ORIENTED_EDGE('',*,*,#6715,.F.);
#8631=ORIENTED_EDGE('',*,*,#6714,.F.);
#8632=ORIENTED_EDGE('',*,*,#6716,.F.);
#8633=ORIENTED_EDGE('',*,*,#6717,.T.);
#8634=ORIENTED_EDGE('',*,*,#6718,.F.);
#8635=ORIENTED_EDGE('',*,*,#6717,.F.);
#8636=ORIENTED_EDGE('',*,*,#6719,.F.);
#8637=ORIENTED_EDGE('',*,*,#6720,.F.);
#8638=ORIENTED_EDGE('',*,*,#6721,.F.);
#8639=ORIENTED_EDGE('',*,*,#6722,.T.);
#8640=ORIENTED_EDGE('',*,*,#6723,.F.);
#8641=ORIENTED_EDGE('',*,*,#6722,.F.);
#8642=ORIENTED_EDGE('',*,*,#6724,.F.);
#8643=ORIENTED_EDGE('',*,*,#6725,.T.);
#8644=ORIENTED_EDGE('',*,*,#6726,.F.);
#8645=ORIENTED_EDGE('',*,*,#6725,.F.);
#8646=ORIENTED_EDGE('',*,*,#6727,.F.);
#8647=ORIENTED_EDGE('',*,*,#6728,.T.);
#8648=ORIENTED_EDGE('',*,*,#6729,.F.);
#8649=ORIENTED_EDGE('',*,*,#6728,.F.);
#8650=ORIENTED_EDGE('',*,*,#6730,.F.);
#8651=ORIENTED_EDGE('',*,*,#6720,.T.);
#8652=ORIENTED_EDGE('',*,*,#6731,.F.);
#8653=ORIENTED_EDGE('',*,*,#6732,.F.);
#8654=ORIENTED_EDGE('',*,*,#6733,.F.);
#8655=ORIENTED_EDGE('',*,*,#6734,.T.);
#8656=ORIENTED_EDGE('',*,*,#6735,.F.);
#8657=ORIENTED_EDGE('',*,*,#6734,.F.);
#8658=ORIENTED_EDGE('',*,*,#6736,.F.);
#8659=ORIENTED_EDGE('',*,*,#6737,.T.);
#8660=ORIENTED_EDGE('',*,*,#6738,.F.);
#8661=ORIENTED_EDGE('',*,*,#6737,.F.);
#8662=ORIENTED_EDGE('',*,*,#6739,.F.);
#8663=ORIENTED_EDGE('',*,*,#6740,.T.);
#8664=ORIENTED_EDGE('',*,*,#6741,.F.);
#8665=ORIENTED_EDGE('',*,*,#6740,.F.);
#8666=ORIENTED_EDGE('',*,*,#6742,.F.);
#8667=ORIENTED_EDGE('',*,*,#6732,.T.);
#8668=ORIENTED_EDGE('',*,*,#6743,.F.);
#8669=ORIENTED_EDGE('',*,*,#6744,.T.);
#8670=ORIENTED_EDGE('',*,*,#6745,.F.);
#8671=ORIENTED_EDGE('',*,*,#6744,.F.);
#8672=ORIENTED_EDGE('',*,*,#6746,.F.);
#8673=ORIENTED_EDGE('',*,*,#6747,.T.);
#8674=ORIENTED_EDGE('',*,*,#6748,.F.);
#8675=ORIENTED_EDGE('',*,*,#6747,.F.);
#8676=ORIENTED_EDGE('',*,*,#6749,.F.);
#8677=ORIENTED_EDGE('',*,*,#6750,.T.);
#8678=ORIENTED_EDGE('',*,*,#6751,.F.);
#8679=ORIENTED_EDGE('',*,*,#6750,.F.);
#8680=ORIENTED_EDGE('',*,*,#6752,.F.);
#8681=ORIENTED_EDGE('',*,*,#6753,.T.);
#8682=ORIENTED_EDGE('',*,*,#6754,.F.);
#8683=ORIENTED_EDGE('',*,*,#6753,.F.);
#8684=ORIENTED_EDGE('',*,*,#6755,.F.);
#8685=ORIENTED_EDGE('',*,*,#6756,.T.);
#8686=ORIENTED_EDGE('',*,*,#6757,.F.);
#8687=ORIENTED_EDGE('',*,*,#6756,.F.);
#8688=ORIENTED_EDGE('',*,*,#6758,.F.);
#8689=ORIENTED_EDGE('',*,*,#6759,.F.);
#8690=ORIENTED_EDGE('',*,*,#6760,.F.);
#8691=ORIENTED_EDGE('',*,*,#6761,.T.);
#8692=ORIENTED_EDGE('',*,*,#6762,.F.);
#8693=ORIENTED_EDGE('',*,*,#6761,.F.);
#8694=ORIENTED_EDGE('',*,*,#6763,.F.);
#8695=ORIENTED_EDGE('',*,*,#6764,.T.);
#8696=ORIENTED_EDGE('',*,*,#6765,.F.);
#8697=ORIENTED_EDGE('',*,*,#6764,.F.);
#8698=ORIENTED_EDGE('',*,*,#6766,.F.);
#8699=ORIENTED_EDGE('',*,*,#6767,.T.);
#8700=ORIENTED_EDGE('',*,*,#6768,.F.);
#8701=ORIENTED_EDGE('',*,*,#6767,.F.);
#8702=ORIENTED_EDGE('',*,*,#6769,.F.);
#8703=ORIENTED_EDGE('',*,*,#6759,.T.);
#8704=ORIENTED_EDGE('',*,*,#6770,.F.);
#8705=ORIENTED_EDGE('',*,*,#6771,.F.);
#8706=ORIENTED_EDGE('',*,*,#6772,.F.);
#8707=ORIENTED_EDGE('',*,*,#6773,.T.);
#8708=ORIENTED_EDGE('',*,*,#6774,.F.);
#8709=ORIENTED_EDGE('',*,*,#6773,.F.);
#8710=ORIENTED_EDGE('',*,*,#6775,.F.);
#8711=ORIENTED_EDGE('',*,*,#6776,.T.);
#8712=ORIENTED_EDGE('',*,*,#6777,.F.);
#8713=ORIENTED_EDGE('',*,*,#6776,.F.);
#8714=ORIENTED_EDGE('',*,*,#6778,.F.);
#8715=ORIENTED_EDGE('',*,*,#6779,.T.);
#8716=ORIENTED_EDGE('',*,*,#6780,.F.);
#8717=ORIENTED_EDGE('',*,*,#6779,.F.);
#8718=ORIENTED_EDGE('',*,*,#6781,.F.);
#8719=ORIENTED_EDGE('',*,*,#6771,.T.);
#8720=ORIENTED_EDGE('',*,*,#6782,.F.);
#8721=ORIENTED_EDGE('',*,*,#6783,.T.);
#8722=ORIENTED_EDGE('',*,*,#6784,.F.);
#8723=ORIENTED_EDGE('',*,*,#6783,.F.);
#8724=ORIENTED_EDGE('',*,*,#6785,.F.);
#8725=ORIENTED_EDGE('',*,*,#6786,.T.);
#8726=ORIENTED_EDGE('',*,*,#6787,.F.);
#8727=ORIENTED_EDGE('',*,*,#6786,.F.);
#8728=ORIENTED_EDGE('',*,*,#6788,.F.);
#8729=ORIENTED_EDGE('',*,*,#6789,.T.);
#8730=ORIENTED_EDGE('',*,*,#6790,.F.);
#8731=ORIENTED_EDGE('',*,*,#6789,.F.);
#8732=ORIENTED_EDGE('',*,*,#6791,.F.);
#8733=ORIENTED_EDGE('',*,*,#6792,.T.);
#8734=ORIENTED_EDGE('',*,*,#6793,.F.);
#8735=ORIENTED_EDGE('',*,*,#6792,.F.);
#8736=ORIENTED_EDGE('',*,*,#6794,.F.);
#8737=ORIENTED_EDGE('',*,*,#6795,.T.);
#8738=ORIENTED_EDGE('',*,*,#6796,.F.);
#8739=ORIENTED_EDGE('',*,*,#6795,.F.);
#8740=ORIENTED_EDGE('',*,*,#6797,.F.);
#8741=ORIENTED_EDGE('',*,*,#6798,.F.);
#8742=ORIENTED_EDGE('',*,*,#6799,.F.);
#8743=ORIENTED_EDGE('',*,*,#6800,.T.);
#8744=ORIENTED_EDGE('',*,*,#6801,.F.);
#8745=ORIENTED_EDGE('',*,*,#6800,.F.);
#8746=ORIENTED_EDGE('',*,*,#6802,.F.);
#8747=ORIENTED_EDGE('',*,*,#6803,.T.);
#8748=ORIENTED_EDGE('',*,*,#6804,.F.);
#8749=ORIENTED_EDGE('',*,*,#6803,.F.);
#8750=ORIENTED_EDGE('',*,*,#6805,.F.);
#8751=ORIENTED_EDGE('',*,*,#6806,.T.);
#8752=ORIENTED_EDGE('',*,*,#6807,.F.);
#8753=ORIENTED_EDGE('',*,*,#6806,.F.);
#8754=ORIENTED_EDGE('',*,*,#6808,.F.);
#8755=ORIENTED_EDGE('',*,*,#6798,.T.);
#8756=ORIENTED_EDGE('',*,*,#6809,.F.);
#8757=ORIENTED_EDGE('',*,*,#6810,.F.);
#8758=ORIENTED_EDGE('',*,*,#6811,.F.);
#8759=ORIENTED_EDGE('',*,*,#6812,.T.);
#8760=ORIENTED_EDGE('',*,*,#6813,.F.);
#8761=ORIENTED_EDGE('',*,*,#6812,.F.);
#8762=ORIENTED_EDGE('',*,*,#6814,.F.);
#8763=ORIENTED_EDGE('',*,*,#6815,.T.);
#8764=ORIENTED_EDGE('',*,*,#6816,.F.);
#8765=ORIENTED_EDGE('',*,*,#6815,.F.);
#8766=ORIENTED_EDGE('',*,*,#6817,.F.);
#8767=ORIENTED_EDGE('',*,*,#6818,.T.);
#8768=ORIENTED_EDGE('',*,*,#6819,.F.);
#8769=ORIENTED_EDGE('',*,*,#6818,.F.);
#8770=ORIENTED_EDGE('',*,*,#6820,.F.);
#8771=ORIENTED_EDGE('',*,*,#6810,.T.);
#8772=ORIENTED_EDGE('',*,*,#6821,.F.);
#8773=ORIENTED_EDGE('',*,*,#6822,.T.);
#8774=ORIENTED_EDGE('',*,*,#6823,.F.);
#8775=ORIENTED_EDGE('',*,*,#6822,.F.);
#8776=ORIENTED_EDGE('',*,*,#6824,.F.);
#8777=ORIENTED_EDGE('',*,*,#6825,.T.);
#8778=ORIENTED_EDGE('',*,*,#6826,.F.);
#8779=ORIENTED_EDGE('',*,*,#6825,.F.);
#8780=ORIENTED_EDGE('',*,*,#6827,.F.);
#8781=ORIENTED_EDGE('',*,*,#6828,.T.);
#8782=ORIENTED_EDGE('',*,*,#6829,.F.);
#8783=ORIENTED_EDGE('',*,*,#6828,.F.);
#8784=ORIENTED_EDGE('',*,*,#6830,.F.);
#8785=ORIENTED_EDGE('',*,*,#6831,.T.);
#8786=ORIENTED_EDGE('',*,*,#6832,.F.);
#8787=ORIENTED_EDGE('',*,*,#6831,.F.);
#8788=ORIENTED_EDGE('',*,*,#6833,.F.);
#8789=ORIENTED_EDGE('',*,*,#6834,.T.);
#8790=ORIENTED_EDGE('',*,*,#6835,.F.);
#8791=ORIENTED_EDGE('',*,*,#6834,.F.);
#8792=ORIENTED_EDGE('',*,*,#6836,.F.);
#8793=ORIENTED_EDGE('',*,*,#6837,.F.);
#8794=ORIENTED_EDGE('',*,*,#6838,.F.);
#8795=ORIENTED_EDGE('',*,*,#6839,.T.);
#8796=ORIENTED_EDGE('',*,*,#6840,.F.);
#8797=ORIENTED_EDGE('',*,*,#6839,.F.);
#8798=ORIENTED_EDGE('',*,*,#6841,.F.);
#8799=ORIENTED_EDGE('',*,*,#6842,.T.);
#8800=ORIENTED_EDGE('',*,*,#6843,.F.);
#8801=ORIENTED_EDGE('',*,*,#6842,.F.);
#8802=ORIENTED_EDGE('',*,*,#6844,.F.);
#8803=ORIENTED_EDGE('',*,*,#6845,.T.);
#8804=ORIENTED_EDGE('',*,*,#6846,.F.);
#8805=ORIENTED_EDGE('',*,*,#6845,.F.);
#8806=ORIENTED_EDGE('',*,*,#6847,.F.);
#8807=ORIENTED_EDGE('',*,*,#6837,.T.);
#8808=ORIENTED_EDGE('',*,*,#6848,.F.);
#8809=ORIENTED_EDGE('',*,*,#6849,.F.);
#8810=ORIENTED_EDGE('',*,*,#6850,.F.);
#8811=ORIENTED_EDGE('',*,*,#6851,.T.);
#8812=ORIENTED_EDGE('',*,*,#6852,.F.);
#8813=ORIENTED_EDGE('',*,*,#6851,.F.);
#8814=ORIENTED_EDGE('',*,*,#6853,.F.);
#8815=ORIENTED_EDGE('',*,*,#6854,.T.);
#8816=ORIENTED_EDGE('',*,*,#6855,.F.);
#8817=ORIENTED_EDGE('',*,*,#6854,.F.);
#8818=ORIENTED_EDGE('',*,*,#6856,.F.);
#8819=ORIENTED_EDGE('',*,*,#6857,.T.);
#8820=ORIENTED_EDGE('',*,*,#6858,.F.);
#8821=ORIENTED_EDGE('',*,*,#6857,.F.);
#8822=ORIENTED_EDGE('',*,*,#6859,.F.);
#8823=ORIENTED_EDGE('',*,*,#6849,.T.);
#8824=ORIENTED_EDGE('',*,*,#6860,.F.);
#8825=ORIENTED_EDGE('',*,*,#6861,.T.);
#8826=ORIENTED_EDGE('',*,*,#6862,.F.);
#8827=ORIENTED_EDGE('',*,*,#6861,.F.);
#8828=ORIENTED_EDGE('',*,*,#6863,.F.);
#8829=ORIENTED_EDGE('',*,*,#6864,.T.);
#8830=ORIENTED_EDGE('',*,*,#6865,.F.);
#8831=ORIENTED_EDGE('',*,*,#6864,.F.);
#8832=ORIENTED_EDGE('',*,*,#6866,.F.);
#8833=ORIENTED_EDGE('',*,*,#6867,.F.);
#8834=ORIENTED_EDGE('',*,*,#6868,.F.);
#8835=ORIENTED_EDGE('',*,*,#6869,.T.);
#8836=ORIENTED_EDGE('',*,*,#6870,.F.);
#8837=ORIENTED_EDGE('',*,*,#6869,.F.);
#8838=ORIENTED_EDGE('',*,*,#6871,.F.);
#8839=ORIENTED_EDGE('',*,*,#6872,.T.);
#8840=ORIENTED_EDGE('',*,*,#6873,.F.);
#8841=ORIENTED_EDGE('',*,*,#6872,.F.);
#8842=ORIENTED_EDGE('',*,*,#6874,.F.);
#8843=ORIENTED_EDGE('',*,*,#6875,.T.);
#8844=ORIENTED_EDGE('',*,*,#6876,.F.);
#8845=ORIENTED_EDGE('',*,*,#6875,.F.);
#8846=ORIENTED_EDGE('',*,*,#6877,.F.);
#8847=ORIENTED_EDGE('',*,*,#6867,.T.);
#8848=ORIENTED_EDGE('',*,*,#6878,.F.);
#8849=ORIENTED_EDGE('',*,*,#6879,.F.);
#8850=ORIENTED_EDGE('',*,*,#6880,.F.);
#8851=ORIENTED_EDGE('',*,*,#6881,.T.);
#8852=ORIENTED_EDGE('',*,*,#6882,.F.);
#8853=ORIENTED_EDGE('',*,*,#6881,.F.);
#8854=ORIENTED_EDGE('',*,*,#6883,.F.);
#8855=ORIENTED_EDGE('',*,*,#6884,.T.);
#8856=ORIENTED_EDGE('',*,*,#6885,.F.);
#8857=ORIENTED_EDGE('',*,*,#6884,.F.);
#8858=ORIENTED_EDGE('',*,*,#6886,.F.);
#8859=ORIENTED_EDGE('',*,*,#6887,.T.);
#8860=ORIENTED_EDGE('',*,*,#6888,.F.);
#8861=ORIENTED_EDGE('',*,*,#6887,.F.);
#8862=ORIENTED_EDGE('',*,*,#6889,.F.);
#8863=ORIENTED_EDGE('',*,*,#6879,.T.);
#8864=ORIENTED_EDGE('',*,*,#6890,.F.);
#8865=ORIENTED_EDGE('',*,*,#6891,.T.);
#8866=ORIENTED_EDGE('',*,*,#6892,.F.);
#8867=ORIENTED_EDGE('',*,*,#6891,.F.);
#8868=ORIENTED_EDGE('',*,*,#6893,.F.);
#8869=ORIENTED_EDGE('',*,*,#6894,.T.);
#8870=ORIENTED_EDGE('',*,*,#6895,.F.);
#8871=ORIENTED_EDGE('',*,*,#6894,.F.);
#8872=ORIENTED_EDGE('',*,*,#6896,.F.);
#8873=ORIENTED_EDGE('',*,*,#6897,.T.);
#8874=ORIENTED_EDGE('',*,*,#6898,.F.);
#8875=ORIENTED_EDGE('',*,*,#6897,.F.);
#8876=ORIENTED_EDGE('',*,*,#6899,.T.);
#8877=ORIENTED_EDGE('',*,*,#6900,.T.);
#8878=ORIENTED_EDGE('',*,*,#6901,.T.);
#8879=ORIENTED_EDGE('',*,*,#6902,.T.);
#8880=ORIENTED_EDGE('',*,*,#6900,.F.);
#8881=ORIENTED_EDGE('',*,*,#6903,.T.);
#8882=ORIENTED_EDGE('',*,*,#6904,.F.);
#8883=ORIENTED_EDGE('',*,*,#6905,.F.);
#8884=ORIENTED_EDGE('',*,*,#6862,.T.);
#8885=ORIENTED_EDGE('',*,*,#6865,.T.);
#8886=ORIENTED_EDGE('',*,*,#6873,.T.);
#8887=ORIENTED_EDGE('',*,*,#6876,.T.);
#8888=ORIENTED_EDGE('',*,*,#6866,.T.);
#8889=ORIENTED_EDGE('',*,*,#6870,.T.);
#8890=ORIENTED_EDGE('',*,*,#6885,.T.);
#8891=ORIENTED_EDGE('',*,*,#6888,.T.);
#8892=ORIENTED_EDGE('',*,*,#6878,.T.);
#8893=ORIENTED_EDGE('',*,*,#6882,.T.);
#8894=ORIENTED_EDGE('',*,*,#6892,.T.);
#8895=ORIENTED_EDGE('',*,*,#6895,.T.);
#8896=ORIENTED_EDGE('',*,*,#6898,.T.);
#8897=ORIENTED_EDGE('',*,*,#6855,.T.);
#8898=ORIENTED_EDGE('',*,*,#6858,.T.);
#8899=ORIENTED_EDGE('',*,*,#6848,.T.);
#8900=ORIENTED_EDGE('',*,*,#6852,.T.);
#8901=ORIENTED_EDGE('',*,*,#6843,.T.);
#8902=ORIENTED_EDGE('',*,*,#6846,.T.);
#8903=ORIENTED_EDGE('',*,*,#6836,.T.);
#8904=ORIENTED_EDGE('',*,*,#6840,.T.);
#8905=ORIENTED_EDGE('',*,*,#6835,.T.);
#8906=ORIENTED_EDGE('',*,*,#6832,.T.);
#8907=ORIENTED_EDGE('',*,*,#6829,.T.);
#8908=ORIENTED_EDGE('',*,*,#6826,.T.);
#8909=ORIENTED_EDGE('',*,*,#6823,.T.);
#8910=ORIENTED_EDGE('',*,*,#6816,.T.);
#8911=ORIENTED_EDGE('',*,*,#6819,.T.);
#8912=ORIENTED_EDGE('',*,*,#6809,.T.);
#8913=ORIENTED_EDGE('',*,*,#6813,.T.);
#8914=ORIENTED_EDGE('',*,*,#6804,.T.);
#8915=ORIENTED_EDGE('',*,*,#6807,.T.);
#8916=ORIENTED_EDGE('',*,*,#6797,.T.);
#8917=ORIENTED_EDGE('',*,*,#6801,.T.);
#8918=ORIENTED_EDGE('',*,*,#6796,.T.);
#8919=ORIENTED_EDGE('',*,*,#6793,.T.);
#8920=ORIENTED_EDGE('',*,*,#6790,.T.);
#8921=ORIENTED_EDGE('',*,*,#6787,.T.);
#8922=ORIENTED_EDGE('',*,*,#6784,.T.);
#8923=ORIENTED_EDGE('',*,*,#6777,.T.);
#8924=ORIENTED_EDGE('',*,*,#6780,.T.);
#8925=ORIENTED_EDGE('',*,*,#6770,.T.);
#8926=ORIENTED_EDGE('',*,*,#6774,.T.);
#8927=ORIENTED_EDGE('',*,*,#6765,.T.);
#8928=ORIENTED_EDGE('',*,*,#6768,.T.);
#8929=ORIENTED_EDGE('',*,*,#6758,.T.);
#8930=ORIENTED_EDGE('',*,*,#6762,.T.);
#8931=ORIENTED_EDGE('',*,*,#6757,.T.);
#8932=ORIENTED_EDGE('',*,*,#6754,.T.);
#8933=ORIENTED_EDGE('',*,*,#6751,.T.);
#8934=ORIENTED_EDGE('',*,*,#6748,.T.);
#8935=ORIENTED_EDGE('',*,*,#6745,.T.);
#8936=ORIENTED_EDGE('',*,*,#6738,.T.);
#8937=ORIENTED_EDGE('',*,*,#6741,.T.);
#8938=ORIENTED_EDGE('',*,*,#6731,.T.);
#8939=ORIENTED_EDGE('',*,*,#6735,.T.);
#8940=ORIENTED_EDGE('',*,*,#6726,.T.);
#8941=ORIENTED_EDGE('',*,*,#6729,.T.);
#8942=ORIENTED_EDGE('',*,*,#6719,.T.);
#8943=ORIENTED_EDGE('',*,*,#6723,.T.);
#8944=ORIENTED_EDGE('',*,*,#6718,.T.);
#8945=ORIENTED_EDGE('',*,*,#6715,.T.);
#8946=ORIENTED_EDGE('',*,*,#6712,.T.);
#8947=ORIENTED_EDGE('',*,*,#6709,.T.);
#8948=ORIENTED_EDGE('',*,*,#6706,.T.);
#8949=ORIENTED_EDGE('',*,*,#6699,.T.);
#8950=ORIENTED_EDGE('',*,*,#6702,.T.);
#8951=ORIENTED_EDGE('',*,*,#6692,.T.);
#8952=ORIENTED_EDGE('',*,*,#6696,.T.);
#8953=ORIENTED_EDGE('',*,*,#6687,.T.);
#8954=ORIENTED_EDGE('',*,*,#6690,.T.);
#8955=ORIENTED_EDGE('',*,*,#6680,.T.);
#8956=ORIENTED_EDGE('',*,*,#6684,.T.);
#8957=ORIENTED_EDGE('',*,*,#6679,.T.);
#8958=ORIENTED_EDGE('',*,*,#6676,.T.);
#8959=ORIENTED_EDGE('',*,*,#6673,.T.);
#8960=ORIENTED_EDGE('',*,*,#6670,.T.);
#8961=ORIENTED_EDGE('',*,*,#6667,.T.);
#8962=ORIENTED_EDGE('',*,*,#6660,.T.);
#8963=ORIENTED_EDGE('',*,*,#6663,.T.);
#8964=ORIENTED_EDGE('',*,*,#6653,.T.);
#8965=ORIENTED_EDGE('',*,*,#6657,.T.);
#8966=ORIENTED_EDGE('',*,*,#6648,.T.);
#8967=ORIENTED_EDGE('',*,*,#6651,.T.);
#8968=ORIENTED_EDGE('',*,*,#6641,.T.);
#8969=ORIENTED_EDGE('',*,*,#6645,.T.);
#8970=ORIENTED_EDGE('',*,*,#6640,.T.);
#8971=ORIENTED_EDGE('',*,*,#6637,.T.);
#8972=ORIENTED_EDGE('',*,*,#6634,.T.);
#8973=ORIENTED_EDGE('',*,*,#6631,.T.);
#8974=ORIENTED_EDGE('',*,*,#6628,.T.);
#8975=ORIENTED_EDGE('',*,*,#6621,.T.);
#8976=ORIENTED_EDGE('',*,*,#6624,.T.);
#8977=ORIENTED_EDGE('',*,*,#6614,.T.);
#8978=ORIENTED_EDGE('',*,*,#6618,.T.);
#8979=ORIENTED_EDGE('',*,*,#6609,.T.);
#8980=ORIENTED_EDGE('',*,*,#6612,.T.);
#8981=ORIENTED_EDGE('',*,*,#6602,.T.);
#8982=ORIENTED_EDGE('',*,*,#6606,.T.);
#8983=ORIENTED_EDGE('',*,*,#6601,.T.);
#8984=ORIENTED_EDGE('',*,*,#6598,.T.);
#8985=ORIENTED_EDGE('',*,*,#6595,.T.);
#8986=ORIENTED_EDGE('',*,*,#6592,.T.);
#8987=ORIENTED_EDGE('',*,*,#6589,.T.);
#8988=ORIENTED_EDGE('',*,*,#6582,.T.);
#8989=ORIENTED_EDGE('',*,*,#6585,.T.);
#8990=ORIENTED_EDGE('',*,*,#6575,.T.);
#8991=ORIENTED_EDGE('',*,*,#6579,.T.);
#8992=ORIENTED_EDGE('',*,*,#6570,.T.);
#8993=ORIENTED_EDGE('',*,*,#6573,.T.);
#8994=ORIENTED_EDGE('',*,*,#6563,.T.);
#8995=ORIENTED_EDGE('',*,*,#6567,.T.);
#8996=ORIENTED_EDGE('',*,*,#6562,.T.);
#8997=ORIENTED_EDGE('',*,*,#6559,.T.);
#8998=ORIENTED_EDGE('',*,*,#6556,.T.);
#8999=ORIENTED_EDGE('',*,*,#6553,.T.);
#9000=ORIENTED_EDGE('',*,*,#6550,.T.);
#9001=ORIENTED_EDGE('',*,*,#6543,.T.);
#9002=ORIENTED_EDGE('',*,*,#6546,.T.);
#9003=ORIENTED_EDGE('',*,*,#6536,.T.);
#9004=ORIENTED_EDGE('',*,*,#6540,.T.);
#9005=ORIENTED_EDGE('',*,*,#6531,.T.);
#9006=ORIENTED_EDGE('',*,*,#6534,.T.);
#9007=ORIENTED_EDGE('',*,*,#6524,.T.);
#9008=ORIENTED_EDGE('',*,*,#6528,.T.);
#9009=ORIENTED_EDGE('',*,*,#6523,.T.);
#9010=ORIENTED_EDGE('',*,*,#6520,.T.);
#9011=ORIENTED_EDGE('',*,*,#6517,.T.);
#9012=ORIENTED_EDGE('',*,*,#6514,.T.);
#9013=ORIENTED_EDGE('',*,*,#6511,.T.);
#9014=ORIENTED_EDGE('',*,*,#6906,.T.);
#9015=ORIENTED_EDGE('',*,*,#6907,.T.);
#9016=ORIENTED_EDGE('',*,*,#6908,.T.);
#9017=ORIENTED_EDGE('',*,*,#6904,.T.);
#9018=ORIENTED_EDGE('',*,*,#6907,.F.);
#9019=ORIENTED_EDGE('',*,*,#6909,.T.);
#9020=ORIENTED_EDGE('',*,*,#6910,.T.);
#9021=ORIENTED_EDGE('',*,*,#6911,.T.);
#9022=ORIENTED_EDGE('',*,*,#6912,.F.);
#9023=ORIENTED_EDGE('',*,*,#6913,.F.);
#9024=ORIENTED_EDGE('',*,*,#6914,.F.);
#9025=ORIENTED_EDGE('',*,*,#6915,.F.);
#9026=ORIENTED_EDGE('',*,*,#6916,.F.);
#9027=ORIENTED_EDGE('',*,*,#6917,.F.);
#9028=ORIENTED_EDGE('',*,*,#6918,.F.);
#9029=ORIENTED_EDGE('',*,*,#6919,.F.);
#9030=ORIENTED_EDGE('',*,*,#6920,.F.);
#9031=ORIENTED_EDGE('',*,*,#6921,.F.);
#9032=ORIENTED_EDGE('',*,*,#6922,.F.);
#9033=ORIENTED_EDGE('',*,*,#6923,.F.);
#9034=ORIENTED_EDGE('',*,*,#6924,.F.);
#9035=ORIENTED_EDGE('',*,*,#6925,.F.);
#9036=ORIENTED_EDGE('',*,*,#6926,.F.);
#9037=ORIENTED_EDGE('',*,*,#6927,.F.);
#9038=ORIENTED_EDGE('',*,*,#6928,.F.);
#9039=ORIENTED_EDGE('',*,*,#6929,.F.);
#9040=ORIENTED_EDGE('',*,*,#6930,.F.);
#9041=ORIENTED_EDGE('',*,*,#6931,.F.);
#9042=ORIENTED_EDGE('',*,*,#6932,.F.);
#9043=ORIENTED_EDGE('',*,*,#6933,.F.);
#9044=ORIENTED_EDGE('',*,*,#6934,.F.);
#9045=ORIENTED_EDGE('',*,*,#6935,.F.);
#9046=ORIENTED_EDGE('',*,*,#6936,.F.);
#9047=ORIENTED_EDGE('',*,*,#6937,.F.);
#9048=ORIENTED_EDGE('',*,*,#6938,.F.);
#9049=ORIENTED_EDGE('',*,*,#6939,.F.);
#9050=ORIENTED_EDGE('',*,*,#6940,.F.);
#9051=ORIENTED_EDGE('',*,*,#6941,.F.);
#9052=ORIENTED_EDGE('',*,*,#6942,.F.);
#9053=ORIENTED_EDGE('',*,*,#6943,.F.);
#9054=ORIENTED_EDGE('',*,*,#6944,.F.);
#9055=ORIENTED_EDGE('',*,*,#6945,.F.);
#9056=ORIENTED_EDGE('',*,*,#6946,.F.);
#9057=ORIENTED_EDGE('',*,*,#6947,.F.);
#9058=ORIENTED_EDGE('',*,*,#6948,.F.);
#9059=ORIENTED_EDGE('',*,*,#6949,.F.);
#9060=ORIENTED_EDGE('',*,*,#6950,.F.);
#9061=ORIENTED_EDGE('',*,*,#6951,.F.);
#9062=ORIENTED_EDGE('',*,*,#6952,.F.);
#9063=ORIENTED_EDGE('',*,*,#6953,.F.);
#9064=ORIENTED_EDGE('',*,*,#6954,.F.);
#9065=ORIENTED_EDGE('',*,*,#6955,.F.);
#9066=ORIENTED_EDGE('',*,*,#6956,.F.);
#9067=ORIENTED_EDGE('',*,*,#6957,.F.);
#9068=ORIENTED_EDGE('',*,*,#6958,.F.);
#9069=ORIENTED_EDGE('',*,*,#6959,.T.);
#9070=ORIENTED_EDGE('',*,*,#6960,.T.);
#9071=ORIENTED_EDGE('',*,*,#6961,.T.);
#9072=ORIENTED_EDGE('',*,*,#6962,.T.);
#9073=ORIENTED_EDGE('',*,*,#6962,.F.);
#9074=ORIENTED_EDGE('',*,*,#6963,.F.);
#9075=ORIENTED_EDGE('',*,*,#6964,.F.);
#9076=ORIENTED_EDGE('',*,*,#6965,.T.);
#9077=ORIENTED_EDGE('',*,*,#6860,.T.);
#9078=ORIENTED_EDGE('',*,*,#6863,.T.);
#9079=ORIENTED_EDGE('',*,*,#6874,.T.);
#9080=ORIENTED_EDGE('',*,*,#6871,.T.);
#9081=ORIENTED_EDGE('',*,*,#6868,.T.);
#9082=ORIENTED_EDGE('',*,*,#6877,.T.);
#9083=ORIENTED_EDGE('',*,*,#6886,.T.);
#9084=ORIENTED_EDGE('',*,*,#6883,.T.);
#9085=ORIENTED_EDGE('',*,*,#6880,.T.);
#9086=ORIENTED_EDGE('',*,*,#6889,.T.);
#9087=ORIENTED_EDGE('',*,*,#6890,.T.);
#9088=ORIENTED_EDGE('',*,*,#6893,.T.);
#9089=ORIENTED_EDGE('',*,*,#6896,.T.);
#9090=ORIENTED_EDGE('',*,*,#6856,.T.);
#9091=ORIENTED_EDGE('',*,*,#6853,.T.);
#9092=ORIENTED_EDGE('',*,*,#6850,.T.);
#9093=ORIENTED_EDGE('',*,*,#6859,.T.);
#9094=ORIENTED_EDGE('',*,*,#6844,.T.);
#9095=ORIENTED_EDGE('',*,*,#6841,.T.);
#9096=ORIENTED_EDGE('',*,*,#6838,.T.);
#9097=ORIENTED_EDGE('',*,*,#6847,.T.);
#9098=ORIENTED_EDGE('',*,*,#6833,.T.);
#9099=ORIENTED_EDGE('',*,*,#6830,.T.);
#9100=ORIENTED_EDGE('',*,*,#6827,.T.);
#9101=ORIENTED_EDGE('',*,*,#6824,.T.);
#9102=ORIENTED_EDGE('',*,*,#6821,.T.);
#9103=ORIENTED_EDGE('',*,*,#6817,.T.);
#9104=ORIENTED_EDGE('',*,*,#6814,.T.);
#9105=ORIENTED_EDGE('',*,*,#6811,.T.);
#9106=ORIENTED_EDGE('',*,*,#6820,.T.);
#9107=ORIENTED_EDGE('',*,*,#6805,.T.);
#9108=ORIENTED_EDGE('',*,*,#6802,.T.);
#9109=ORIENTED_EDGE('',*,*,#6799,.T.);
#9110=ORIENTED_EDGE('',*,*,#6808,.T.);
#9111=ORIENTED_EDGE('',*,*,#6794,.T.);
#9112=ORIENTED_EDGE('',*,*,#6791,.T.);
#9113=ORIENTED_EDGE('',*,*,#6788,.T.);
#9114=ORIENTED_EDGE('',*,*,#6785,.T.);
#9115=ORIENTED_EDGE('',*,*,#6782,.T.);
#9116=ORIENTED_EDGE('',*,*,#6778,.T.);
#9117=ORIENTED_EDGE('',*,*,#6775,.T.);
#9118=ORIENTED_EDGE('',*,*,#6772,.T.);
#9119=ORIENTED_EDGE('',*,*,#6781,.T.);
#9120=ORIENTED_EDGE('',*,*,#6766,.T.);
#9121=ORIENTED_EDGE('',*,*,#6763,.T.);
#9122=ORIENTED_EDGE('',*,*,#6760,.T.);
#9123=ORIENTED_EDGE('',*,*,#6769,.T.);
#9124=ORIENTED_EDGE('',*,*,#6755,.T.);
#9125=ORIENTED_EDGE('',*,*,#6752,.T.);
#9126=ORIENTED_EDGE('',*,*,#6749,.T.);
#9127=ORIENTED_EDGE('',*,*,#6746,.T.);
#9128=ORIENTED_EDGE('',*,*,#6743,.T.);
#9129=ORIENTED_EDGE('',*,*,#6739,.T.);
#9130=ORIENTED_EDGE('',*,*,#6736,.T.);
#9131=ORIENTED_EDGE('',*,*,#6733,.T.);
#9132=ORIENTED_EDGE('',*,*,#6742,.T.);
#9133=ORIENTED_EDGE('',*,*,#6727,.T.);
#9134=ORIENTED_EDGE('',*,*,#6724,.T.);
#9135=ORIENTED_EDGE('',*,*,#6721,.T.);
#9136=ORIENTED_EDGE('',*,*,#6730,.T.);
#9137=ORIENTED_EDGE('',*,*,#6716,.T.);
#9138=ORIENTED_EDGE('',*,*,#6713,.T.);
#9139=ORIENTED_EDGE('',*,*,#6710,.T.);
#9140=ORIENTED_EDGE('',*,*,#6707,.T.);
#9141=ORIENTED_EDGE('',*,*,#6704,.T.);
#9142=ORIENTED_EDGE('',*,*,#6700,.T.);
#9143=ORIENTED_EDGE('',*,*,#6697,.T.);
#9144=ORIENTED_EDGE('',*,*,#6694,.T.);
#9145=ORIENTED_EDGE('',*,*,#6703,.T.);
#9146=ORIENTED_EDGE('',*,*,#6688,.T.);
#9147=ORIENTED_EDGE('',*,*,#6685,.T.);
#9148=ORIENTED_EDGE('',*,*,#6682,.T.);
#9149=ORIENTED_EDGE('',*,*,#6691,.T.);
#9150=ORIENTED_EDGE('',*,*,#6677,.T.);
#9151=ORIENTED_EDGE('',*,*,#6674,.T.);
#9152=ORIENTED_EDGE('',*,*,#6671,.T.);
#9153=ORIENTED_EDGE('',*,*,#6668,.T.);
#9154=ORIENTED_EDGE('',*,*,#6665,.T.);
#9155=ORIENTED_EDGE('',*,*,#6661,.T.);
#9156=ORIENTED_EDGE('',*,*,#6658,.T.);
#9157=ORIENTED_EDGE('',*,*,#6655,.T.);
#9158=ORIENTED_EDGE('',*,*,#6664,.T.);
#9159=ORIENTED_EDGE('',*,*,#6649,.T.);
#9160=ORIENTED_EDGE('',*,*,#6646,.T.);
#9161=ORIENTED_EDGE('',*,*,#6643,.T.);
#9162=ORIENTED_EDGE('',*,*,#6652,.T.);
#9163=ORIENTED_EDGE('',*,*,#6638,.T.);
#9164=ORIENTED_EDGE('',*,*,#6635,.T.);
#9165=ORIENTED_EDGE('',*,*,#6632,.T.);
#9166=ORIENTED_EDGE('',*,*,#6629,.T.);
#9167=ORIENTED_EDGE('',*,*,#6626,.T.);
#9168=ORIENTED_EDGE('',*,*,#6622,.T.);
#9169=ORIENTED_EDGE('',*,*,#6619,.T.);
#9170=ORIENTED_EDGE('',*,*,#6616,.T.);
#9171=ORIENTED_EDGE('',*,*,#6625,.T.);
#9172=ORIENTED_EDGE('',*,*,#6610,.T.);
#9173=ORIENTED_EDGE('',*,*,#6607,.T.);
#9174=ORIENTED_EDGE('',*,*,#6604,.T.);
#9175=ORIENTED_EDGE('',*,*,#6613,.T.);
#9176=ORIENTED_EDGE('',*,*,#6599,.T.);
#9177=ORIENTED_EDGE('',*,*,#6596,.T.);
#9178=ORIENTED_EDGE('',*,*,#6593,.T.);
#9179=ORIENTED_EDGE('',*,*,#6590,.T.);
#9180=ORIENTED_EDGE('',*,*,#6587,.T.);
#9181=ORIENTED_EDGE('',*,*,#6583,.T.);
#9182=ORIENTED_EDGE('',*,*,#6580,.T.);
#9183=ORIENTED_EDGE('',*,*,#6577,.T.);
#9184=ORIENTED_EDGE('',*,*,#6586,.T.);
#9185=ORIENTED_EDGE('',*,*,#6571,.T.);
#9186=ORIENTED_EDGE('',*,*,#6568,.T.);
#9187=ORIENTED_EDGE('',*,*,#6565,.T.);
#9188=ORIENTED_EDGE('',*,*,#6574,.T.);
#9189=ORIENTED_EDGE('',*,*,#6560,.T.);
#9190=ORIENTED_EDGE('',*,*,#6557,.T.);
#9191=ORIENTED_EDGE('',*,*,#6554,.T.);
#9192=ORIENTED_EDGE('',*,*,#6551,.T.);
#9193=ORIENTED_EDGE('',*,*,#6548,.T.);
#9194=ORIENTED_EDGE('',*,*,#6544,.T.);
#9195=ORIENTED_EDGE('',*,*,#6541,.T.);
#9196=ORIENTED_EDGE('',*,*,#6538,.T.);
#9197=ORIENTED_EDGE('',*,*,#6547,.T.);
#9198=ORIENTED_EDGE('',*,*,#6532,.T.);
#9199=ORIENTED_EDGE('',*,*,#6529,.T.);
#9200=ORIENTED_EDGE('',*,*,#6526,.T.);
#9201=ORIENTED_EDGE('',*,*,#6535,.T.);
#9202=ORIENTED_EDGE('',*,*,#6521,.T.);
#9203=ORIENTED_EDGE('',*,*,#6518,.T.);
#9204=ORIENTED_EDGE('',*,*,#6515,.T.);
#9205=ORIENTED_EDGE('',*,*,#6512,.T.);
#9206=ORIENTED_EDGE('',*,*,#6509,.T.);
#9207=ORIENTED_EDGE('',*,*,#6961,.F.);
#9208=ORIENTED_EDGE('',*,*,#6966,.F.);
#9209=ORIENTED_EDGE('',*,*,#6967,.F.);
#9210=ORIENTED_EDGE('',*,*,#6909,.F.);
#9211=ORIENTED_EDGE('',*,*,#6906,.F.);
#9212=ORIENTED_EDGE('',*,*,#6903,.F.);
#9213=ORIENTED_EDGE('',*,*,#6899,.F.);
#9214=ORIENTED_EDGE('',*,*,#6968,.F.);
#9215=ORIENTED_EDGE('',*,*,#6969,.F.);
#9216=ORIENTED_EDGE('',*,*,#6970,.F.);
#9217=ORIENTED_EDGE('',*,*,#6971,.F.);
#9218=ORIENTED_EDGE('',*,*,#6963,.T.);
#9219=ORIENTED_EDGE('',*,*,#6972,.T.);
#9220=ORIENTED_EDGE('',*,*,#6964,.T.);
#9221=ORIENTED_EDGE('',*,*,#6971,.T.);
#9222=ORIENTED_EDGE('',*,*,#6973,.T.);
#9223=ORIENTED_EDGE('',*,*,#6974,.F.);
#9224=ORIENTED_EDGE('',*,*,#6975,.T.);
#9225=ORIENTED_EDGE('',*,*,#6912,.T.);
#9226=ORIENTED_EDGE('',*,*,#6975,.F.);
#9227=ORIENTED_EDGE('',*,*,#6976,.F.);
#9228=ORIENTED_EDGE('',*,*,#6977,.T.);
#9229=ORIENTED_EDGE('',*,*,#6913,.T.);
#9230=ORIENTED_EDGE('',*,*,#6977,.F.);
#9231=ORIENTED_EDGE('',*,*,#6978,.F.);
#9232=ORIENTED_EDGE('',*,*,#6979,.T.);
#9233=ORIENTED_EDGE('',*,*,#6914,.T.);
#9234=ORIENTED_EDGE('',*,*,#6979,.F.);
#9235=ORIENTED_EDGE('',*,*,#6980,.F.);
#9236=ORIENTED_EDGE('',*,*,#6981,.T.);
#9237=ORIENTED_EDGE('',*,*,#6915,.T.);
#9238=ORIENTED_EDGE('',*,*,#6981,.F.);
#9239=ORIENTED_EDGE('',*,*,#6982,.F.);
#9240=ORIENTED_EDGE('',*,*,#6983,.T.);
#9241=ORIENTED_EDGE('',*,*,#6916,.T.);
#9242=ORIENTED_EDGE('',*,*,#6983,.F.);
#9243=ORIENTED_EDGE('',*,*,#6984,.F.);
#9244=ORIENTED_EDGE('',*,*,#6985,.T.);
#9245=ORIENTED_EDGE('',*,*,#6917,.T.);
#9246=ORIENTED_EDGE('',*,*,#6985,.F.);
#9247=ORIENTED_EDGE('',*,*,#6986,.F.);
#9248=ORIENTED_EDGE('',*,*,#6987,.T.);
#9249=ORIENTED_EDGE('',*,*,#6918,.T.);
#9250=ORIENTED_EDGE('',*,*,#6987,.F.);
#9251=ORIENTED_EDGE('',*,*,#6988,.F.);
#9252=ORIENTED_EDGE('',*,*,#6989,.T.);
#9253=ORIENTED_EDGE('',*,*,#6919,.T.);
#9254=ORIENTED_EDGE('',*,*,#6989,.F.);
#9255=ORIENTED_EDGE('',*,*,#6990,.F.);
#9256=ORIENTED_EDGE('',*,*,#6991,.T.);
#9257=ORIENTED_EDGE('',*,*,#6920,.T.);
#9258=ORIENTED_EDGE('',*,*,#6991,.F.);
#9259=ORIENTED_EDGE('',*,*,#6992,.F.);
#9260=ORIENTED_EDGE('',*,*,#6993,.T.);
#9261=ORIENTED_EDGE('',*,*,#6921,.T.);
#9262=ORIENTED_EDGE('',*,*,#6993,.F.);
#9263=ORIENTED_EDGE('',*,*,#6994,.F.);
#9264=ORIENTED_EDGE('',*,*,#6995,.T.);
#9265=ORIENTED_EDGE('',*,*,#6922,.T.);
#9266=ORIENTED_EDGE('',*,*,#6995,.F.);
#9267=ORIENTED_EDGE('',*,*,#6996,.F.);
#9268=ORIENTED_EDGE('',*,*,#6997,.T.);
#9269=ORIENTED_EDGE('',*,*,#6923,.T.);
#9270=ORIENTED_EDGE('',*,*,#6997,.F.);
#9271=ORIENTED_EDGE('',*,*,#6998,.F.);
#9272=ORIENTED_EDGE('',*,*,#6999,.T.);
#9273=ORIENTED_EDGE('',*,*,#6924,.T.);
#9274=ORIENTED_EDGE('',*,*,#6999,.F.);
#9275=ORIENTED_EDGE('',*,*,#7000,.F.);
#9276=ORIENTED_EDGE('',*,*,#7001,.T.);
#9277=ORIENTED_EDGE('',*,*,#6925,.T.);
#9278=ORIENTED_EDGE('',*,*,#7001,.F.);
#9279=ORIENTED_EDGE('',*,*,#7002,.F.);
#9280=ORIENTED_EDGE('',*,*,#7003,.T.);
#9281=ORIENTED_EDGE('',*,*,#6926,.T.);
#9282=ORIENTED_EDGE('',*,*,#7003,.F.);
#9283=ORIENTED_EDGE('',*,*,#7004,.F.);
#9284=ORIENTED_EDGE('',*,*,#7005,.T.);
#9285=ORIENTED_EDGE('',*,*,#6927,.T.);
#9286=ORIENTED_EDGE('',*,*,#7005,.F.);
#9287=ORIENTED_EDGE('',*,*,#7006,.F.);
#9288=ORIENTED_EDGE('',*,*,#7007,.T.);
#9289=ORIENTED_EDGE('',*,*,#6928,.T.);
#9290=ORIENTED_EDGE('',*,*,#7007,.F.);
#9291=ORIENTED_EDGE('',*,*,#7008,.F.);
#9292=ORIENTED_EDGE('',*,*,#7009,.T.);
#9293=ORIENTED_EDGE('',*,*,#6929,.T.);
#9294=ORIENTED_EDGE('',*,*,#7009,.F.);
#9295=ORIENTED_EDGE('',*,*,#7010,.F.);
#9296=ORIENTED_EDGE('',*,*,#7011,.T.);
#9297=ORIENTED_EDGE('',*,*,#6930,.T.);
#9298=ORIENTED_EDGE('',*,*,#7011,.F.);
#9299=ORIENTED_EDGE('',*,*,#7012,.F.);
#9300=ORIENTED_EDGE('',*,*,#7013,.T.);
#9301=ORIENTED_EDGE('',*,*,#6931,.T.);
#9302=ORIENTED_EDGE('',*,*,#7013,.F.);
#9303=ORIENTED_EDGE('',*,*,#7014,.F.);
#9304=ORIENTED_EDGE('',*,*,#7015,.T.);
#9305=ORIENTED_EDGE('',*,*,#6932,.T.);
#9306=ORIENTED_EDGE('',*,*,#7015,.F.);
#9307=ORIENTED_EDGE('',*,*,#7016,.F.);
#9308=ORIENTED_EDGE('',*,*,#7017,.T.);
#9309=ORIENTED_EDGE('',*,*,#6933,.T.);
#9310=ORIENTED_EDGE('',*,*,#7017,.F.);
#9311=ORIENTED_EDGE('',*,*,#7018,.F.);
#9312=ORIENTED_EDGE('',*,*,#7019,.T.);
#9313=ORIENTED_EDGE('',*,*,#6934,.T.);
#9314=ORIENTED_EDGE('',*,*,#7019,.F.);
#9315=ORIENTED_EDGE('',*,*,#7020,.F.);
#9316=ORIENTED_EDGE('',*,*,#7021,.T.);
#9317=ORIENTED_EDGE('',*,*,#6935,.T.);
#9318=ORIENTED_EDGE('',*,*,#7021,.F.);
#9319=ORIENTED_EDGE('',*,*,#7022,.F.);
#9320=ORIENTED_EDGE('',*,*,#7023,.T.);
#9321=ORIENTED_EDGE('',*,*,#6936,.T.);
#9322=ORIENTED_EDGE('',*,*,#7023,.F.);
#9323=ORIENTED_EDGE('',*,*,#7024,.F.);
#9324=ORIENTED_EDGE('',*,*,#7025,.T.);
#9325=ORIENTED_EDGE('',*,*,#6937,.T.);
#9326=ORIENTED_EDGE('',*,*,#7025,.F.);
#9327=ORIENTED_EDGE('',*,*,#7026,.F.);
#9328=ORIENTED_EDGE('',*,*,#7027,.T.);
#9329=ORIENTED_EDGE('',*,*,#6938,.T.);
#9330=ORIENTED_EDGE('',*,*,#7027,.F.);
#9331=ORIENTED_EDGE('',*,*,#7028,.F.);
#9332=ORIENTED_EDGE('',*,*,#7029,.T.);
#9333=ORIENTED_EDGE('',*,*,#6939,.T.);
#9334=ORIENTED_EDGE('',*,*,#7029,.F.);
#9335=ORIENTED_EDGE('',*,*,#7030,.F.);
#9336=ORIENTED_EDGE('',*,*,#7031,.T.);
#9337=ORIENTED_EDGE('',*,*,#6940,.T.);
#9338=ORIENTED_EDGE('',*,*,#7031,.F.);
#9339=ORIENTED_EDGE('',*,*,#7032,.F.);
#9340=ORIENTED_EDGE('',*,*,#7033,.T.);
#9341=ORIENTED_EDGE('',*,*,#6941,.T.);
#9342=ORIENTED_EDGE('',*,*,#7033,.F.);
#9343=ORIENTED_EDGE('',*,*,#7034,.F.);
#9344=ORIENTED_EDGE('',*,*,#7035,.T.);
#9345=ORIENTED_EDGE('',*,*,#6942,.T.);
#9346=ORIENTED_EDGE('',*,*,#7035,.F.);
#9347=ORIENTED_EDGE('',*,*,#7036,.F.);
#9348=ORIENTED_EDGE('',*,*,#7037,.T.);
#9349=ORIENTED_EDGE('',*,*,#6943,.T.);
#9350=ORIENTED_EDGE('',*,*,#7037,.F.);
#9351=ORIENTED_EDGE('',*,*,#7038,.F.);
#9352=ORIENTED_EDGE('',*,*,#7039,.T.);
#9353=ORIENTED_EDGE('',*,*,#6944,.T.);
#9354=ORIENTED_EDGE('',*,*,#7039,.F.);
#9355=ORIENTED_EDGE('',*,*,#7040,.F.);
#9356=ORIENTED_EDGE('',*,*,#7041,.T.);
#9357=ORIENTED_EDGE('',*,*,#6945,.T.);
#9358=ORIENTED_EDGE('',*,*,#7041,.F.);
#9359=ORIENTED_EDGE('',*,*,#7042,.F.);
#9360=ORIENTED_EDGE('',*,*,#7043,.T.);
#9361=ORIENTED_EDGE('',*,*,#6946,.T.);
#9362=ORIENTED_EDGE('',*,*,#7043,.F.);
#9363=ORIENTED_EDGE('',*,*,#7044,.F.);
#9364=ORIENTED_EDGE('',*,*,#7045,.T.);
#9365=ORIENTED_EDGE('',*,*,#6947,.T.);
#9366=ORIENTED_EDGE('',*,*,#7045,.F.);
#9367=ORIENTED_EDGE('',*,*,#7046,.F.);
#9368=ORIENTED_EDGE('',*,*,#7047,.T.);
#9369=ORIENTED_EDGE('',*,*,#6948,.T.);
#9370=ORIENTED_EDGE('',*,*,#7047,.F.);
#9371=ORIENTED_EDGE('',*,*,#7048,.F.);
#9372=ORIENTED_EDGE('',*,*,#7049,.T.);
#9373=ORIENTED_EDGE('',*,*,#6949,.T.);
#9374=ORIENTED_EDGE('',*,*,#7049,.F.);
#9375=ORIENTED_EDGE('',*,*,#7050,.F.);
#9376=ORIENTED_EDGE('',*,*,#7051,.T.);
#9377=ORIENTED_EDGE('',*,*,#6950,.T.);
#9378=ORIENTED_EDGE('',*,*,#7051,.F.);
#9379=ORIENTED_EDGE('',*,*,#7052,.F.);
#9380=ORIENTED_EDGE('',*,*,#7053,.T.);
#9381=ORIENTED_EDGE('',*,*,#6951,.T.);
#9382=ORIENTED_EDGE('',*,*,#7053,.F.);
#9383=ORIENTED_EDGE('',*,*,#7054,.F.);
#9384=ORIENTED_EDGE('',*,*,#7055,.T.);
#9385=ORIENTED_EDGE('',*,*,#6952,.T.);
#9386=ORIENTED_EDGE('',*,*,#7055,.F.);
#9387=ORIENTED_EDGE('',*,*,#7056,.F.);
#9388=ORIENTED_EDGE('',*,*,#7057,.T.);
#9389=ORIENTED_EDGE('',*,*,#6953,.T.);
#9390=ORIENTED_EDGE('',*,*,#7057,.F.);
#9391=ORIENTED_EDGE('',*,*,#7058,.F.);
#9392=ORIENTED_EDGE('',*,*,#7059,.T.);
#9393=ORIENTED_EDGE('',*,*,#6954,.T.);
#9394=ORIENTED_EDGE('',*,*,#7059,.F.);
#9395=ORIENTED_EDGE('',*,*,#7060,.F.);
#9396=ORIENTED_EDGE('',*,*,#7061,.T.);
#9397=ORIENTED_EDGE('',*,*,#6955,.T.);
#9398=ORIENTED_EDGE('',*,*,#7061,.F.);
#9399=ORIENTED_EDGE('',*,*,#7062,.F.);
#9400=ORIENTED_EDGE('',*,*,#7063,.T.);
#9401=ORIENTED_EDGE('',*,*,#6956,.T.);
#9402=ORIENTED_EDGE('',*,*,#7063,.F.);
#9403=ORIENTED_EDGE('',*,*,#7064,.F.);
#9404=ORIENTED_EDGE('',*,*,#7065,.T.);
#9405=ORIENTED_EDGE('',*,*,#6957,.T.);
#9406=ORIENTED_EDGE('',*,*,#7065,.F.);
#9407=ORIENTED_EDGE('',*,*,#7066,.F.);
#9408=ORIENTED_EDGE('',*,*,#7067,.T.);
#9409=ORIENTED_EDGE('',*,*,#6958,.T.);
#9410=ORIENTED_EDGE('',*,*,#7067,.F.);
#9411=ORIENTED_EDGE('',*,*,#6910,.F.);
#9412=ORIENTED_EDGE('',*,*,#6967,.T.);
#9413=ORIENTED_EDGE('',*,*,#7068,.F.);
#9414=ORIENTED_EDGE('',*,*,#7069,.F.);
#9415=ORIENTED_EDGE('',*,*,#6960,.F.);
#9416=ORIENTED_EDGE('',*,*,#7070,.T.);
#9417=ORIENTED_EDGE('',*,*,#7068,.T.);
#9418=ORIENTED_EDGE('',*,*,#6966,.T.);
#9419=ORIENTED_EDGE('',*,*,#6974,.T.);
#9420=ORIENTED_EDGE('',*,*,#6976,.T.);
#9421=ORIENTED_EDGE('',*,*,#6978,.T.);
#9422=ORIENTED_EDGE('',*,*,#6980,.T.);
#9423=ORIENTED_EDGE('',*,*,#6982,.T.);
#9424=ORIENTED_EDGE('',*,*,#6984,.T.);
#9425=ORIENTED_EDGE('',*,*,#6986,.T.);
#9426=ORIENTED_EDGE('',*,*,#6988,.T.);
#9427=ORIENTED_EDGE('',*,*,#6990,.T.);
#9428=ORIENTED_EDGE('',*,*,#6992,.T.);
#9429=ORIENTED_EDGE('',*,*,#6994,.T.);
#9430=ORIENTED_EDGE('',*,*,#6996,.T.);
#9431=ORIENTED_EDGE('',*,*,#6998,.T.);
#9432=ORIENTED_EDGE('',*,*,#7000,.T.);
#9433=ORIENTED_EDGE('',*,*,#7002,.T.);
#9434=ORIENTED_EDGE('',*,*,#7004,.T.);
#9435=ORIENTED_EDGE('',*,*,#7006,.T.);
#9436=ORIENTED_EDGE('',*,*,#7008,.T.);
#9437=ORIENTED_EDGE('',*,*,#7010,.T.);
#9438=ORIENTED_EDGE('',*,*,#7012,.T.);
#9439=ORIENTED_EDGE('',*,*,#7014,.T.);
#9440=ORIENTED_EDGE('',*,*,#7016,.T.);
#9441=ORIENTED_EDGE('',*,*,#7018,.T.);
#9442=ORIENTED_EDGE('',*,*,#7020,.T.);
#9443=ORIENTED_EDGE('',*,*,#7022,.T.);
#9444=ORIENTED_EDGE('',*,*,#7024,.T.);
#9445=ORIENTED_EDGE('',*,*,#7026,.T.);
#9446=ORIENTED_EDGE('',*,*,#7028,.T.);
#9447=ORIENTED_EDGE('',*,*,#7030,.T.);
#9448=ORIENTED_EDGE('',*,*,#7032,.T.);
#9449=ORIENTED_EDGE('',*,*,#7034,.T.);
#9450=ORIENTED_EDGE('',*,*,#7036,.T.);
#9451=ORIENTED_EDGE('',*,*,#7038,.T.);
#9452=ORIENTED_EDGE('',*,*,#7040,.T.);
#9453=ORIENTED_EDGE('',*,*,#7042,.T.);
#9454=ORIENTED_EDGE('',*,*,#7044,.T.);
#9455=ORIENTED_EDGE('',*,*,#7046,.T.);
#9456=ORIENTED_EDGE('',*,*,#7048,.T.);
#9457=ORIENTED_EDGE('',*,*,#7050,.T.);
#9458=ORIENTED_EDGE('',*,*,#7052,.T.);
#9459=ORIENTED_EDGE('',*,*,#7054,.T.);
#9460=ORIENTED_EDGE('',*,*,#7056,.T.);
#9461=ORIENTED_EDGE('',*,*,#7058,.T.);
#9462=ORIENTED_EDGE('',*,*,#7060,.T.);
#9463=ORIENTED_EDGE('',*,*,#7062,.T.);
#9464=ORIENTED_EDGE('',*,*,#7064,.T.);
#9465=ORIENTED_EDGE('',*,*,#7066,.T.);
#9466=ORIENTED_EDGE('',*,*,#7071,.F.);
#9467=ORIENTED_EDGE('',*,*,#7072,.T.);
#9468=ORIENTED_EDGE('',*,*,#7073,.T.);
#9469=ORIENTED_EDGE('',*,*,#7072,.F.);
#9470=ORIENTED_EDGE('',*,*,#7074,.F.);
#9471=ORIENTED_EDGE('',*,*,#7075,.T.);
#9472=ORIENTED_EDGE('',*,*,#7076,.T.);
#9473=ORIENTED_EDGE('',*,*,#7075,.F.);
#9474=ORIENTED_EDGE('',*,*,#7077,.F.);
#9475=ORIENTED_EDGE('',*,*,#7078,.T.);
#9476=ORIENTED_EDGE('',*,*,#7079,.T.);
#9477=ORIENTED_EDGE('',*,*,#7078,.F.);
#9478=ORIENTED_EDGE('',*,*,#7080,.F.);
#9479=ORIENTED_EDGE('',*,*,#7081,.T.);
#9480=ORIENTED_EDGE('',*,*,#7082,.T.);
#9481=ORIENTED_EDGE('',*,*,#7081,.F.);
#9482=ORIENTED_EDGE('',*,*,#7083,.F.);
#9483=ORIENTED_EDGE('',*,*,#7084,.T.);
#9484=ORIENTED_EDGE('',*,*,#7085,.T.);
#9485=ORIENTED_EDGE('',*,*,#7084,.F.);
#9486=ORIENTED_EDGE('',*,*,#7086,.F.);
#9487=ORIENTED_EDGE('',*,*,#7087,.T.);
#9488=ORIENTED_EDGE('',*,*,#7088,.T.);
#9489=ORIENTED_EDGE('',*,*,#7087,.F.);
#9490=ORIENTED_EDGE('',*,*,#7089,.F.);
#9491=ORIENTED_EDGE('',*,*,#7090,.T.);
#9492=ORIENTED_EDGE('',*,*,#7091,.T.);
#9493=ORIENTED_EDGE('',*,*,#7090,.F.);
#9494=ORIENTED_EDGE('',*,*,#7092,.F.);
#9495=ORIENTED_EDGE('',*,*,#7093,.T.);
#9496=ORIENTED_EDGE('',*,*,#7094,.T.);
#9497=ORIENTED_EDGE('',*,*,#7093,.F.);
#9498=ORIENTED_EDGE('',*,*,#7095,.F.);
#9499=ORIENTED_EDGE('',*,*,#7096,.T.);
#9500=ORIENTED_EDGE('',*,*,#7097,.T.);
#9501=ORIENTED_EDGE('',*,*,#7096,.F.);
#9502=ORIENTED_EDGE('',*,*,#7098,.F.);
#9503=ORIENTED_EDGE('',*,*,#7099,.T.);
#9504=ORIENTED_EDGE('',*,*,#7100,.T.);
#9505=ORIENTED_EDGE('',*,*,#7099,.F.);
#9506=ORIENTED_EDGE('',*,*,#7101,.F.);
#9507=ORIENTED_EDGE('',*,*,#7102,.T.);
#9508=ORIENTED_EDGE('',*,*,#7103,.T.);
#9509=ORIENTED_EDGE('',*,*,#7102,.F.);
#9510=ORIENTED_EDGE('',*,*,#7104,.F.);
#9511=ORIENTED_EDGE('',*,*,#7105,.T.);
#9512=ORIENTED_EDGE('',*,*,#7106,.T.);
#9513=ORIENTED_EDGE('',*,*,#7105,.F.);
#9514=ORIENTED_EDGE('',*,*,#7107,.F.);
#9515=ORIENTED_EDGE('',*,*,#7108,.T.);
#9516=ORIENTED_EDGE('',*,*,#7109,.T.);
#9517=ORIENTED_EDGE('',*,*,#7108,.F.);
#9518=ORIENTED_EDGE('',*,*,#7110,.F.);
#9519=ORIENTED_EDGE('',*,*,#7111,.T.);
#9520=ORIENTED_EDGE('',*,*,#7112,.T.);
#9521=ORIENTED_EDGE('',*,*,#7111,.F.);
#9522=ORIENTED_EDGE('',*,*,#7113,.F.);
#9523=ORIENTED_EDGE('',*,*,#7114,.T.);
#9524=ORIENTED_EDGE('',*,*,#7115,.T.);
#9525=ORIENTED_EDGE('',*,*,#7114,.F.);
#9526=ORIENTED_EDGE('',*,*,#7116,.F.);
#9527=ORIENTED_EDGE('',*,*,#7117,.T.);
#9528=ORIENTED_EDGE('',*,*,#7118,.T.);
#9529=ORIENTED_EDGE('',*,*,#7117,.F.);
#9530=ORIENTED_EDGE('',*,*,#7119,.F.);
#9531=ORIENTED_EDGE('',*,*,#7120,.T.);
#9532=ORIENTED_EDGE('',*,*,#7121,.T.);
#9533=ORIENTED_EDGE('',*,*,#7120,.F.);
#9534=ORIENTED_EDGE('',*,*,#7122,.F.);
#9535=ORIENTED_EDGE('',*,*,#7123,.T.);
#9536=ORIENTED_EDGE('',*,*,#7124,.T.);
#9537=ORIENTED_EDGE('',*,*,#7123,.F.);
#9538=ORIENTED_EDGE('',*,*,#7125,.F.);
#9539=ORIENTED_EDGE('',*,*,#7126,.T.);
#9540=ORIENTED_EDGE('',*,*,#7127,.T.);
#9541=ORIENTED_EDGE('',*,*,#7126,.F.);
#9542=ORIENTED_EDGE('',*,*,#7128,.F.);
#9543=ORIENTED_EDGE('',*,*,#7129,.T.);
#9544=ORIENTED_EDGE('',*,*,#7130,.T.);
#9545=ORIENTED_EDGE('',*,*,#7129,.F.);
#9546=ORIENTED_EDGE('',*,*,#7131,.F.);
#9547=ORIENTED_EDGE('',*,*,#7132,.T.);
#9548=ORIENTED_EDGE('',*,*,#7133,.T.);
#9549=ORIENTED_EDGE('',*,*,#7132,.F.);
#9550=ORIENTED_EDGE('',*,*,#7134,.F.);
#9551=ORIENTED_EDGE('',*,*,#7135,.T.);
#9552=ORIENTED_EDGE('',*,*,#7136,.T.);
#9553=ORIENTED_EDGE('',*,*,#7135,.F.);
#9554=ORIENTED_EDGE('',*,*,#7137,.F.);
#9555=ORIENTED_EDGE('',*,*,#7138,.T.);
#9556=ORIENTED_EDGE('',*,*,#7139,.T.);
#9557=ORIENTED_EDGE('',*,*,#7138,.F.);
#9558=ORIENTED_EDGE('',*,*,#7140,.F.);
#9559=ORIENTED_EDGE('',*,*,#7141,.T.);
#9560=ORIENTED_EDGE('',*,*,#7142,.T.);
#9561=ORIENTED_EDGE('',*,*,#7141,.F.);
#9562=ORIENTED_EDGE('',*,*,#7143,.F.);
#9563=ORIENTED_EDGE('',*,*,#7144,.T.);
#9564=ORIENTED_EDGE('',*,*,#7145,.T.);
#9565=ORIENTED_EDGE('',*,*,#7144,.F.);
#9566=ORIENTED_EDGE('',*,*,#7146,.F.);
#9567=ORIENTED_EDGE('',*,*,#7147,.T.);
#9568=ORIENTED_EDGE('',*,*,#7148,.T.);
#9569=ORIENTED_EDGE('',*,*,#7147,.F.);
#9570=ORIENTED_EDGE('',*,*,#7149,.F.);
#9571=ORIENTED_EDGE('',*,*,#7150,.T.);
#9572=ORIENTED_EDGE('',*,*,#7151,.T.);
#9573=ORIENTED_EDGE('',*,*,#7150,.F.);
#9574=ORIENTED_EDGE('',*,*,#7152,.F.);
#9575=ORIENTED_EDGE('',*,*,#7153,.T.);
#9576=ORIENTED_EDGE('',*,*,#7154,.T.);
#9577=ORIENTED_EDGE('',*,*,#7153,.F.);
#9578=ORIENTED_EDGE('',*,*,#7155,.F.);
#9579=ORIENTED_EDGE('',*,*,#7156,.T.);
#9580=ORIENTED_EDGE('',*,*,#7157,.T.);
#9581=ORIENTED_EDGE('',*,*,#7156,.F.);
#9582=ORIENTED_EDGE('',*,*,#7158,.F.);
#9583=ORIENTED_EDGE('',*,*,#7159,.T.);
#9584=ORIENTED_EDGE('',*,*,#7160,.T.);
#9585=ORIENTED_EDGE('',*,*,#7159,.F.);
#9586=ORIENTED_EDGE('',*,*,#7161,.F.);
#9587=ORIENTED_EDGE('',*,*,#7162,.T.);
#9588=ORIENTED_EDGE('',*,*,#7163,.T.);
#9589=ORIENTED_EDGE('',*,*,#7162,.F.);
#9590=ORIENTED_EDGE('',*,*,#7164,.F.);
#9591=ORIENTED_EDGE('',*,*,#7165,.T.);
#9592=ORIENTED_EDGE('',*,*,#7166,.T.);
#9593=ORIENTED_EDGE('',*,*,#7165,.F.);
#9594=ORIENTED_EDGE('',*,*,#7167,.F.);
#9595=ORIENTED_EDGE('',*,*,#7168,.T.);
#9596=ORIENTED_EDGE('',*,*,#7169,.T.);
#9597=ORIENTED_EDGE('',*,*,#7168,.F.);
#9598=ORIENTED_EDGE('',*,*,#7170,.F.);
#9599=ORIENTED_EDGE('',*,*,#7171,.T.);
#9600=ORIENTED_EDGE('',*,*,#7172,.T.);
#9601=ORIENTED_EDGE('',*,*,#7171,.F.);
#9602=ORIENTED_EDGE('',*,*,#7173,.F.);
#9603=ORIENTED_EDGE('',*,*,#7174,.T.);
#9604=ORIENTED_EDGE('',*,*,#7175,.T.);
#9605=ORIENTED_EDGE('',*,*,#7174,.F.);
#9606=ORIENTED_EDGE('',*,*,#7176,.F.);
#9607=ORIENTED_EDGE('',*,*,#7177,.T.);
#9608=ORIENTED_EDGE('',*,*,#7178,.T.);
#9609=ORIENTED_EDGE('',*,*,#7177,.F.);
#9610=ORIENTED_EDGE('',*,*,#7179,.F.);
#9611=ORIENTED_EDGE('',*,*,#7180,.T.);
#9612=ORIENTED_EDGE('',*,*,#7181,.T.);
#9613=ORIENTED_EDGE('',*,*,#7180,.F.);
#9614=ORIENTED_EDGE('',*,*,#7182,.F.);
#9615=ORIENTED_EDGE('',*,*,#7183,.T.);
#9616=ORIENTED_EDGE('',*,*,#7184,.T.);
#9617=ORIENTED_EDGE('',*,*,#7183,.F.);
#9618=ORIENTED_EDGE('',*,*,#7185,.F.);
#9619=ORIENTED_EDGE('',*,*,#7186,.T.);
#9620=ORIENTED_EDGE('',*,*,#7187,.T.);
#9621=ORIENTED_EDGE('',*,*,#7186,.F.);
#9622=ORIENTED_EDGE('',*,*,#7188,.F.);
#9623=ORIENTED_EDGE('',*,*,#7189,.T.);
#9624=ORIENTED_EDGE('',*,*,#7190,.T.);
#9625=ORIENTED_EDGE('',*,*,#7189,.F.);
#9626=ORIENTED_EDGE('',*,*,#7191,.F.);
#9627=ORIENTED_EDGE('',*,*,#7192,.T.);
#9628=ORIENTED_EDGE('',*,*,#7193,.T.);
#9629=ORIENTED_EDGE('',*,*,#7192,.F.);
#9630=ORIENTED_EDGE('',*,*,#7194,.F.);
#9631=ORIENTED_EDGE('',*,*,#7195,.T.);
#9632=ORIENTED_EDGE('',*,*,#7196,.T.);
#9633=ORIENTED_EDGE('',*,*,#7195,.F.);
#9634=ORIENTED_EDGE('',*,*,#7197,.F.);
#9635=ORIENTED_EDGE('',*,*,#7198,.T.);
#9636=ORIENTED_EDGE('',*,*,#7199,.T.);
#9637=ORIENTED_EDGE('',*,*,#7198,.F.);
#9638=ORIENTED_EDGE('',*,*,#7200,.F.);
#9639=ORIENTED_EDGE('',*,*,#7201,.T.);
#9640=ORIENTED_EDGE('',*,*,#7202,.T.);
#9641=ORIENTED_EDGE('',*,*,#7201,.F.);
#9642=ORIENTED_EDGE('',*,*,#7203,.F.);
#9643=ORIENTED_EDGE('',*,*,#7204,.T.);
#9644=ORIENTED_EDGE('',*,*,#7205,.T.);
#9645=ORIENTED_EDGE('',*,*,#7204,.F.);
#9646=ORIENTED_EDGE('',*,*,#7206,.F.);
#9647=ORIENTED_EDGE('',*,*,#7207,.T.);
#9648=ORIENTED_EDGE('',*,*,#7208,.T.);
#9649=ORIENTED_EDGE('',*,*,#7207,.F.);
#9650=ORIENTED_EDGE('',*,*,#7209,.F.);
#9651=ORIENTED_EDGE('',*,*,#7210,.T.);
#9652=ORIENTED_EDGE('',*,*,#7211,.T.);
#9653=ORIENTED_EDGE('',*,*,#7210,.F.);
#9654=ORIENTED_EDGE('',*,*,#7212,.F.);
#9655=ORIENTED_EDGE('',*,*,#6969,.T.);
#9656=ORIENTED_EDGE('',*,*,#7213,.F.);
#9657=ORIENTED_EDGE('',*,*,#7214,.F.);
#9658=ORIENTED_EDGE('',*,*,#6959,.F.);
#9659=ORIENTED_EDGE('',*,*,#6965,.F.);
#9660=ORIENTED_EDGE('',*,*,#6972,.F.);
#9661=ORIENTED_EDGE('',*,*,#7215,.F.);
#9662=ORIENTED_EDGE('',*,*,#7214,.T.);
#9663=ORIENTED_EDGE('',*,*,#7216,.F.);
#9664=ORIENTED_EDGE('',*,*,#6901,.F.);
#9665=ORIENTED_EDGE('',*,*,#6905,.T.);
#9666=ORIENTED_EDGE('',*,*,#6908,.F.);
#9667=ORIENTED_EDGE('',*,*,#6911,.F.);
#9668=ORIENTED_EDGE('',*,*,#7069,.T.);
#9669=ORIENTED_EDGE('',*,*,#7070,.F.);
#9670=ORIENTED_EDGE('',*,*,#6902,.F.);
#9671=ORIENTED_EDGE('',*,*,#7216,.T.);
#9672=ORIENTED_EDGE('',*,*,#7213,.T.);
#9673=ORIENTED_EDGE('',*,*,#6968,.T.);
#9674=ORIENTED_EDGE('',*,*,#7209,.T.);
#9675=ORIENTED_EDGE('',*,*,#7206,.T.);
#9676=ORIENTED_EDGE('',*,*,#7203,.T.);
#9677=ORIENTED_EDGE('',*,*,#7200,.T.);
#9678=ORIENTED_EDGE('',*,*,#7197,.T.);
#9679=ORIENTED_EDGE('',*,*,#7194,.T.);
#9680=ORIENTED_EDGE('',*,*,#7191,.T.);
#9681=ORIENTED_EDGE('',*,*,#7188,.T.);
#9682=ORIENTED_EDGE('',*,*,#7185,.T.);
#9683=ORIENTED_EDGE('',*,*,#7182,.T.);
#9684=ORIENTED_EDGE('',*,*,#7179,.T.);
#9685=ORIENTED_EDGE('',*,*,#7176,.T.);
#9686=ORIENTED_EDGE('',*,*,#7173,.T.);
#9687=ORIENTED_EDGE('',*,*,#7170,.T.);
#9688=ORIENTED_EDGE('',*,*,#7167,.T.);
#9689=ORIENTED_EDGE('',*,*,#7164,.T.);
#9690=ORIENTED_EDGE('',*,*,#7161,.T.);
#9691=ORIENTED_EDGE('',*,*,#7158,.T.);
#9692=ORIENTED_EDGE('',*,*,#7155,.T.);
#9693=ORIENTED_EDGE('',*,*,#7152,.T.);
#9694=ORIENTED_EDGE('',*,*,#7149,.T.);
#9695=ORIENTED_EDGE('',*,*,#7146,.T.);
#9696=ORIENTED_EDGE('',*,*,#7143,.T.);
#9697=ORIENTED_EDGE('',*,*,#7140,.T.);
#9698=ORIENTED_EDGE('',*,*,#7137,.T.);
#9699=ORIENTED_EDGE('',*,*,#7134,.T.);
#9700=ORIENTED_EDGE('',*,*,#7131,.T.);
#9701=ORIENTED_EDGE('',*,*,#7128,.T.);
#9702=ORIENTED_EDGE('',*,*,#7125,.T.);
#9703=ORIENTED_EDGE('',*,*,#7122,.T.);
#9704=ORIENTED_EDGE('',*,*,#7119,.T.);
#9705=ORIENTED_EDGE('',*,*,#7116,.T.);
#9706=ORIENTED_EDGE('',*,*,#7113,.T.);
#9707=ORIENTED_EDGE('',*,*,#7110,.T.);
#9708=ORIENTED_EDGE('',*,*,#7107,.T.);
#9709=ORIENTED_EDGE('',*,*,#7104,.T.);
#9710=ORIENTED_EDGE('',*,*,#7101,.T.);
#9711=ORIENTED_EDGE('',*,*,#7098,.T.);
#9712=ORIENTED_EDGE('',*,*,#7095,.T.);
#9713=ORIENTED_EDGE('',*,*,#7092,.T.);
#9714=ORIENTED_EDGE('',*,*,#7089,.T.);
#9715=ORIENTED_EDGE('',*,*,#7086,.T.);
#9716=ORIENTED_EDGE('',*,*,#7083,.T.);
#9717=ORIENTED_EDGE('',*,*,#7080,.T.);
#9718=ORIENTED_EDGE('',*,*,#7077,.T.);
#9719=ORIENTED_EDGE('',*,*,#7074,.T.);
#9720=ORIENTED_EDGE('',*,*,#7071,.T.);
#9721=ORIENTED_EDGE('',*,*,#6973,.F.);
#9722=ORIENTED_EDGE('',*,*,#6970,.T.);
#9723=ORIENTED_EDGE('',*,*,#7212,.T.);
#9724=ORIENTED_EDGE('',*,*,#7215,.T.);
#9725=ORIENTED_EDGE('',*,*,#7211,.F.);
#9726=ORIENTED_EDGE('',*,*,#7208,.F.);
#9727=ORIENTED_EDGE('',*,*,#7205,.F.);
#9728=ORIENTED_EDGE('',*,*,#7202,.F.);
#9729=ORIENTED_EDGE('',*,*,#7199,.F.);
#9730=ORIENTED_EDGE('',*,*,#7196,.F.);
#9731=ORIENTED_EDGE('',*,*,#7193,.F.);
#9732=ORIENTED_EDGE('',*,*,#7190,.F.);
#9733=ORIENTED_EDGE('',*,*,#7187,.F.);
#9734=ORIENTED_EDGE('',*,*,#7184,.F.);
#9735=ORIENTED_EDGE('',*,*,#7181,.F.);
#9736=ORIENTED_EDGE('',*,*,#7178,.F.);
#9737=ORIENTED_EDGE('',*,*,#7175,.F.);
#9738=ORIENTED_EDGE('',*,*,#7172,.F.);
#9739=ORIENTED_EDGE('',*,*,#7169,.F.);
#9740=ORIENTED_EDGE('',*,*,#7166,.F.);
#9741=ORIENTED_EDGE('',*,*,#7163,.F.);
#9742=ORIENTED_EDGE('',*,*,#7160,.F.);
#9743=ORIENTED_EDGE('',*,*,#7157,.F.);
#9744=ORIENTED_EDGE('',*,*,#7154,.F.);
#9745=ORIENTED_EDGE('',*,*,#7151,.F.);
#9746=ORIENTED_EDGE('',*,*,#7148,.F.);
#9747=ORIENTED_EDGE('',*,*,#7145,.F.);
#9748=ORIENTED_EDGE('',*,*,#7142,.F.);
#9749=ORIENTED_EDGE('',*,*,#7139,.F.);
#9750=ORIENTED_EDGE('',*,*,#7136,.F.);
#9751=ORIENTED_EDGE('',*,*,#7133,.F.);
#9752=ORIENTED_EDGE('',*,*,#7130,.F.);
#9753=ORIENTED_EDGE('',*,*,#7127,.F.);
#9754=ORIENTED_EDGE('',*,*,#7124,.F.);
#9755=ORIENTED_EDGE('',*,*,#7121,.F.);
#9756=ORIENTED_EDGE('',*,*,#7118,.F.);
#9757=ORIENTED_EDGE('',*,*,#7115,.F.);
#9758=ORIENTED_EDGE('',*,*,#7112,.F.);
#9759=ORIENTED_EDGE('',*,*,#7109,.F.);
#9760=ORIENTED_EDGE('',*,*,#7106,.F.);
#9761=ORIENTED_EDGE('',*,*,#7103,.F.);
#9762=ORIENTED_EDGE('',*,*,#7100,.F.);
#9763=ORIENTED_EDGE('',*,*,#7097,.F.);
#9764=ORIENTED_EDGE('',*,*,#7094,.F.);
#9765=ORIENTED_EDGE('',*,*,#7091,.F.);
#9766=ORIENTED_EDGE('',*,*,#7088,.F.);
#9767=ORIENTED_EDGE('',*,*,#7085,.F.);
#9768=ORIENTED_EDGE('',*,*,#7082,.F.);
#9769=ORIENTED_EDGE('',*,*,#7079,.F.);
#9770=ORIENTED_EDGE('',*,*,#7076,.F.);
#9771=ORIENTED_EDGE('',*,*,#7073,.F.);
#10894=ADVANCED_FACE('',(#3018),#2613,.F.);
#10895=ADVANCED_FACE('',(#3019),#2614,.F.);
#10896=ADVANCED_FACE('',(#3020),#2615,.F.);
#10897=ADVANCED_FACE('',(#3021),#2616,.F.);
#10898=ADVANCED_FACE('',(#3022),#2617,.F.);
#10899=ADVANCED_FACE('',(#3023),#682,.F.);
#10900=ADVANCED_FACE('',(#3024),#2618,.F.);
#10901=ADVANCED_FACE('',(#3025),#683,.F.);
#10902=ADVANCED_FACE('',(#3026),#2619,.F.);
#10903=ADVANCED_FACE('',(#3027),#684,.F.);
#10904=ADVANCED_FACE('',(#3028),#2620,.F.);
#10905=ADVANCED_FACE('',(#3029),#685,.F.);
#10906=ADVANCED_FACE('',(#3030),#2621,.F.);
#10907=ADVANCED_FACE('',(#3031),#2622,.F.);
#10908=ADVANCED_FACE('',(#3032),#2623,.F.);
#10909=ADVANCED_FACE('',(#3033),#2624,.F.);
#10910=ADVANCED_FACE('',(#3034),#2625,.F.);
#10911=ADVANCED_FACE('',(#3035),#2626,.F.);
#10912=ADVANCED_FACE('',(#3036),#686,.F.);
#10913=ADVANCED_FACE('',(#3037),#2627,.F.);
#10914=ADVANCED_FACE('',(#3038),#687,.F.);
#10915=ADVANCED_FACE('',(#3039),#2628,.F.);
#10916=ADVANCED_FACE('',(#3040),#688,.F.);
#10917=ADVANCED_FACE('',(#3041),#2629,.F.);
#10918=ADVANCED_FACE('',(#3042),#689,.F.);
#10919=ADVANCED_FACE('',(#3043),#2630,.F.);
#10920=ADVANCED_FACE('',(#3044),#2631,.F.);
#10921=ADVANCED_FACE('',(#3045),#2632,.F.);
#10922=ADVANCED_FACE('',(#3046),#2633,.F.);
#10923=ADVANCED_FACE('',(#3047),#2634,.F.);
#10924=ADVANCED_FACE('',(#3048),#2635,.F.);
#10925=ADVANCED_FACE('',(#3049),#690,.F.);
#10926=ADVANCED_FACE('',(#3050),#2636,.F.);
#10927=ADVANCED_FACE('',(#3051),#691,.F.);
#10928=ADVANCED_FACE('',(#3052),#2637,.F.);
#10929=ADVANCED_FACE('',(#3053),#692,.F.);
#10930=ADVANCED_FACE('',(#3054),#2638,.F.);
#10931=ADVANCED_FACE('',(#3055),#693,.F.);
#10932=ADVANCED_FACE('',(#3056),#2639,.F.);
#10933=ADVANCED_FACE('',(#3057),#2640,.F.);
#10934=ADVANCED_FACE('',(#3058),#2641,.F.);
#10935=ADVANCED_FACE('',(#3059),#2642,.F.);
#10936=ADVANCED_FACE('',(#3060),#2643,.F.);
#10937=ADVANCED_FACE('',(#3061),#2644,.F.);
#10938=ADVANCED_FACE('',(#3062),#694,.F.);
#10939=ADVANCED_FACE('',(#3063),#2645,.F.);
#10940=ADVANCED_FACE('',(#3064),#695,.F.);
#10941=ADVANCED_FACE('',(#3065),#2646,.F.);
#10942=ADVANCED_FACE('',(#3066),#696,.F.);
#10943=ADVANCED_FACE('',(#3067),#2647,.F.);
#10944=ADVANCED_FACE('',(#3068),#697,.F.);
#10945=ADVANCED_FACE('',(#3069),#2648,.F.);
#10946=ADVANCED_FACE('',(#3070),#2649,.F.);
#10947=ADVANCED_FACE('',(#3071),#2650,.F.);
#10948=ADVANCED_FACE('',(#3072),#2651,.F.);
#10949=ADVANCED_FACE('',(#3073),#2652,.F.);
#10950=ADVANCED_FACE('',(#3074),#2653,.F.);
#10951=ADVANCED_FACE('',(#3075),#698,.F.);
#10952=ADVANCED_FACE('',(#3076),#2654,.F.);
#10953=ADVANCED_FACE('',(#3077),#699,.F.);
#10954=ADVANCED_FACE('',(#3078),#2655,.F.);
#10955=ADVANCED_FACE('',(#3079),#700,.F.);
#10956=ADVANCED_FACE('',(#3080),#2656,.F.);
#10957=ADVANCED_FACE('',(#3081),#701,.F.);
#10958=ADVANCED_FACE('',(#3082),#2657,.F.);
#10959=ADVANCED_FACE('',(#3083),#2658,.F.);
#10960=ADVANCED_FACE('',(#3084),#2659,.F.);
#10961=ADVANCED_FACE('',(#3085),#2660,.F.);
#10962=ADVANCED_FACE('',(#3086),#2661,.F.);
#10963=ADVANCED_FACE('',(#3087),#2662,.F.);
#10964=ADVANCED_FACE('',(#3088),#702,.F.);
#10965=ADVANCED_FACE('',(#3089),#2663,.F.);
#10966=ADVANCED_FACE('',(#3090),#703,.F.);
#10967=ADVANCED_FACE('',(#3091),#2664,.F.);
#10968=ADVANCED_FACE('',(#3092),#704,.F.);
#10969=ADVANCED_FACE('',(#3093),#2665,.F.);
#10970=ADVANCED_FACE('',(#3094),#705,.F.);
#10971=ADVANCED_FACE('',(#3095),#2666,.F.);
#10972=ADVANCED_FACE('',(#3096),#2667,.F.);
#10973=ADVANCED_FACE('',(#3097),#2668,.F.);
#10974=ADVANCED_FACE('',(#3098),#2669,.F.);
#10975=ADVANCED_FACE('',(#3099),#2670,.F.);
#10976=ADVANCED_FACE('',(#3100),#2671,.F.);
#10977=ADVANCED_FACE('',(#3101),#706,.F.);
#10978=ADVANCED_FACE('',(#3102),#2672,.F.);
#10979=ADVANCED_FACE('',(#3103),#707,.F.);
#10980=ADVANCED_FACE('',(#3104),#2673,.F.);
#10981=ADVANCED_FACE('',(#3105),#708,.F.);
#10982=ADVANCED_FACE('',(#3106),#2674,.F.);
#10983=ADVANCED_FACE('',(#3107),#709,.F.);
#10984=ADVANCED_FACE('',(#3108),#2675,.F.);
#10985=ADVANCED_FACE('',(#3109),#2676,.F.);
#10986=ADVANCED_FACE('',(#3110),#2677,.F.);
#10987=ADVANCED_FACE('',(#3111),#2678,.F.);
#10988=ADVANCED_FACE('',(#3112),#2679,.F.);
#10989=ADVANCED_FACE('',(#3113),#2680,.F.);
#10990=ADVANCED_FACE('',(#3114),#710,.F.);
#10991=ADVANCED_FACE('',(#3115),#2681,.F.);
#10992=ADVANCED_FACE('',(#3116),#711,.F.);
#10993=ADVANCED_FACE('',(#3117),#2682,.F.);
#10994=ADVANCED_FACE('',(#3118),#712,.F.);
#10995=ADVANCED_FACE('',(#3119),#2683,.F.);
#10996=ADVANCED_FACE('',(#3120),#713,.F.);
#10997=ADVANCED_FACE('',(#3121),#2684,.F.);
#10998=ADVANCED_FACE('',(#3122),#2685,.F.);
#10999=ADVANCED_FACE('',(#3123),#2686,.F.);
#11000=ADVANCED_FACE('',(#3124),#2687,.F.);
#11001=ADVANCED_FACE('',(#3125),#2688,.F.);
#11002=ADVANCED_FACE('',(#3126),#2689,.F.);
#11003=ADVANCED_FACE('',(#3127),#714,.F.);
#11004=ADVANCED_FACE('',(#3128),#2690,.F.);
#11005=ADVANCED_FACE('',(#3129),#715,.F.);
#11006=ADVANCED_FACE('',(#3130),#2691,.F.);
#11007=ADVANCED_FACE('',(#3131),#716,.F.);
#11008=ADVANCED_FACE('',(#3132),#2692,.F.);
#11009=ADVANCED_FACE('',(#3133),#717,.F.);
#11010=ADVANCED_FACE('',(#3134),#2693,.F.);
#11011=ADVANCED_FACE('',(#3135),#2694,.F.);
#11012=ADVANCED_FACE('',(#3136),#2695,.F.);
#11013=ADVANCED_FACE('',(#3137),#718,.F.);
#11014=ADVANCED_FACE('',(#3138),#2696,.F.);
#11015=ADVANCED_FACE('',(#3139),#719,.F.);
#11016=ADVANCED_FACE('',(#3140),#2697,.F.);
#11017=ADVANCED_FACE('',(#3141),#720,.F.);
#11018=ADVANCED_FACE('',(#3142),#2698,.F.);
#11019=ADVANCED_FACE('',(#3143),#721,.F.);
#11020=ADVANCED_FACE('',(#3144),#2699,.F.);
#11021=ADVANCED_FACE('',(#3145),#2700,.F.);
#11022=ADVANCED_FACE('',(#3146),#2701,.F.);
#11023=ADVANCED_FACE('',(#3147),#2702,.F.);
#11024=ADVANCED_FACE('',(#3148),#2703,.F.);
#11025=ADVANCED_FACE('',(#3149,#187,#188,#189,#190,#191,#192,#193,#194,
#195,#196,#197,#198,#199,#200,#201,#202,#203,#204,#205,#206,#207,#208,#209,
#210,#211,#212,#213,#214,#215,#216,#217,#218,#219,#220,#221,#222,#223,#224,
#225,#226,#227,#228,#229,#230,#231,#232,#233,#234,#235,#236,#237,#238,#239,
#240,#241,#242,#243,#244,#245,#246,#247,#248,#249,#250,#251,#252,#253,#254,
#255,#256),#722,.T.);
#11026=ADVANCED_FACE('',(#3150),#2704,.F.);
#11027=ADVANCED_FACE('',(#3151,#257,#258,#259,#260,#261,#262,#263,#264,
#265,#266,#267,#268,#269,#270,#271,#272,#273,#274,#275,#276,#277,#278,#279,
#280,#281,#282,#283,#284,#285,#286,#287,#288,#289,#290,#291,#292,#293,#294,
#295,#296,#297,#298,#299,#300,#301,#302,#303),#723,.F.);
#11028=ADVANCED_FACE('',(#3152),#2705,.T.);
#11029=ADVANCED_FACE('',(#3153,#304,#305,#306,#307,#308,#309,#310,#311,
#312,#313,#314,#315,#316,#317,#318,#319,#320,#321,#322,#323,#324,#325,#326,
#327,#328,#329,#330,#331,#332,#333,#334,#335,#336,#337,#338,#339,#340,#341,
#342,#343,#344,#345,#346,#347,#348,#349,#350,#351,#352,#353,#354,#355,#356,
#357,#358,#359,#360,#361,#362,#363,#364,#365,#366,#367,#368,#369,#370,#371,
#372,#373),#724,.T.);
#11030=ADVANCED_FACE('',(#3154),#725,.T.);
#11031=ADVANCED_FACE('',(#3155),#2706,.T.);
#11032=ADVANCED_FACE('',(#3156),#2707,.F.);
#11033=ADVANCED_FACE('',(#3157),#2708,.F.);
#11034=ADVANCED_FACE('',(#3158),#2709,.F.);
#11035=ADVANCED_FACE('',(#3159),#2710,.F.);
#11036=ADVANCED_FACE('',(#3160),#2711,.F.);
#11037=ADVANCED_FACE('',(#3161),#2712,.F.);
#11038=ADVANCED_FACE('',(#3162),#2713,.F.);
#11039=ADVANCED_FACE('',(#3163),#2714,.F.);
#11040=ADVANCED_FACE('',(#3164),#2715,.F.);
#11041=ADVANCED_FACE('',(#3165),#2716,.F.);
#11042=ADVANCED_FACE('',(#3166),#2717,.F.);
#11043=ADVANCED_FACE('',(#3167),#2718,.F.);
#11044=ADVANCED_FACE('',(#3168),#2719,.F.);
#11045=ADVANCED_FACE('',(#3169),#2720,.F.);
#11046=ADVANCED_FACE('',(#3170),#2721,.F.);
#11047=ADVANCED_FACE('',(#3171),#2722,.F.);
#11048=ADVANCED_FACE('',(#3172),#2723,.F.);
#11049=ADVANCED_FACE('',(#3173),#2724,.F.);
#11050=ADVANCED_FACE('',(#3174),#2725,.F.);
#11051=ADVANCED_FACE('',(#3175),#2726,.F.);
#11052=ADVANCED_FACE('',(#3176),#2727,.F.);
#11053=ADVANCED_FACE('',(#3177),#2728,.F.);
#11054=ADVANCED_FACE('',(#3178),#2729,.F.);
#11055=ADVANCED_FACE('',(#3179),#2730,.F.);
#11056=ADVANCED_FACE('',(#3180),#2731,.F.);
#11057=ADVANCED_FACE('',(#3181),#2732,.F.);
#11058=ADVANCED_FACE('',(#3182),#2733,.F.);
#11059=ADVANCED_FACE('',(#3183),#2734,.F.);
#11060=ADVANCED_FACE('',(#3184),#2735,.F.);
#11061=ADVANCED_FACE('',(#3185),#2736,.F.);
#11062=ADVANCED_FACE('',(#3186),#2737,.F.);
#11063=ADVANCED_FACE('',(#3187),#2738,.F.);
#11064=ADVANCED_FACE('',(#3188),#2739,.F.);
#11065=ADVANCED_FACE('',(#3189),#2740,.F.);
#11066=ADVANCED_FACE('',(#3190),#2741,.F.);
#11067=ADVANCED_FACE('',(#3191),#2742,.F.);
#11068=ADVANCED_FACE('',(#3192),#2743,.F.);
#11069=ADVANCED_FACE('',(#3193),#2744,.F.);
#11070=ADVANCED_FACE('',(#3194),#2745,.F.);
#11071=ADVANCED_FACE('',(#3195),#2746,.F.);
#11072=ADVANCED_FACE('',(#3196),#2747,.F.);
#11073=ADVANCED_FACE('',(#3197),#2748,.F.);
#11074=ADVANCED_FACE('',(#3198),#2749,.F.);
#11075=ADVANCED_FACE('',(#3199),#2750,.F.);
#11076=ADVANCED_FACE('',(#3200),#2751,.F.);
#11077=ADVANCED_FACE('',(#3201),#2752,.F.);
#11078=ADVANCED_FACE('',(#3202),#2753,.F.);
#11079=ADVANCED_FACE('',(#3203),#726,.T.);
#11080=ADVANCED_FACE('',(#3204,#374,#375,#376,#377,#378,#379,#380,#381,
#382,#383,#384,#385,#386,#387,#388,#389,#390,#391,#392,#393,#394,#395,#396,
#397,#398,#399,#400,#401,#402,#403,#404,#405,#406,#407,#408,#409,#410,#411,
#412,#413,#414,#415,#416,#417,#418,#419,#420),#727,.T.);
#11081=ADVANCED_FACE('',(#3205),#2754,.F.);
#11082=ADVANCED_FACE('',(#3206),#2755,.F.);
#11083=ADVANCED_FACE('',(#3207),#2756,.F.);
#11084=ADVANCED_FACE('',(#3208),#2757,.F.);
#11085=ADVANCED_FACE('',(#3209),#2758,.F.);
#11086=ADVANCED_FACE('',(#3210),#2759,.F.);
#11087=ADVANCED_FACE('',(#3211),#2760,.F.);
#11088=ADVANCED_FACE('',(#3212),#2761,.F.);
#11089=ADVANCED_FACE('',(#3213),#2762,.F.);
#11090=ADVANCED_FACE('',(#3214),#2763,.F.);
#11091=ADVANCED_FACE('',(#3215),#2764,.F.);
#11092=ADVANCED_FACE('',(#3216),#2765,.F.);
#11093=ADVANCED_FACE('',(#3217),#2766,.F.);
#11094=ADVANCED_FACE('',(#3218),#2767,.F.);
#11095=ADVANCED_FACE('',(#3219),#2768,.F.);
#11096=ADVANCED_FACE('',(#3220),#2769,.F.);
#11097=ADVANCED_FACE('',(#3221),#2770,.F.);
#11098=ADVANCED_FACE('',(#3222),#2771,.F.);
#11099=ADVANCED_FACE('',(#3223),#2772,.F.);
#11100=ADVANCED_FACE('',(#3224),#2773,.F.);
#11101=ADVANCED_FACE('',(#3225),#2774,.F.);
#11102=ADVANCED_FACE('',(#3226),#2775,.F.);
#11103=ADVANCED_FACE('',(#3227),#2776,.F.);
#11104=ADVANCED_FACE('',(#3228),#2777,.F.);
#11105=ADVANCED_FACE('',(#3229),#2778,.F.);
#11106=ADVANCED_FACE('',(#3230),#2779,.F.);
#11107=ADVANCED_FACE('',(#3231),#2780,.F.);
#11108=ADVANCED_FACE('',(#3232),#2781,.F.);
#11109=ADVANCED_FACE('',(#3233),#2782,.F.);
#11110=ADVANCED_FACE('',(#3234),#2783,.F.);
#11111=ADVANCED_FACE('',(#3235),#2784,.F.);
#11112=ADVANCED_FACE('',(#3236),#2785,.F.);
#11113=ADVANCED_FACE('',(#3237),#2786,.F.);
#11114=ADVANCED_FACE('',(#3238),#2787,.F.);
#11115=ADVANCED_FACE('',(#3239),#2788,.F.);
#11116=ADVANCED_FACE('',(#3240),#2789,.F.);
#11117=ADVANCED_FACE('',(#3241),#2790,.F.);
#11118=ADVANCED_FACE('',(#3242),#2791,.F.);
#11119=ADVANCED_FACE('',(#3243),#2792,.F.);
#11120=ADVANCED_FACE('',(#3244),#2793,.F.);
#11121=ADVANCED_FACE('',(#3245),#2794,.F.);
#11122=ADVANCED_FACE('',(#3246),#2795,.F.);
#11123=ADVANCED_FACE('',(#3247),#2796,.F.);
#11124=ADVANCED_FACE('',(#3248),#2797,.F.);
#11125=ADVANCED_FACE('',(#3249),#2798,.F.);
#11126=ADVANCED_FACE('',(#3250),#2799,.F.);
#11127=ADVANCED_FACE('',(#3251),#2800,.F.);
#11128=ADVANCED_FACE('',(#3252),#728,.T.);
#11129=ADVANCED_FACE('',(#3253),#729,.T.);
#11130=ADVANCED_FACE('',(#3254,#421,#422,#423,#424,#425,#426,#427,#428,
#429,#430,#431,#432,#433,#434,#435,#436,#437,#438,#439,#440,#441,#442,#443,
#444,#445,#446,#447,#448,#449,#450,#451,#452,#453,#454,#455,#456,#457,#458,
#459,#460,#461,#462,#463,#464,#465,#466,#467),#730,.T.);
#11131=ADVANCED_FACE('',(#3255,#468,#469,#470,#471,#472,#473,#474,#475,
#476,#477,#478,#479,#480,#481,#482,#483,#484,#485,#486,#487,#488,#489,#490,
#491,#492,#493,#494,#495,#496,#497,#498,#499,#500,#501,#502,#503,#504,#505,
#506,#507,#508,#509,#510,#511,#512,#513,#514),#731,.F.);
#11319=CLOSED_SHELL('',(#10894,#10895,#10896,#10897,#10898,#10899,#10900,
#10901,#10902,#10903,#10904,#10905,#10906,#10907,#10908,#10909,#10910,#10911,
#10912,#10913,#10914,#10915,#10916,#10917,#10918,#10919,#10920,#10921,#10922,
#10923,#10924,#10925,#10926,#10927,#10928,#10929,#10930,#10931,#10932,#10933,
#10934,#10935,#10936,#10937,#10938,#10939,#10940,#10941,#10942,#10943,#10944,
#10945,#10946,#10947,#10948,#10949,#10950,#10951,#10952,#10953,#10954,#10955,
#10956,#10957,#10958,#10959,#10960,#10961,#10962,#10963,#10964,#10965,#10966,
#10967,#10968,#10969,#10970,#10971,#10972,#10973,#10974,#10975,#10976,#10977,
#10978,#10979,#10980,#10981,#10982,#10983,#10984,#10985,#10986,#10987,#10988,
#10989,#10990,#10991,#10992,#10993,#10994,#10995,#10996,#10997,#10998,#10999,
#11000,#11001,#11002,#11003,#11004,#11005,#11006,#11007,#11008,#11009,#11010,
#11011,#11012,#11013,#11014,#11015,#11016,#11017,#11018,#11019,#11020,#11021,
#11022,#11023,#11024,#11025,#11026,#11027,#11028,#11029,#11030,#11031,#11032,
#11033,#11034,#11035,#11036,#11037,#11038,#11039,#11040,#11041,#11042,#11043,
#11044,#11045,#11046,#11047,#11048,#11049,#11050,#11051,#11052,#11053,#11054,
#11055,#11056,#11057,#11058,#11059,#11060,#11061,#11062,#11063,#11064,#11065,
#11066,#11067,#11068,#11069,#11070,#11071,#11072,#11073,#11074,#11075,#11076,
#11077,#11078,#11079,#11080,#11081,#11082,#11083,#11084,#11085,#11086,#11087,
#11088,#11089,#11090,#11091,#11092,#11093,#11094,#11095,#11096,#11097,#11098,
#11099,#11100,#11101,#11102,#11103,#11104,#11105,#11106,#11107,#11108,#11109,
#11110,#11111,#11112,#11113,#11114,#11115,#11116,#11117,#11118,#11119,#11120,
#11121,#11122,#11123,#11124,#11125,#11126,#11127,#11128,#11129,#11130,#11131));
#11759=AXIS2_PLACEMENT_3D('',#16741,#13458,#13459);
#11760=AXIS2_PLACEMENT_3D('',#16742,#13460,#13461);
#11761=AXIS2_PLACEMENT_3D('',#16744,#13462,#13463);
#11762=AXIS2_PLACEMENT_3D('',#16747,#13465,#13466);
#11763=AXIS2_PLACEMENT_3D('',#16748,#13467,#13468);
#11764=AXIS2_PLACEMENT_3D('',#16750,#13469,#13470);
#11765=AXIS2_PLACEMENT_3D('',#16753,#13472,#13473);
#11766=AXIS2_PLACEMENT_3D('',#16754,#13474,#13475);
#11767=AXIS2_PLACEMENT_3D('',#16756,#13476,#13477);
#11768=AXIS2_PLACEMENT_3D('',#16759,#13479,#13480);
#11769=AXIS2_PLACEMENT_3D('',#16760,#13481,#13482);
#11770=AXIS2_PLACEMENT_3D('',#16762,#13483,#13484);
#11771=AXIS2_PLACEMENT_3D('',#16765,#13486,#13487);
#11772=AXIS2_PLACEMENT_3D('',#16766,#13488,#13489);
#11773=AXIS2_PLACEMENT_3D('',#16768,#13490,#13491);
#11774=AXIS2_PLACEMENT_3D('',#16771,#13493,#13494);
#11775=AXIS2_PLACEMENT_3D('',#16772,#13495,#13496);
#11776=AXIS2_PLACEMENT_3D('',#16781,#13501,#13502);
#11777=AXIS2_PLACEMENT_3D('',#16783,#13503,#13504);
#11778=AXIS2_PLACEMENT_3D('',#16785,#13505,#13506);
#11779=AXIS2_PLACEMENT_3D('',#16787,#13508,#13509);
#11780=AXIS2_PLACEMENT_3D('',#16793,#13513,#13514);
#11781=AXIS2_PLACEMENT_3D('',#16794,#13515,#13516);
#11782=AXIS2_PLACEMENT_3D('',#16795,#13517,#13518);
#11783=AXIS2_PLACEMENT_3D('',#16796,#13519,#13520);
#11784=AXIS2_PLACEMENT_3D('',#16805,#13525,#13526);
#11785=AXIS2_PLACEMENT_3D('',#16807,#13527,#13528);
#11786=AXIS2_PLACEMENT_3D('',#16809,#13529,#13530);
#11787=AXIS2_PLACEMENT_3D('',#16811,#13532,#13533);
#11788=AXIS2_PLACEMENT_3D('',#16817,#13537,#13538);
#11789=AXIS2_PLACEMENT_3D('',#16818,#13539,#13540);
#11790=AXIS2_PLACEMENT_3D('',#16819,#13541,#13542);
#11791=AXIS2_PLACEMENT_3D('',#16820,#13543,#13544);
#11792=AXIS2_PLACEMENT_3D('',#16822,#13545,#13546);
#11793=AXIS2_PLACEMENT_3D('',#16825,#13548,#13549);
#11794=AXIS2_PLACEMENT_3D('',#16826,#13550,#13551);
#11795=AXIS2_PLACEMENT_3D('',#16828,#13552,#13553);
#11796=AXIS2_PLACEMENT_3D('',#16831,#13555,#13556);
#11797=AXIS2_PLACEMENT_3D('',#16832,#13557,#13558);
#11798=AXIS2_PLACEMENT_3D('',#16834,#13559,#13560);
#11799=AXIS2_PLACEMENT_3D('',#16837,#13562,#13563);
#11800=AXIS2_PLACEMENT_3D('',#16838,#13564,#13565);
#11801=AXIS2_PLACEMENT_3D('',#16840,#13566,#13567);
#11802=AXIS2_PLACEMENT_3D('',#16843,#13569,#13570);
#11803=AXIS2_PLACEMENT_3D('',#16844,#13571,#13572);
#11804=AXIS2_PLACEMENT_3D('',#16846,#13573,#13574);
#11805=AXIS2_PLACEMENT_3D('',#16849,#13576,#13577);
#11806=AXIS2_PLACEMENT_3D('',#16850,#13578,#13579);
#11807=AXIS2_PLACEMENT_3D('',#16859,#13584,#13585);
#11808=AXIS2_PLACEMENT_3D('',#16861,#13586,#13587);
#11809=AXIS2_PLACEMENT_3D('',#16863,#13588,#13589);
#11810=AXIS2_PLACEMENT_3D('',#16865,#13591,#13592);
#11811=AXIS2_PLACEMENT_3D('',#16871,#13596,#13597);
#11812=AXIS2_PLACEMENT_3D('',#16872,#13598,#13599);
#11813=AXIS2_PLACEMENT_3D('',#16873,#13600,#13601);
#11814=AXIS2_PLACEMENT_3D('',#16874,#13602,#13603);
#11815=AXIS2_PLACEMENT_3D('',#16883,#13608,#13609);
#11816=AXIS2_PLACEMENT_3D('',#16885,#13610,#13611);
#11817=AXIS2_PLACEMENT_3D('',#16887,#13612,#13613);
#11818=AXIS2_PLACEMENT_3D('',#16889,#13615,#13616);
#11819=AXIS2_PLACEMENT_3D('',#16895,#13620,#13621);
#11820=AXIS2_PLACEMENT_3D('',#16896,#13622,#13623);
#11821=AXIS2_PLACEMENT_3D('',#16897,#13624,#13625);
#11822=AXIS2_PLACEMENT_3D('',#16898,#13626,#13627);
#11823=AXIS2_PLACEMENT_3D('',#16900,#13628,#13629);
#11824=AXIS2_PLACEMENT_3D('',#16903,#13631,#13632);
#11825=AXIS2_PLACEMENT_3D('',#16904,#13633,#13634);
#11826=AXIS2_PLACEMENT_3D('',#16906,#13635,#13636);
#11827=AXIS2_PLACEMENT_3D('',#16909,#13638,#13639);
#11828=AXIS2_PLACEMENT_3D('',#16910,#13640,#13641);
#11829=AXIS2_PLACEMENT_3D('',#16912,#13642,#13643);
#11830=AXIS2_PLACEMENT_3D('',#16915,#13645,#13646);
#11831=AXIS2_PLACEMENT_3D('',#16916,#13647,#13648);
#11832=AXIS2_PLACEMENT_3D('',#16918,#13649,#13650);
#11833=AXIS2_PLACEMENT_3D('',#16921,#13652,#13653);
#11834=AXIS2_PLACEMENT_3D('',#16922,#13654,#13655);
#11835=AXIS2_PLACEMENT_3D('',#16924,#13656,#13657);
#11836=AXIS2_PLACEMENT_3D('',#16927,#13659,#13660);
#11837=AXIS2_PLACEMENT_3D('',#16928,#13661,#13662);
#11838=AXIS2_PLACEMENT_3D('',#16937,#13667,#13668);
#11839=AXIS2_PLACEMENT_3D('',#16939,#13669,#13670);
#11840=AXIS2_PLACEMENT_3D('',#16941,#13671,#13672);
#11841=AXIS2_PLACEMENT_3D('',#16943,#13674,#13675);
#11842=AXIS2_PLACEMENT_3D('',#16949,#13679,#13680);
#11843=AXIS2_PLACEMENT_3D('',#16950,#13681,#13682);
#11844=AXIS2_PLACEMENT_3D('',#16951,#13683,#13684);
#11845=AXIS2_PLACEMENT_3D('',#16952,#13685,#13686);
#11846=AXIS2_PLACEMENT_3D('',#16961,#13691,#13692);
#11847=AXIS2_PLACEMENT_3D('',#16963,#13693,#13694);
#11848=AXIS2_PLACEMENT_3D('',#16965,#13695,#13696);
#11849=AXIS2_PLACEMENT_3D('',#16967,#13698,#13699);
#11850=AXIS2_PLACEMENT_3D('',#16973,#13703,#13704);
#11851=AXIS2_PLACEMENT_3D('',#16974,#13705,#13706);
#11852=AXIS2_PLACEMENT_3D('',#16975,#13707,#13708);
#11853=AXIS2_PLACEMENT_3D('',#16976,#13709,#13710);
#11854=AXIS2_PLACEMENT_3D('',#16978,#13711,#13712);
#11855=AXIS2_PLACEMENT_3D('',#16981,#13714,#13715);
#11856=AXIS2_PLACEMENT_3D('',#16982,#13716,#13717);
#11857=AXIS2_PLACEMENT_3D('',#16984,#13718,#13719);
#11858=AXIS2_PLACEMENT_3D('',#16987,#13721,#13722);
#11859=AXIS2_PLACEMENT_3D('',#16988,#13723,#13724);
#11860=AXIS2_PLACEMENT_3D('',#16990,#13725,#13726);
#11861=AXIS2_PLACEMENT_3D('',#16993,#13728,#13729);
#11862=AXIS2_PLACEMENT_3D('',#16994,#13730,#13731);
#11863=AXIS2_PLACEMENT_3D('',#16996,#13732,#13733);
#11864=AXIS2_PLACEMENT_3D('',#16999,#13735,#13736);
#11865=AXIS2_PLACEMENT_3D('',#17000,#13737,#13738);
#11866=AXIS2_PLACEMENT_3D('',#17002,#13739,#13740);
#11867=AXIS2_PLACEMENT_3D('',#17005,#13742,#13743);
#11868=AXIS2_PLACEMENT_3D('',#17006,#13744,#13745);
#11869=AXIS2_PLACEMENT_3D('',#17015,#13750,#13751);
#11870=AXIS2_PLACEMENT_3D('',#17017,#13752,#13753);
#11871=AXIS2_PLACEMENT_3D('',#17019,#13754,#13755);
#11872=AXIS2_PLACEMENT_3D('',#17021,#13757,#13758);
#11873=AXIS2_PLACEMENT_3D('',#17027,#13762,#13763);
#11874=AXIS2_PLACEMENT_3D('',#17028,#13764,#13765);
#11875=AXIS2_PLACEMENT_3D('',#17029,#13766,#13767);
#11876=AXIS2_PLACEMENT_3D('',#17030,#13768,#13769);
#11877=AXIS2_PLACEMENT_3D('',#17039,#13774,#13775);
#11878=AXIS2_PLACEMENT_3D('',#17041,#13776,#13777);
#11879=AXIS2_PLACEMENT_3D('',#17043,#13778,#13779);
#11880=AXIS2_PLACEMENT_3D('',#17045,#13781,#13782);
#11881=AXIS2_PLACEMENT_3D('',#17051,#13786,#13787);
#11882=AXIS2_PLACEMENT_3D('',#17052,#13788,#13789);
#11883=AXIS2_PLACEMENT_3D('',#17053,#13790,#13791);
#11884=AXIS2_PLACEMENT_3D('',#17054,#13792,#13793);
#11885=AXIS2_PLACEMENT_3D('',#17056,#13794,#13795);
#11886=AXIS2_PLACEMENT_3D('',#17059,#13797,#13798);
#11887=AXIS2_PLACEMENT_3D('',#17060,#13799,#13800);
#11888=AXIS2_PLACEMENT_3D('',#17062,#13801,#13802);
#11889=AXIS2_PLACEMENT_3D('',#17065,#13804,#13805);
#11890=AXIS2_PLACEMENT_3D('',#17066,#13806,#13807);
#11891=AXIS2_PLACEMENT_3D('',#17068,#13808,#13809);
#11892=AXIS2_PLACEMENT_3D('',#17071,#13811,#13812);
#11893=AXIS2_PLACEMENT_3D('',#17072,#13813,#13814);
#11894=AXIS2_PLACEMENT_3D('',#17074,#13815,#13816);
#11895=AXIS2_PLACEMENT_3D('',#17077,#13818,#13819);
#11896=AXIS2_PLACEMENT_3D('',#17078,#13820,#13821);
#11897=AXIS2_PLACEMENT_3D('',#17080,#13822,#13823);
#11898=AXIS2_PLACEMENT_3D('',#17083,#13825,#13826);
#11899=AXIS2_PLACEMENT_3D('',#17084,#13827,#13828);
#11900=AXIS2_PLACEMENT_3D('',#17093,#13833,#13834);
#11901=AXIS2_PLACEMENT_3D('',#17095,#13835,#13836);
#11902=AXIS2_PLACEMENT_3D('',#17097,#13837,#13838);
#11903=AXIS2_PLACEMENT_3D('',#17099,#13840,#13841);
#11904=AXIS2_PLACEMENT_3D('',#17105,#13845,#13846);
#11905=AXIS2_PLACEMENT_3D('',#17106,#13847,#13848);
#11906=AXIS2_PLACEMENT_3D('',#17107,#13849,#13850);
#11907=AXIS2_PLACEMENT_3D('',#17108,#13851,#13852);
#11908=AXIS2_PLACEMENT_3D('',#17117,#13857,#13858);
#11909=AXIS2_PLACEMENT_3D('',#17119,#13859,#13860);
#11910=AXIS2_PLACEMENT_3D('',#17121,#13861,#13862);
#11911=AXIS2_PLACEMENT_3D('',#17123,#13864,#13865);
#11912=AXIS2_PLACEMENT_3D('',#17129,#13869,#13870);
#11913=AXIS2_PLACEMENT_3D('',#17130,#13871,#13872);
#11914=AXIS2_PLACEMENT_3D('',#17131,#13873,#13874);
#11915=AXIS2_PLACEMENT_3D('',#17132,#13875,#13876);
#11916=AXIS2_PLACEMENT_3D('',#17134,#13877,#13878);
#11917=AXIS2_PLACEMENT_3D('',#17137,#13880,#13881);
#11918=AXIS2_PLACEMENT_3D('',#17138,#13882,#13883);
#11919=AXIS2_PLACEMENT_3D('',#17140,#13884,#13885);
#11920=AXIS2_PLACEMENT_3D('',#17143,#13887,#13888);
#11921=AXIS2_PLACEMENT_3D('',#17144,#13889,#13890);
#11922=AXIS2_PLACEMENT_3D('',#17146,#13891,#13892);
#11923=AXIS2_PLACEMENT_3D('',#17149,#13894,#13895);
#11924=AXIS2_PLACEMENT_3D('',#17150,#13896,#13897);
#11925=AXIS2_PLACEMENT_3D('',#17152,#13898,#13899);
#11926=AXIS2_PLACEMENT_3D('',#17155,#13901,#13902);
#11927=AXIS2_PLACEMENT_3D('',#17156,#13903,#13904);
#11928=AXIS2_PLACEMENT_3D('',#17158,#13905,#13906);
#11929=AXIS2_PLACEMENT_3D('',#17161,#13908,#13909);
#11930=AXIS2_PLACEMENT_3D('',#17162,#13910,#13911);
#11931=AXIS2_PLACEMENT_3D('',#17171,#13916,#13917);
#11932=AXIS2_PLACEMENT_3D('',#17173,#13918,#13919);
#11933=AXIS2_PLACEMENT_3D('',#17175,#13920,#13921);
#11934=AXIS2_PLACEMENT_3D('',#17177,#13923,#13924);
#11935=AXIS2_PLACEMENT_3D('',#17183,#13928,#13929);
#11936=AXIS2_PLACEMENT_3D('',#17184,#13930,#13931);
#11937=AXIS2_PLACEMENT_3D('',#17185,#13932,#13933);
#11938=AXIS2_PLACEMENT_3D('',#17186,#13934,#13935);
#11939=AXIS2_PLACEMENT_3D('',#17195,#13940,#13941);
#11940=AXIS2_PLACEMENT_3D('',#17197,#13942,#13943);
#11941=AXIS2_PLACEMENT_3D('',#17199,#13944,#13945);
#11942=AXIS2_PLACEMENT_3D('',#17201,#13947,#13948);
#11943=AXIS2_PLACEMENT_3D('',#17207,#13952,#13953);
#11944=AXIS2_PLACEMENT_3D('',#17208,#13954,#13955);
#11945=AXIS2_PLACEMENT_3D('',#17209,#13956,#13957);
#11946=AXIS2_PLACEMENT_3D('',#17210,#13958,#13959);
#11947=AXIS2_PLACEMENT_3D('',#17212,#13960,#13961);
#11948=AXIS2_PLACEMENT_3D('',#17215,#13963,#13964);
#11949=AXIS2_PLACEMENT_3D('',#17216,#13965,#13966);
#11950=AXIS2_PLACEMENT_3D('',#17218,#13967,#13968);
#11951=AXIS2_PLACEMENT_3D('',#17221,#13970,#13971);
#11952=AXIS2_PLACEMENT_3D('',#17222,#13972,#13973);
#11953=AXIS2_PLACEMENT_3D('',#17224,#13974,#13975);
#11954=AXIS2_PLACEMENT_3D('',#17227,#13977,#13978);
#11955=AXIS2_PLACEMENT_3D('',#17228,#13979,#13980);
#11956=AXIS2_PLACEMENT_3D('',#17230,#13981,#13982);
#11957=AXIS2_PLACEMENT_3D('',#17233,#13984,#13985);
#11958=AXIS2_PLACEMENT_3D('',#17234,#13986,#13987);
#11959=AXIS2_PLACEMENT_3D('',#17236,#13988,#13989);
#11960=AXIS2_PLACEMENT_3D('',#17239,#13991,#13992);
#11961=AXIS2_PLACEMENT_3D('',#17240,#13993,#13994);
#11962=AXIS2_PLACEMENT_3D('',#17249,#13999,#14000);
#11963=AXIS2_PLACEMENT_3D('',#17251,#14001,#14002);
#11964=AXIS2_PLACEMENT_3D('',#17253,#14003,#14004);
#11965=AXIS2_PLACEMENT_3D('',#17255,#14006,#14007);
#11966=AXIS2_PLACEMENT_3D('',#17261,#14011,#14012);
#11967=AXIS2_PLACEMENT_3D('',#17262,#14013,#14014);
#11968=AXIS2_PLACEMENT_3D('',#17263,#14015,#14016);
#11969=AXIS2_PLACEMENT_3D('',#17264,#14017,#14018);
#11970=AXIS2_PLACEMENT_3D('',#17273,#14023,#14024);
#11971=AXIS2_PLACEMENT_3D('',#17275,#14025,#14026);
#11972=AXIS2_PLACEMENT_3D('',#17277,#14027,#14028);
#11973=AXIS2_PLACEMENT_3D('',#17279,#14030,#14031);
#11974=AXIS2_PLACEMENT_3D('',#17285,#14035,#14036);
#11975=AXIS2_PLACEMENT_3D('',#17286,#14037,#14038);
#11976=AXIS2_PLACEMENT_3D('',#17287,#14039,#14040);
#11977=AXIS2_PLACEMENT_3D('',#17288,#14041,#14042);
#11978=AXIS2_PLACEMENT_3D('',#17290,#14043,#14044);
#11979=AXIS2_PLACEMENT_3D('',#17293,#14046,#14047);
#11980=AXIS2_PLACEMENT_3D('',#17294,#14048,#14049);
#11981=AXIS2_PLACEMENT_3D('',#17296,#14050,#14051);
#11982=AXIS2_PLACEMENT_3D('',#17299,#14053,#14054);
#11983=AXIS2_PLACEMENT_3D('',#17300,#14055,#14056);
#11984=AXIS2_PLACEMENT_3D('',#17302,#14057,#14058);
#11985=AXIS2_PLACEMENT_3D('',#17305,#14060,#14061);
#11986=AXIS2_PLACEMENT_3D('',#17306,#14062,#14063);
#11987=AXIS2_PLACEMENT_3D('',#17308,#14064,#14065);
#11988=AXIS2_PLACEMENT_3D('',#17311,#14067,#14068);
#11989=AXIS2_PLACEMENT_3D('',#17312,#14069,#14070);
#11990=AXIS2_PLACEMENT_3D('',#17314,#14071,#14072);
#11991=AXIS2_PLACEMENT_3D('',#17317,#14074,#14075);
#11992=AXIS2_PLACEMENT_3D('',#17318,#14076,#14077);
#11993=AXIS2_PLACEMENT_3D('',#17327,#14082,#14083);
#11994=AXIS2_PLACEMENT_3D('',#17329,#14084,#14085);
#11995=AXIS2_PLACEMENT_3D('',#17331,#14086,#14087);
#11996=AXIS2_PLACEMENT_3D('',#17333,#14089,#14090);
#11997=AXIS2_PLACEMENT_3D('',#17339,#14094,#14095);
#11998=AXIS2_PLACEMENT_3D('',#17340,#14096,#14097);
#11999=AXIS2_PLACEMENT_3D('',#17341,#14098,#14099);
#12000=AXIS2_PLACEMENT_3D('',#17342,#14100,#14101);
#12001=AXIS2_PLACEMENT_3D('',#17351,#14106,#14107);
#12002=AXIS2_PLACEMENT_3D('',#17353,#14108,#14109);
#12003=AXIS2_PLACEMENT_3D('',#17355,#14110,#14111);
#12004=AXIS2_PLACEMENT_3D('',#17357,#14113,#14114);
#12005=AXIS2_PLACEMENT_3D('',#17363,#14118,#14119);
#12006=AXIS2_PLACEMENT_3D('',#17364,#14120,#14121);
#12007=AXIS2_PLACEMENT_3D('',#17365,#14122,#14123);
#12008=AXIS2_PLACEMENT_3D('',#17366,#14124,#14125);
#12009=AXIS2_PLACEMENT_3D('',#17368,#14126,#14127);
#12010=AXIS2_PLACEMENT_3D('',#17371,#14129,#14130);
#12011=AXIS2_PLACEMENT_3D('',#17372,#14131,#14132);
#12012=AXIS2_PLACEMENT_3D('',#17374,#14133,#14134);
#12013=AXIS2_PLACEMENT_3D('',#17377,#14136,#14137);
#12014=AXIS2_PLACEMENT_3D('',#17378,#14138,#14139);
#12015=AXIS2_PLACEMENT_3D('',#17380,#14140,#14141);
#12016=AXIS2_PLACEMENT_3D('',#17383,#14143,#14144);
#12017=AXIS2_PLACEMENT_3D('',#17384,#14145,#14146);
#12018=AXIS2_PLACEMENT_3D('',#17386,#14147,#14148);
#12019=AXIS2_PLACEMENT_3D('',#17389,#14150,#14151);
#12020=AXIS2_PLACEMENT_3D('',#17390,#14152,#14153);
#12021=AXIS2_PLACEMENT_3D('',#17392,#14154,#14155);
#12022=AXIS2_PLACEMENT_3D('',#17395,#14157,#14158);
#12023=AXIS2_PLACEMENT_3D('',#17396,#14159,#14160);
#12024=AXIS2_PLACEMENT_3D('',#17405,#14165,#14166);
#12025=AXIS2_PLACEMENT_3D('',#17407,#14167,#14168);
#12026=AXIS2_PLACEMENT_3D('',#17409,#14169,#14170);
#12027=AXIS2_PLACEMENT_3D('',#17411,#14172,#14173);
#12028=AXIS2_PLACEMENT_3D('',#17417,#14177,#14178);
#12029=AXIS2_PLACEMENT_3D('',#17418,#14179,#14180);
#12030=AXIS2_PLACEMENT_3D('',#17419,#14181,#14182);
#12031=AXIS2_PLACEMENT_3D('',#17420,#14183,#14184);
#12032=AXIS2_PLACEMENT_3D('',#17429,#14189,#14190);
#12033=AXIS2_PLACEMENT_3D('',#17431,#14191,#14192);
#12034=AXIS2_PLACEMENT_3D('',#17433,#14193,#14194);
#12035=AXIS2_PLACEMENT_3D('',#17435,#14196,#14197);
#12036=AXIS2_PLACEMENT_3D('',#17441,#14201,#14202);
#12037=AXIS2_PLACEMENT_3D('',#17442,#14203,#14204);
#12038=AXIS2_PLACEMENT_3D('',#17443,#14205,#14206);
#12039=AXIS2_PLACEMENT_3D('',#17444,#14207,#14208);
#12040=AXIS2_PLACEMENT_3D('',#17446,#14209,#14210);
#12041=AXIS2_PLACEMENT_3D('',#17449,#14212,#14213);
#12042=AXIS2_PLACEMENT_3D('',#17450,#14214,#14215);
#12043=AXIS2_PLACEMENT_3D('',#17452,#14216,#14217);
#12044=AXIS2_PLACEMENT_3D('',#17455,#14219,#14220);
#12045=AXIS2_PLACEMENT_3D('',#17456,#14221,#14222);
#12046=AXIS2_PLACEMENT_3D('',#17465,#14227,#14228);
#12047=AXIS2_PLACEMENT_3D('',#17467,#14229,#14230);
#12048=AXIS2_PLACEMENT_3D('',#17469,#14231,#14232);
#12049=AXIS2_PLACEMENT_3D('',#17471,#14234,#14235);
#12050=AXIS2_PLACEMENT_3D('',#17477,#14239,#14240);
#12051=AXIS2_PLACEMENT_3D('',#17478,#14241,#14242);
#12052=AXIS2_PLACEMENT_3D('',#17479,#14243,#14244);
#12053=AXIS2_PLACEMENT_3D('',#17480,#14245,#14246);
#12054=AXIS2_PLACEMENT_3D('',#17489,#14251,#14252);
#12055=AXIS2_PLACEMENT_3D('',#17491,#14253,#14254);
#12056=AXIS2_PLACEMENT_3D('',#17493,#14255,#14256);
#12057=AXIS2_PLACEMENT_3D('',#17495,#14258,#14259);
#12058=AXIS2_PLACEMENT_3D('',#17501,#14263,#14264);
#12059=AXIS2_PLACEMENT_3D('',#17502,#14265,#14266);
#12060=AXIS2_PLACEMENT_3D('',#17503,#14267,#14268);
#12061=AXIS2_PLACEMENT_3D('',#17504,#14269,#14270);
#12062=AXIS2_PLACEMENT_3D('',#17506,#14271,#14272);
#12063=AXIS2_PLACEMENT_3D('',#17509,#14274,#14275);
#12064=AXIS2_PLACEMENT_3D('',#17510,#14276,#14277);
#12065=AXIS2_PLACEMENT_3D('',#17512,#14278,#14279);
#12066=AXIS2_PLACEMENT_3D('',#17515,#14281,#14282);
#12067=AXIS2_PLACEMENT_3D('',#17516,#14283,#14284);
#12068=AXIS2_PLACEMENT_3D('',#17518,#14285,#14286);
#12069=AXIS2_PLACEMENT_3D('',#17521,#14288,#14289);
#12070=AXIS2_PLACEMENT_3D('',#17522,#14290,#14291);
#12071=AXIS2_PLACEMENT_3D('',#17525,#14292,#14293);
#12072=AXIS2_PLACEMENT_3D('',#17529,#14295,#14296);
#12073=AXIS2_PLACEMENT_3D('',#17531,#14298,#14299);
#12074=AXIS2_PLACEMENT_3D('',#17537,#14303,#14304);
#12075=AXIS2_PLACEMENT_3D('',#17539,#14305,#14306);
#12076=AXIS2_PLACEMENT_3D('',#17542,#14308,#14309);
#12077=AXIS2_PLACEMENT_3D('',#17543,#14310,#14311);
#12078=AXIS2_PLACEMENT_3D('',#17550,#14315,#14316);
#12079=AXIS2_PLACEMENT_3D('',#17552,#14317,#14318);
#12080=AXIS2_PLACEMENT_3D('',#17554,#14319,#14320);
#12081=AXIS2_PLACEMENT_3D('',#17556,#14321,#14322);
#12082=AXIS2_PLACEMENT_3D('',#17558,#14323,#14324);
#12083=AXIS2_PLACEMENT_3D('',#17560,#14325,#14326);
#12084=AXIS2_PLACEMENT_3D('',#17562,#14327,#14328);
#12085=AXIS2_PLACEMENT_3D('',#17564,#14329,#14330);
#12086=AXIS2_PLACEMENT_3D('',#17566,#14331,#14332);
#12087=AXIS2_PLACEMENT_3D('',#17568,#14333,#14334);
#12088=AXIS2_PLACEMENT_3D('',#17570,#14335,#14336);
#12089=AXIS2_PLACEMENT_3D('',#17572,#14337,#14338);
#12090=AXIS2_PLACEMENT_3D('',#17574,#14339,#14340);
#12091=AXIS2_PLACEMENT_3D('',#17576,#14341,#14342);
#12092=AXIS2_PLACEMENT_3D('',#17578,#14343,#14344);
#12093=AXIS2_PLACEMENT_3D('',#17580,#14345,#14346);
#12094=AXIS2_PLACEMENT_3D('',#17582,#14347,#14348);
#12095=AXIS2_PLACEMENT_3D('',#17584,#14349,#14350);
#12096=AXIS2_PLACEMENT_3D('',#17586,#14351,#14352);
#12097=AXIS2_PLACEMENT_3D('',#17588,#14353,#14354);
#12098=AXIS2_PLACEMENT_3D('',#17590,#14355,#14356);
#12099=AXIS2_PLACEMENT_3D('',#17592,#14357,#14358);
#12100=AXIS2_PLACEMENT_3D('',#17594,#14359,#14360);
#12101=AXIS2_PLACEMENT_3D('',#17596,#14361,#14362);
#12102=AXIS2_PLACEMENT_3D('',#17598,#14363,#14364);
#12103=AXIS2_PLACEMENT_3D('',#17600,#14365,#14366);
#12104=AXIS2_PLACEMENT_3D('',#17602,#14367,#14368);
#12105=AXIS2_PLACEMENT_3D('',#17604,#14369,#14370);
#12106=AXIS2_PLACEMENT_3D('',#17606,#14371,#14372);
#12107=AXIS2_PLACEMENT_3D('',#17608,#14373,#14374);
#12108=AXIS2_PLACEMENT_3D('',#17610,#14375,#14376);
#12109=AXIS2_PLACEMENT_3D('',#17612,#14377,#14378);
#12110=AXIS2_PLACEMENT_3D('',#17614,#14379,#14380);
#12111=AXIS2_PLACEMENT_3D('',#17616,#14381,#14382);
#12112=AXIS2_PLACEMENT_3D('',#17618,#14383,#14384);
#12113=AXIS2_PLACEMENT_3D('',#17620,#14385,#14386);
#12114=AXIS2_PLACEMENT_3D('',#17622,#14387,#14388);
#12115=AXIS2_PLACEMENT_3D('',#17624,#14389,#14390);
#12116=AXIS2_PLACEMENT_3D('',#17626,#14391,#14392);
#12117=AXIS2_PLACEMENT_3D('',#17628,#14393,#14394);
#12118=AXIS2_PLACEMENT_3D('',#17630,#14395,#14396);
#12119=AXIS2_PLACEMENT_3D('',#17632,#14397,#14398);
#12120=AXIS2_PLACEMENT_3D('',#17634,#14399,#14400);
#12121=AXIS2_PLACEMENT_3D('',#17636,#14401,#14402);
#12122=AXIS2_PLACEMENT_3D('',#17638,#14403,#14404);
#12123=AXIS2_PLACEMENT_3D('',#17640,#14405,#14406);
#12124=AXIS2_PLACEMENT_3D('',#17642,#14407,#14408);
#12125=AXIS2_PLACEMENT_3D('',#17643,#14409,#14410);
#12126=AXIS2_PLACEMENT_3D('',#17646,#14411,#14412);
#12127=AXIS2_PLACEMENT_3D('',#17650,#14414,#14415);
#12128=AXIS2_PLACEMENT_3D('',#17652,#14417,#14418);
#12129=AXIS2_PLACEMENT_3D('',#17658,#14422,#14423);
#12130=AXIS2_PLACEMENT_3D('',#17668,#14429,#14430);
#12131=AXIS2_PLACEMENT_3D('',#17669,#14431,#14432);
#12132=AXIS2_PLACEMENT_3D('',#17671,#14433,#14434);
#12133=AXIS2_PLACEMENT_3D('',#17673,#14436,#14437);
#12134=AXIS2_PLACEMENT_3D('',#17675,#14438,#14439);
#12135=AXIS2_PLACEMENT_3D('',#17677,#14441,#14442);
#12136=AXIS2_PLACEMENT_3D('',#17679,#14443,#14444);
#12137=AXIS2_PLACEMENT_3D('',#17681,#14446,#14447);
#12138=AXIS2_PLACEMENT_3D('',#17683,#14448,#14449);
#12139=AXIS2_PLACEMENT_3D('',#17685,#14451,#14452);
#12140=AXIS2_PLACEMENT_3D('',#17687,#14453,#14454);
#12141=AXIS2_PLACEMENT_3D('',#17689,#14456,#14457);
#12142=AXIS2_PLACEMENT_3D('',#17691,#14458,#14459);
#12143=AXIS2_PLACEMENT_3D('',#17693,#14461,#14462);
#12144=AXIS2_PLACEMENT_3D('',#17695,#14463,#14464);
#12145=AXIS2_PLACEMENT_3D('',#17697,#14466,#14467);
#12146=AXIS2_PLACEMENT_3D('',#17699,#14468,#14469);
#12147=AXIS2_PLACEMENT_3D('',#17701,#14471,#14472);
#12148=AXIS2_PLACEMENT_3D('',#17703,#14473,#14474);
#12149=AXIS2_PLACEMENT_3D('',#17705,#14476,#14477);
#12150=AXIS2_PLACEMENT_3D('',#17707,#14478,#14479);
#12151=AXIS2_PLACEMENT_3D('',#17709,#14481,#14482);
#12152=AXIS2_PLACEMENT_3D('',#17711,#14483,#14484);
#12153=AXIS2_PLACEMENT_3D('',#17713,#14486,#14487);
#12154=AXIS2_PLACEMENT_3D('',#17715,#14488,#14489);
#12155=AXIS2_PLACEMENT_3D('',#17717,#14491,#14492);
#12156=AXIS2_PLACEMENT_3D('',#17719,#14493,#14494);
#12157=AXIS2_PLACEMENT_3D('',#17721,#14496,#14497);
#12158=AXIS2_PLACEMENT_3D('',#17723,#14498,#14499);
#12159=AXIS2_PLACEMENT_3D('',#17725,#14501,#14502);
#12160=AXIS2_PLACEMENT_3D('',#17727,#14503,#14504);
#12161=AXIS2_PLACEMENT_3D('',#17729,#14506,#14507);
#12162=AXIS2_PLACEMENT_3D('',#17731,#14508,#14509);
#12163=AXIS2_PLACEMENT_3D('',#17733,#14511,#14512);
#12164=AXIS2_PLACEMENT_3D('',#17735,#14513,#14514);
#12165=AXIS2_PLACEMENT_3D('',#17737,#14516,#14517);
#12166=AXIS2_PLACEMENT_3D('',#17739,#14518,#14519);
#12167=AXIS2_PLACEMENT_3D('',#17741,#14521,#14522);
#12168=AXIS2_PLACEMENT_3D('',#17743,#14523,#14524);
#12169=AXIS2_PLACEMENT_3D('',#17745,#14526,#14527);
#12170=AXIS2_PLACEMENT_3D('',#17747,#14528,#14529);
#12171=AXIS2_PLACEMENT_3D('',#17749,#14531,#14532);
#12172=AXIS2_PLACEMENT_3D('',#17751,#14533,#14534);
#12173=AXIS2_PLACEMENT_3D('',#17753,#14536,#14537);
#12174=AXIS2_PLACEMENT_3D('',#17755,#14538,#14539);
#12175=AXIS2_PLACEMENT_3D('',#17757,#14541,#14542);
#12176=AXIS2_PLACEMENT_3D('',#17759,#14543,#14544);
#12177=AXIS2_PLACEMENT_3D('',#17761,#14546,#14547);
#12178=AXIS2_PLACEMENT_3D('',#17763,#14548,#14549);
#12179=AXIS2_PLACEMENT_3D('',#17765,#14551,#14552);
#12180=AXIS2_PLACEMENT_3D('',#17767,#14553,#14554);
#12181=AXIS2_PLACEMENT_3D('',#17769,#14556,#14557);
#12182=AXIS2_PLACEMENT_3D('',#17771,#14558,#14559);
#12183=AXIS2_PLACEMENT_3D('',#17773,#14561,#14562);
#12184=AXIS2_PLACEMENT_3D('',#17775,#14563,#14564);
#12185=AXIS2_PLACEMENT_3D('',#17777,#14566,#14567);
#12186=AXIS2_PLACEMENT_3D('',#17779,#14568,#14569);
#12187=AXIS2_PLACEMENT_3D('',#17781,#14571,#14572);
#12188=AXIS2_PLACEMENT_3D('',#17783,#14573,#14574);
#12189=AXIS2_PLACEMENT_3D('',#17785,#14576,#14577);
#12190=AXIS2_PLACEMENT_3D('',#17787,#14578,#14579);
#12191=AXIS2_PLACEMENT_3D('',#17789,#14581,#14582);
#12192=AXIS2_PLACEMENT_3D('',#17791,#14583,#14584);
#12193=AXIS2_PLACEMENT_3D('',#17793,#14586,#14587);
#12194=AXIS2_PLACEMENT_3D('',#17795,#14588,#14589);
#12195=AXIS2_PLACEMENT_3D('',#17797,#14591,#14592);
#12196=AXIS2_PLACEMENT_3D('',#17799,#14593,#14594);
#12197=AXIS2_PLACEMENT_3D('',#17801,#14596,#14597);
#12198=AXIS2_PLACEMENT_3D('',#17803,#14598,#14599);
#12199=AXIS2_PLACEMENT_3D('',#17805,#14601,#14602);
#12200=AXIS2_PLACEMENT_3D('',#17807,#14603,#14604);
#12201=AXIS2_PLACEMENT_3D('',#17809,#14606,#14607);
#12202=AXIS2_PLACEMENT_3D('',#17811,#14608,#14609);
#12203=AXIS2_PLACEMENT_3D('',#17813,#14611,#14612);
#12204=AXIS2_PLACEMENT_3D('',#17815,#14613,#14614);
#12205=AXIS2_PLACEMENT_3D('',#17817,#14616,#14617);
#12206=AXIS2_PLACEMENT_3D('',#17819,#14618,#14619);
#12207=AXIS2_PLACEMENT_3D('',#17821,#14621,#14622);
#12208=AXIS2_PLACEMENT_3D('',#17823,#14623,#14624);
#12209=AXIS2_PLACEMENT_3D('',#17825,#14626,#14627);
#12210=AXIS2_PLACEMENT_3D('',#17827,#14628,#14629);
#12211=AXIS2_PLACEMENT_3D('',#17829,#14631,#14632);
#12212=AXIS2_PLACEMENT_3D('',#17831,#14633,#14634);
#12213=AXIS2_PLACEMENT_3D('',#17833,#14636,#14637);
#12214=AXIS2_PLACEMENT_3D('',#17835,#14638,#14639);
#12215=AXIS2_PLACEMENT_3D('',#17837,#14641,#14642);
#12216=AXIS2_PLACEMENT_3D('',#17839,#14643,#14644);
#12217=AXIS2_PLACEMENT_3D('',#17841,#14646,#14647);
#12218=AXIS2_PLACEMENT_3D('',#17843,#14648,#14649);
#12219=AXIS2_PLACEMENT_3D('',#17845,#14651,#14652);
#12220=AXIS2_PLACEMENT_3D('',#17847,#14653,#14654);
#12221=AXIS2_PLACEMENT_3D('',#17849,#14656,#14657);
#12222=AXIS2_PLACEMENT_3D('',#17851,#14658,#14659);
#12223=AXIS2_PLACEMENT_3D('',#17853,#14661,#14662);
#12224=AXIS2_PLACEMENT_3D('',#17855,#14663,#14664);
#12225=AXIS2_PLACEMENT_3D('',#17857,#14666,#14667);
#12226=AXIS2_PLACEMENT_3D('',#17859,#14668,#14669);
#12227=AXIS2_PLACEMENT_3D('',#17861,#14671,#14672);
#12228=AXIS2_PLACEMENT_3D('',#17865,#14675,#14676);
#12229=AXIS2_PLACEMENT_3D('',#17867,#14678,#14679);
#12230=AXIS2_PLACEMENT_3D('',#17869,#14680,#14681);
#12231=AXIS2_PLACEMENT_3D('',#17872,#14683,#14684);
#12232=AXIS2_PLACEMENT_3D('',#17873,#14685,#14686);
#12233=AXIS2_PLACEMENT_3D('',#17875,#14687,#14688);
#12234=AXIS2_PLACEMENT_3D('',#17878,#14690,#14691);
#12235=AXIS2_PLACEMENT_3D('',#17879,#14692,#14693);
#12236=AXIS2_PLACEMENT_3D('',#17881,#14694,#14695);
#12237=AXIS2_PLACEMENT_3D('',#17884,#14697,#14698);
#12238=AXIS2_PLACEMENT_3D('',#17885,#14699,#14700);
#12239=AXIS2_PLACEMENT_3D('',#17887,#14701,#14702);
#12240=AXIS2_PLACEMENT_3D('',#17890,#14704,#14705);
#12241=AXIS2_PLACEMENT_3D('',#17891,#14706,#14707);
#12242=AXIS2_PLACEMENT_3D('',#17893,#14708,#14709);
#12243=AXIS2_PLACEMENT_3D('',#17896,#14711,#14712);
#12244=AXIS2_PLACEMENT_3D('',#17897,#14713,#14714);
#12245=AXIS2_PLACEMENT_3D('',#17899,#14715,#14716);
#12246=AXIS2_PLACEMENT_3D('',#17902,#14718,#14719);
#12247=AXIS2_PLACEMENT_3D('',#17903,#14720,#14721);
#12248=AXIS2_PLACEMENT_3D('',#17905,#14722,#14723);
#12249=AXIS2_PLACEMENT_3D('',#17908,#14725,#14726);
#12250=AXIS2_PLACEMENT_3D('',#17909,#14727,#14728);
#12251=AXIS2_PLACEMENT_3D('',#17911,#14729,#14730);
#12252=AXIS2_PLACEMENT_3D('',#17914,#14732,#14733);
#12253=AXIS2_PLACEMENT_3D('',#17915,#14734,#14735);
#12254=AXIS2_PLACEMENT_3D('',#17917,#14736,#14737);
#12255=AXIS2_PLACEMENT_3D('',#17920,#14739,#14740);
#12256=AXIS2_PLACEMENT_3D('',#17921,#14741,#14742);
#12257=AXIS2_PLACEMENT_3D('',#17923,#14743,#14744);
#12258=AXIS2_PLACEMENT_3D('',#17926,#14746,#14747);
#12259=AXIS2_PLACEMENT_3D('',#17927,#14748,#14749);
#12260=AXIS2_PLACEMENT_3D('',#17929,#14750,#14751);
#12261=AXIS2_PLACEMENT_3D('',#17932,#14753,#14754);
#12262=AXIS2_PLACEMENT_3D('',#17933,#14755,#14756);
#12263=AXIS2_PLACEMENT_3D('',#17935,#14757,#14758);
#12264=AXIS2_PLACEMENT_3D('',#17938,#14760,#14761);
#12265=AXIS2_PLACEMENT_3D('',#17939,#14762,#14763);
#12266=AXIS2_PLACEMENT_3D('',#17941,#14764,#14765);
#12267=AXIS2_PLACEMENT_3D('',#17944,#14767,#14768);
#12268=AXIS2_PLACEMENT_3D('',#17945,#14769,#14770);
#12269=AXIS2_PLACEMENT_3D('',#17947,#14771,#14772);
#12270=AXIS2_PLACEMENT_3D('',#17950,#14774,#14775);
#12271=AXIS2_PLACEMENT_3D('',#17951,#14776,#14777);
#12272=AXIS2_PLACEMENT_3D('',#17953,#14778,#14779);
#12273=AXIS2_PLACEMENT_3D('',#17956,#14781,#14782);
#12274=AXIS2_PLACEMENT_3D('',#17957,#14783,#14784);
#12275=AXIS2_PLACEMENT_3D('',#17959,#14785,#14786);
#12276=AXIS2_PLACEMENT_3D('',#17962,#14788,#14789);
#12277=AXIS2_PLACEMENT_3D('',#17963,#14790,#14791);
#12278=AXIS2_PLACEMENT_3D('',#17965,#14792,#14793);
#12279=AXIS2_PLACEMENT_3D('',#17968,#14795,#14796);
#12280=AXIS2_PLACEMENT_3D('',#17969,#14797,#14798);
#12281=AXIS2_PLACEMENT_3D('',#17971,#14799,#14800);
#12282=AXIS2_PLACEMENT_3D('',#17974,#14802,#14803);
#12283=AXIS2_PLACEMENT_3D('',#17975,#14804,#14805);
#12284=AXIS2_PLACEMENT_3D('',#17977,#14806,#14807);
#12285=AXIS2_PLACEMENT_3D('',#17980,#14809,#14810);
#12286=AXIS2_PLACEMENT_3D('',#17981,#14811,#14812);
#12287=AXIS2_PLACEMENT_3D('',#17983,#14813,#14814);
#12288=AXIS2_PLACEMENT_3D('',#17986,#14816,#14817);
#12289=AXIS2_PLACEMENT_3D('',#17987,#14818,#14819);
#12290=AXIS2_PLACEMENT_3D('',#17989,#14820,#14821);
#12291=AXIS2_PLACEMENT_3D('',#17992,#14823,#14824);
#12292=AXIS2_PLACEMENT_3D('',#17993,#14825,#14826);
#12293=AXIS2_PLACEMENT_3D('',#17995,#14827,#14828);
#12294=AXIS2_PLACEMENT_3D('',#17998,#14830,#14831);
#12295=AXIS2_PLACEMENT_3D('',#17999,#14832,#14833);
#12296=AXIS2_PLACEMENT_3D('',#18001,#14834,#14835);
#12297=AXIS2_PLACEMENT_3D('',#18004,#14837,#14838);
#12298=AXIS2_PLACEMENT_3D('',#18005,#14839,#14840);
#12299=AXIS2_PLACEMENT_3D('',#18007,#14841,#14842);
#12300=AXIS2_PLACEMENT_3D('',#18010,#14844,#14845);
#12301=AXIS2_PLACEMENT_3D('',#18011,#14846,#14847);
#12302=AXIS2_PLACEMENT_3D('',#18013,#14848,#14849);
#12303=AXIS2_PLACEMENT_3D('',#18016,#14851,#14852);
#12304=AXIS2_PLACEMENT_3D('',#18017,#14853,#14854);
#12305=AXIS2_PLACEMENT_3D('',#18019,#14855,#14856);
#12306=AXIS2_PLACEMENT_3D('',#18022,#14858,#14859);
#12307=AXIS2_PLACEMENT_3D('',#18023,#14860,#14861);
#12308=AXIS2_PLACEMENT_3D('',#18025,#14862,#14863);
#12309=AXIS2_PLACEMENT_3D('',#18028,#14865,#14866);
#12310=AXIS2_PLACEMENT_3D('',#18029,#14867,#14868);
#12311=AXIS2_PLACEMENT_3D('',#18031,#14869,#14870);
#12312=AXIS2_PLACEMENT_3D('',#18034,#14872,#14873);
#12313=AXIS2_PLACEMENT_3D('',#18035,#14874,#14875);
#12314=AXIS2_PLACEMENT_3D('',#18037,#14876,#14877);
#12315=AXIS2_PLACEMENT_3D('',#18040,#14879,#14880);
#12316=AXIS2_PLACEMENT_3D('',#18041,#14881,#14882);
#12317=AXIS2_PLACEMENT_3D('',#18043,#14883,#14884);
#12318=AXIS2_PLACEMENT_3D('',#18046,#14886,#14887);
#12319=AXIS2_PLACEMENT_3D('',#18047,#14888,#14889);
#12320=AXIS2_PLACEMENT_3D('',#18049,#14890,#14891);
#12321=AXIS2_PLACEMENT_3D('',#18052,#14893,#14894);
#12322=AXIS2_PLACEMENT_3D('',#18053,#14895,#14896);
#12323=AXIS2_PLACEMENT_3D('',#18055,#14897,#14898);
#12324=AXIS2_PLACEMENT_3D('',#18058,#14900,#14901);
#12325=AXIS2_PLACEMENT_3D('',#18059,#14902,#14903);
#12326=AXIS2_PLACEMENT_3D('',#18061,#14904,#14905);
#12327=AXIS2_PLACEMENT_3D('',#18064,#14907,#14908);
#12328=AXIS2_PLACEMENT_3D('',#18065,#14909,#14910);
#12329=AXIS2_PLACEMENT_3D('',#18067,#14911,#14912);
#12330=AXIS2_PLACEMENT_3D('',#18070,#14914,#14915);
#12331=AXIS2_PLACEMENT_3D('',#18071,#14916,#14917);
#12332=AXIS2_PLACEMENT_3D('',#18073,#14918,#14919);
#12333=AXIS2_PLACEMENT_3D('',#18076,#14921,#14922);
#12334=AXIS2_PLACEMENT_3D('',#18077,#14923,#14924);
#12335=AXIS2_PLACEMENT_3D('',#18079,#14925,#14926);
#12336=AXIS2_PLACEMENT_3D('',#18082,#14928,#14929);
#12337=AXIS2_PLACEMENT_3D('',#18083,#14930,#14931);
#12338=AXIS2_PLACEMENT_3D('',#18085,#14932,#14933);
#12339=AXIS2_PLACEMENT_3D('',#18088,#14935,#14936);
#12340=AXIS2_PLACEMENT_3D('',#18089,#14937,#14938);
#12341=AXIS2_PLACEMENT_3D('',#18091,#14939,#14940);
#12342=AXIS2_PLACEMENT_3D('',#18094,#14942,#14943);
#12343=AXIS2_PLACEMENT_3D('',#18095,#14944,#14945);
#12344=AXIS2_PLACEMENT_3D('',#18097,#14946,#14947);
#12345=AXIS2_PLACEMENT_3D('',#18100,#14949,#14950);
#12346=AXIS2_PLACEMENT_3D('',#18101,#14951,#14952);
#12347=AXIS2_PLACEMENT_3D('',#18103,#14953,#14954);
#12348=AXIS2_PLACEMENT_3D('',#18106,#14956,#14957);
#12349=AXIS2_PLACEMENT_3D('',#18107,#14958,#14959);
#12350=AXIS2_PLACEMENT_3D('',#18109,#14960,#14961);
#12351=AXIS2_PLACEMENT_3D('',#18112,#14963,#14964);
#12352=AXIS2_PLACEMENT_3D('',#18113,#14965,#14966);
#12353=AXIS2_PLACEMENT_3D('',#18115,#14967,#14968);
#12354=AXIS2_PLACEMENT_3D('',#18118,#14970,#14971);
#12355=AXIS2_PLACEMENT_3D('',#18119,#14972,#14973);
#12356=AXIS2_PLACEMENT_3D('',#18121,#14974,#14975);
#12357=AXIS2_PLACEMENT_3D('',#18124,#14977,#14978);
#12358=AXIS2_PLACEMENT_3D('',#18125,#14979,#14980);
#12359=AXIS2_PLACEMENT_3D('',#18127,#14981,#14982);
#12360=AXIS2_PLACEMENT_3D('',#18130,#14984,#14985);
#12361=AXIS2_PLACEMENT_3D('',#18131,#14986,#14987);
#12362=AXIS2_PLACEMENT_3D('',#18133,#14988,#14989);
#12363=AXIS2_PLACEMENT_3D('',#18136,#14991,#14992);
#12364=AXIS2_PLACEMENT_3D('',#18137,#14993,#14994);
#12365=AXIS2_PLACEMENT_3D('',#18139,#14995,#14996);
#12366=AXIS2_PLACEMENT_3D('',#18142,#14998,#14999);
#12367=AXIS2_PLACEMENT_3D('',#18143,#15000,#15001);
#12368=AXIS2_PLACEMENT_3D('',#18145,#15002,#15003);
#12369=AXIS2_PLACEMENT_3D('',#18148,#15005,#15006);
#12370=AXIS2_PLACEMENT_3D('',#18149,#15007,#15008);
#12371=AXIS2_PLACEMENT_3D('',#18155,#15012,#15013);
#12372=AXIS2_PLACEMENT_3D('',#18158,#15016,#15017);
#12373=AXIS2_PLACEMENT_3D('',#18159,#15018,#15019);
#13458=DIRECTION('axis',(0.,0.,1.));
#13459=DIRECTION('refdir',(1.,0.,0.));
#13460=DIRECTION('center_axis',(0.,0.,-1.));
#13461=DIRECTION('ref_axis',(-1.,0.,0.));
#13462=DIRECTION('center_axis',(0.,0.,-1.));
#13463=DIRECTION('ref_axis',(-1.,0.,0.));
#13464=DIRECTION('',(0.,0.,-1.));
#13465=DIRECTION('center_axis',(0.,0.,1.));
#13466=DIRECTION('ref_axis',(-1.,0.,0.));
#13467=DIRECTION('center_axis',(0.,0.,-1.));
#13468=DIRECTION('ref_axis',(-1.,0.,0.));
#13469=DIRECTION('center_axis',(0.,0.,-1.));
#13470=DIRECTION('ref_axis',(-1.,0.,0.));
#13471=DIRECTION('',(0.,0.,-1.));
#13472=DIRECTION('center_axis',(0.,0.,1.));
#13473=DIRECTION('ref_axis',(-1.,0.,0.));
#13474=DIRECTION('center_axis',(0.,0.,-1.));
#13475=DIRECTION('ref_axis',(-1.,0.,0.));
#13476=DIRECTION('center_axis',(0.,0.,-1.));
#13477=DIRECTION('ref_axis',(-1.,0.,0.));
#13478=DIRECTION('',(0.,0.,-1.));
#13479=DIRECTION('center_axis',(0.,0.,1.));
#13480=DIRECTION('ref_axis',(-1.,0.,0.));
#13481=DIRECTION('center_axis',(0.,0.,-1.));
#13482=DIRECTION('ref_axis',(-1.,0.,0.));
#13483=DIRECTION('center_axis',(0.,0.,-1.));
#13484=DIRECTION('ref_axis',(-1.,0.,0.));
#13485=DIRECTION('',(0.,0.,-1.));
#13486=DIRECTION('center_axis',(0.,0.,1.));
#13487=DIRECTION('ref_axis',(-1.,0.,0.));
#13488=DIRECTION('center_axis',(0.,0.,-1.));
#13489=DIRECTION('ref_axis',(-1.,0.,0.));
#13490=DIRECTION('center_axis',(0.,0.,-1.));
#13491=DIRECTION('ref_axis',(-1.,0.,0.));
#13492=DIRECTION('',(0.,0.,-1.));
#13493=DIRECTION('center_axis',(0.,0.,1.));
#13494=DIRECTION('ref_axis',(-1.,0.,0.));
#13495=DIRECTION('center_axis',(-1.,0.,0.));
#13496=DIRECTION('ref_axis',(0.,1.,0.));
#13497=DIRECTION('',(0.,-1.,0.));
#13498=DIRECTION('',(0.,0.,-1.));
#13499=DIRECTION('',(0.,1.,0.));
#13500=DIRECTION('',(0.,0.,-1.));
#13501=DIRECTION('center_axis',(0.,0.,-1.));
#13502=DIRECTION('ref_axis',(-1.,0.,0.));
#13503=DIRECTION('center_axis',(0.,0.,1.));
#13504=DIRECTION('ref_axis',(-1.,0.,0.));
#13505=DIRECTION('center_axis',(0.,0.,-1.));
#13506=DIRECTION('ref_axis',(-1.,0.,0.));
#13507=DIRECTION('',(0.,0.,-1.));
#13508=DIRECTION('center_axis',(1.,0.,0.));
#13509=DIRECTION('ref_axis',(0.,-1.,0.));
#13510=DIRECTION('',(0.,1.,0.));
#13511=DIRECTION('',(0.,-1.,0.));
#13512=DIRECTION('',(0.,0.,-1.));
#13513=DIRECTION('center_axis',(0.,0.,-1.));
#13514=DIRECTION('ref_axis',(1.,0.,0.));
#13515=DIRECTION('center_axis',(0.,0.,1.));
#13516=DIRECTION('ref_axis',(1.,0.,0.));
#13517=DIRECTION('center_axis',(0.,0.,-1.));
#13518=DIRECTION('ref_axis',(1.,0.,0.));
#13519=DIRECTION('center_axis',(-1.,0.,0.));
#13520=DIRECTION('ref_axis',(0.,1.,0.));
#13521=DIRECTION('',(0.,-1.,0.));
#13522=DIRECTION('',(0.,0.,-1.));
#13523=DIRECTION('',(0.,1.,0.));
#13524=DIRECTION('',(0.,0.,-1.));
#13525=DIRECTION('center_axis',(0.,0.,-1.));
#13526=DIRECTION('ref_axis',(-1.,0.,0.));
#13527=DIRECTION('center_axis',(0.,0.,1.));
#13528=DIRECTION('ref_axis',(-1.,0.,0.));
#13529=DIRECTION('center_axis',(0.,0.,-1.));
#13530=DIRECTION('ref_axis',(-1.,0.,0.));
#13531=DIRECTION('',(0.,0.,-1.));
#13532=DIRECTION('center_axis',(1.,0.,0.));
#13533=DIRECTION('ref_axis',(0.,-1.,0.));
#13534=DIRECTION('',(0.,1.,0.));
#13535=DIRECTION('',(0.,-1.,0.));
#13536=DIRECTION('',(0.,0.,-1.));
#13537=DIRECTION('center_axis',(0.,0.,-1.));
#13538=DIRECTION('ref_axis',(1.,0.,0.));
#13539=DIRECTION('center_axis',(0.,0.,1.));
#13540=DIRECTION('ref_axis',(1.,0.,0.));
#13541=DIRECTION('center_axis',(0.,0.,-1.));
#13542=DIRECTION('ref_axis',(1.,0.,0.));
#13543=DIRECTION('center_axis',(0.,0.,-1.));
#13544=DIRECTION('ref_axis',(-1.,0.,0.));
#13545=DIRECTION('center_axis',(0.,0.,-1.));
#13546=DIRECTION('ref_axis',(-1.,0.,0.));
#13547=DIRECTION('',(0.,0.,-1.));
#13548=DIRECTION('center_axis',(0.,0.,1.));
#13549=DIRECTION('ref_axis',(-1.,0.,0.));
#13550=DIRECTION('center_axis',(0.,0.,-1.));
#13551=DIRECTION('ref_axis',(-1.,0.,0.));
#13552=DIRECTION('center_axis',(0.,0.,-1.));
#13553=DIRECTION('ref_axis',(-1.,0.,0.));
#13554=DIRECTION('',(0.,0.,-1.));
#13555=DIRECTION('center_axis',(0.,0.,1.));
#13556=DIRECTION('ref_axis',(-1.,0.,0.));
#13557=DIRECTION('center_axis',(0.,0.,-1.));
#13558=DIRECTION('ref_axis',(-1.,0.,0.));
#13559=DIRECTION('center_axis',(0.,0.,-1.));
#13560=DIRECTION('ref_axis',(-1.,0.,0.));
#13561=DIRECTION('',(0.,0.,-1.));
#13562=DIRECTION('center_axis',(0.,0.,1.));
#13563=DIRECTION('ref_axis',(-1.,0.,0.));
#13564=DIRECTION('center_axis',(0.,0.,-1.));
#13565=DIRECTION('ref_axis',(-1.,0.,0.));
#13566=DIRECTION('center_axis',(0.,0.,-1.));
#13567=DIRECTION('ref_axis',(-1.,0.,0.));
#13568=DIRECTION('',(0.,0.,-1.));
#13569=DIRECTION('center_axis',(0.,0.,1.));
#13570=DIRECTION('ref_axis',(-1.,0.,0.));
#13571=DIRECTION('center_axis',(0.,0.,-1.));
#13572=DIRECTION('ref_axis',(-1.,0.,0.));
#13573=DIRECTION('center_axis',(0.,0.,-1.));
#13574=DIRECTION('ref_axis',(-1.,0.,0.));
#13575=DIRECTION('',(0.,0.,-1.));
#13576=DIRECTION('center_axis',(0.,0.,1.));
#13577=DIRECTION('ref_axis',(-1.,0.,0.));
#13578=DIRECTION('center_axis',(-1.,0.,0.));
#13579=DIRECTION('ref_axis',(0.,1.,0.));
#13580=DIRECTION('',(0.,-1.,0.));
#13581=DIRECTION('',(0.,0.,-1.));
#13582=DIRECTION('',(0.,1.,0.));
#13583=DIRECTION('',(0.,0.,-1.));
#13584=DIRECTION('center_axis',(0.,0.,-1.));
#13585=DIRECTION('ref_axis',(-1.,0.,0.));
#13586=DIRECTION('center_axis',(0.,0.,1.));
#13587=DIRECTION('ref_axis',(-1.,0.,0.));
#13588=DIRECTION('center_axis',(0.,0.,-1.));
#13589=DIRECTION('ref_axis',(-1.,0.,0.));
#13590=DIRECTION('',(0.,0.,-1.));
#13591=DIRECTION('center_axis',(1.,0.,0.));
#13592=DIRECTION('ref_axis',(0.,-1.,0.));
#13593=DIRECTION('',(0.,1.,0.));
#13594=DIRECTION('',(0.,-1.,0.));
#13595=DIRECTION('',(0.,0.,-1.));
#13596=DIRECTION('center_axis',(0.,0.,-1.));
#13597=DIRECTION('ref_axis',(1.,0.,0.));
#13598=DIRECTION('center_axis',(0.,0.,1.));
#13599=DIRECTION('ref_axis',(1.,0.,0.));
#13600=DIRECTION('center_axis',(0.,0.,-1.));
#13601=DIRECTION('ref_axis',(1.,0.,0.));
#13602=DIRECTION('center_axis',(-1.,0.,0.));
#13603=DIRECTION('ref_axis',(0.,1.,0.));
#13604=DIRECTION('',(0.,-1.,0.));
#13605=DIRECTION('',(0.,0.,-1.));
#13606=DIRECTION('',(0.,1.,0.));
#13607=DIRECTION('',(0.,0.,-1.));
#13608=DIRECTION('center_axis',(0.,0.,-1.));
#13609=DIRECTION('ref_axis',(-1.,0.,0.));
#13610=DIRECTION('center_axis',(0.,0.,1.));
#13611=DIRECTION('ref_axis',(-1.,0.,0.));
#13612=DIRECTION('center_axis',(0.,0.,-1.));
#13613=DIRECTION('ref_axis',(-1.,0.,0.));
#13614=DIRECTION('',(0.,0.,-1.));
#13615=DIRECTION('center_axis',(1.,0.,0.));
#13616=DIRECTION('ref_axis',(0.,-1.,0.));
#13617=DIRECTION('',(0.,1.,0.));
#13618=DIRECTION('',(0.,-1.,0.));
#13619=DIRECTION('',(0.,0.,-1.));
#13620=DIRECTION('center_axis',(0.,0.,-1.));
#13621=DIRECTION('ref_axis',(1.,0.,0.));
#13622=DIRECTION('center_axis',(0.,0.,1.));
#13623=DIRECTION('ref_axis',(1.,0.,0.));
#13624=DIRECTION('center_axis',(0.,0.,-1.));
#13625=DIRECTION('ref_axis',(1.,0.,0.));
#13626=DIRECTION('center_axis',(0.,0.,-1.));
#13627=DIRECTION('ref_axis',(-1.,0.,0.));
#13628=DIRECTION('center_axis',(0.,0.,-1.));
#13629=DIRECTION('ref_axis',(-1.,0.,0.));
#13630=DIRECTION('',(0.,0.,-1.));
#13631=DIRECTION('center_axis',(0.,0.,1.));
#13632=DIRECTION('ref_axis',(-1.,0.,0.));
#13633=DIRECTION('center_axis',(0.,0.,-1.));
#13634=DIRECTION('ref_axis',(-1.,0.,0.));
#13635=DIRECTION('center_axis',(0.,0.,-1.));
#13636=DIRECTION('ref_axis',(-1.,0.,0.));
#13637=DIRECTION('',(0.,0.,-1.));
#13638=DIRECTION('center_axis',(0.,0.,1.));
#13639=DIRECTION('ref_axis',(-1.,0.,0.));
#13640=DIRECTION('center_axis',(0.,0.,-1.));
#13641=DIRECTION('ref_axis',(-1.,0.,0.));
#13642=DIRECTION('center_axis',(0.,0.,-1.));
#13643=DIRECTION('ref_axis',(-1.,0.,0.));
#13644=DIRECTION('',(0.,0.,-1.));
#13645=DIRECTION('center_axis',(0.,0.,1.));
#13646=DIRECTION('ref_axis',(-1.,0.,0.));
#13647=DIRECTION('center_axis',(0.,0.,-1.));
#13648=DIRECTION('ref_axis',(-1.,0.,0.));
#13649=DIRECTION('center_axis',(0.,0.,-1.));
#13650=DIRECTION('ref_axis',(-1.,0.,0.));
#13651=DIRECTION('',(0.,0.,-1.));
#13652=DIRECTION('center_axis',(0.,0.,1.));
#13653=DIRECTION('ref_axis',(-1.,0.,0.));
#13654=DIRECTION('center_axis',(0.,0.,-1.));
#13655=DIRECTION('ref_axis',(-1.,0.,0.));
#13656=DIRECTION('center_axis',(0.,0.,-1.));
#13657=DIRECTION('ref_axis',(-1.,0.,0.));
#13658=DIRECTION('',(0.,0.,-1.));
#13659=DIRECTION('center_axis',(0.,0.,1.));
#13660=DIRECTION('ref_axis',(-1.,0.,0.));
#13661=DIRECTION('center_axis',(-1.,0.,0.));
#13662=DIRECTION('ref_axis',(0.,1.,0.));
#13663=DIRECTION('',(0.,-1.,0.));
#13664=DIRECTION('',(0.,0.,-1.));
#13665=DIRECTION('',(0.,1.,0.));
#13666=DIRECTION('',(0.,0.,-1.));
#13667=DIRECTION('center_axis',(0.,0.,-1.));
#13668=DIRECTION('ref_axis',(-1.,0.,0.));
#13669=DIRECTION('center_axis',(0.,0.,1.));
#13670=DIRECTION('ref_axis',(-1.,0.,0.));
#13671=DIRECTION('center_axis',(0.,0.,-1.));
#13672=DIRECTION('ref_axis',(-1.,0.,0.));
#13673=DIRECTION('',(0.,0.,-1.));
#13674=DIRECTION('center_axis',(1.,0.,0.));
#13675=DIRECTION('ref_axis',(0.,-1.,0.));
#13676=DIRECTION('',(0.,1.,0.));
#13677=DIRECTION('',(0.,-1.,0.));
#13678=DIRECTION('',(0.,0.,-1.));
#13679=DIRECTION('center_axis',(0.,0.,-1.));
#13680=DIRECTION('ref_axis',(1.,0.,0.));
#13681=DIRECTION('center_axis',(0.,0.,1.));
#13682=DIRECTION('ref_axis',(1.,0.,0.));
#13683=DIRECTION('center_axis',(0.,0.,-1.));
#13684=DIRECTION('ref_axis',(1.,0.,0.));
#13685=DIRECTION('center_axis',(-1.,0.,0.));
#13686=DIRECTION('ref_axis',(0.,1.,0.));
#13687=DIRECTION('',(0.,-1.,0.));
#13688=DIRECTION('',(0.,0.,-1.));
#13689=DIRECTION('',(0.,1.,0.));
#13690=DIRECTION('',(0.,0.,-1.));
#13691=DIRECTION('center_axis',(0.,0.,-1.));
#13692=DIRECTION('ref_axis',(-1.,0.,0.));
#13693=DIRECTION('center_axis',(0.,0.,1.));
#13694=DIRECTION('ref_axis',(-1.,0.,0.));
#13695=DIRECTION('center_axis',(0.,0.,-1.));
#13696=DIRECTION('ref_axis',(-1.,0.,0.));
#13697=DIRECTION('',(0.,0.,-1.));
#13698=DIRECTION('center_axis',(1.,0.,0.));
#13699=DIRECTION('ref_axis',(0.,-1.,0.));
#13700=DIRECTION('',(0.,1.,0.));
#13701=DIRECTION('',(0.,-1.,0.));
#13702=DIRECTION('',(0.,0.,-1.));
#13703=DIRECTION('center_axis',(0.,0.,-1.));
#13704=DIRECTION('ref_axis',(1.,0.,0.));
#13705=DIRECTION('center_axis',(0.,0.,1.));
#13706=DIRECTION('ref_axis',(1.,0.,0.));
#13707=DIRECTION('center_axis',(0.,0.,-1.));
#13708=DIRECTION('ref_axis',(1.,0.,0.));
#13709=DIRECTION('center_axis',(0.,0.,-1.));
#13710=DIRECTION('ref_axis',(-1.,0.,0.));
#13711=DIRECTION('center_axis',(0.,0.,-1.));
#13712=DIRECTION('ref_axis',(-1.,0.,0.));
#13713=DIRECTION('',(0.,0.,-1.));
#13714=DIRECTION('center_axis',(0.,0.,1.));
#13715=DIRECTION('ref_axis',(-1.,0.,0.));
#13716=DIRECTION('center_axis',(0.,0.,-1.));
#13717=DIRECTION('ref_axis',(-1.,0.,0.));
#13718=DIRECTION('center_axis',(0.,0.,-1.));
#13719=DIRECTION('ref_axis',(-1.,0.,0.));
#13720=DIRECTION('',(0.,0.,-1.));
#13721=DIRECTION('center_axis',(0.,0.,1.));
#13722=DIRECTION('ref_axis',(-1.,0.,0.));
#13723=DIRECTION('center_axis',(0.,0.,-1.));
#13724=DIRECTION('ref_axis',(-1.,0.,0.));
#13725=DIRECTION('center_axis',(0.,0.,-1.));
#13726=DIRECTION('ref_axis',(-1.,0.,0.));
#13727=DIRECTION('',(0.,0.,-1.));
#13728=DIRECTION('center_axis',(0.,0.,1.));
#13729=DIRECTION('ref_axis',(-1.,0.,0.));
#13730=DIRECTION('center_axis',(0.,0.,-1.));
#13731=DIRECTION('ref_axis',(-1.,0.,0.));
#13732=DIRECTION('center_axis',(0.,0.,-1.));
#13733=DIRECTION('ref_axis',(-1.,0.,0.));
#13734=DIRECTION('',(0.,0.,-1.));
#13735=DIRECTION('center_axis',(0.,0.,1.));
#13736=DIRECTION('ref_axis',(-1.,0.,0.));
#13737=DIRECTION('center_axis',(0.,0.,-1.));
#13738=DIRECTION('ref_axis',(-1.,0.,0.));
#13739=DIRECTION('center_axis',(0.,0.,-1.));
#13740=DIRECTION('ref_axis',(-1.,0.,0.));
#13741=DIRECTION('',(0.,0.,-1.));
#13742=DIRECTION('center_axis',(0.,0.,1.));
#13743=DIRECTION('ref_axis',(-1.,0.,0.));
#13744=DIRECTION('center_axis',(-1.,0.,0.));
#13745=DIRECTION('ref_axis',(0.,1.,0.));
#13746=DIRECTION('',(0.,-1.,0.));
#13747=DIRECTION('',(0.,0.,-1.));
#13748=DIRECTION('',(0.,1.,0.));
#13749=DIRECTION('',(0.,0.,-1.));
#13750=DIRECTION('center_axis',(0.,0.,-1.));
#13751=DIRECTION('ref_axis',(-1.,0.,0.));
#13752=DIRECTION('center_axis',(0.,0.,1.));
#13753=DIRECTION('ref_axis',(-1.,0.,0.));
#13754=DIRECTION('center_axis',(0.,0.,-1.));
#13755=DIRECTION('ref_axis',(-1.,0.,0.));
#13756=DIRECTION('',(0.,0.,-1.));
#13757=DIRECTION('center_axis',(1.,0.,0.));
#13758=DIRECTION('ref_axis',(0.,-1.,0.));
#13759=DIRECTION('',(0.,1.,0.));
#13760=DIRECTION('',(0.,-1.,0.));
#13761=DIRECTION('',(0.,0.,-1.));
#13762=DIRECTION('center_axis',(0.,0.,-1.));
#13763=DIRECTION('ref_axis',(1.,0.,0.));
#13764=DIRECTION('center_axis',(0.,0.,1.));
#13765=DIRECTION('ref_axis',(1.,0.,0.));
#13766=DIRECTION('center_axis',(0.,0.,-1.));
#13767=DIRECTION('ref_axis',(1.,0.,0.));
#13768=DIRECTION('center_axis',(-1.,0.,0.));
#13769=DIRECTION('ref_axis',(0.,1.,0.));
#13770=DIRECTION('',(0.,-1.,0.));
#13771=DIRECTION('',(0.,0.,-1.));
#13772=DIRECTION('',(0.,1.,0.));
#13773=DIRECTION('',(0.,0.,-1.));
#13774=DIRECTION('center_axis',(0.,0.,-1.));
#13775=DIRECTION('ref_axis',(-1.,0.,0.));
#13776=DIRECTION('center_axis',(0.,0.,1.));
#13777=DIRECTION('ref_axis',(-1.,0.,0.));
#13778=DIRECTION('center_axis',(0.,0.,-1.));
#13779=DIRECTION('ref_axis',(-1.,0.,0.));
#13780=DIRECTION('',(0.,0.,-1.));
#13781=DIRECTION('center_axis',(1.,0.,0.));
#13782=DIRECTION('ref_axis',(0.,-1.,0.));
#13783=DIRECTION('',(0.,1.,0.));
#13784=DIRECTION('',(0.,-1.,0.));
#13785=DIRECTION('',(0.,0.,-1.));
#13786=DIRECTION('center_axis',(0.,0.,-1.));
#13787=DIRECTION('ref_axis',(1.,0.,0.));
#13788=DIRECTION('center_axis',(0.,0.,1.));
#13789=DIRECTION('ref_axis',(1.,0.,0.));
#13790=DIRECTION('center_axis',(0.,0.,-1.));
#13791=DIRECTION('ref_axis',(1.,0.,0.));
#13792=DIRECTION('center_axis',(0.,0.,-1.));
#13793=DIRECTION('ref_axis',(-1.,0.,0.));
#13794=DIRECTION('center_axis',(0.,0.,-1.));
#13795=DIRECTION('ref_axis',(-1.,0.,0.));
#13796=DIRECTION('',(0.,0.,-1.));
#13797=DIRECTION('center_axis',(0.,0.,1.));
#13798=DIRECTION('ref_axis',(-1.,0.,0.));
#13799=DIRECTION('center_axis',(0.,0.,-1.));
#13800=DIRECTION('ref_axis',(-1.,0.,0.));
#13801=DIRECTION('center_axis',(0.,0.,-1.));
#13802=DIRECTION('ref_axis',(-1.,0.,0.));
#13803=DIRECTION('',(0.,0.,-1.));
#13804=DIRECTION('center_axis',(0.,0.,1.));
#13805=DIRECTION('ref_axis',(-1.,0.,0.));
#13806=DIRECTION('center_axis',(0.,0.,-1.));
#13807=DIRECTION('ref_axis',(-1.,0.,0.));
#13808=DIRECTION('center_axis',(0.,0.,-1.));
#13809=DIRECTION('ref_axis',(-1.,0.,0.));
#13810=DIRECTION('',(0.,0.,-1.));
#13811=DIRECTION('center_axis',(0.,0.,1.));
#13812=DIRECTION('ref_axis',(-1.,0.,0.));
#13813=DIRECTION('center_axis',(0.,0.,-1.));
#13814=DIRECTION('ref_axis',(-1.,0.,0.));
#13815=DIRECTION('center_axis',(0.,0.,-1.));
#13816=DIRECTION('ref_axis',(-1.,0.,0.));
#13817=DIRECTION('',(0.,0.,-1.));
#13818=DIRECTION('center_axis',(0.,0.,1.));
#13819=DIRECTION('ref_axis',(-1.,0.,0.));
#13820=DIRECTION('center_axis',(0.,0.,-1.));
#13821=DIRECTION('ref_axis',(-1.,0.,0.));
#13822=DIRECTION('center_axis',(0.,0.,-1.));
#13823=DIRECTION('ref_axis',(-1.,0.,0.));
#13824=DIRECTION('',(0.,0.,-1.));
#13825=DIRECTION('center_axis',(0.,0.,1.));
#13826=DIRECTION('ref_axis',(-1.,0.,0.));
#13827=DIRECTION('center_axis',(-1.,0.,0.));
#13828=DIRECTION('ref_axis',(0.,1.,0.));
#13829=DIRECTION('',(0.,-1.,0.));
#13830=DIRECTION('',(0.,0.,-1.));
#13831=DIRECTION('',(0.,1.,0.));
#13832=DIRECTION('',(0.,0.,-1.));
#13833=DIRECTION('center_axis',(0.,0.,-1.));
#13834=DIRECTION('ref_axis',(-1.,0.,0.));
#13835=DIRECTION('center_axis',(0.,0.,1.));
#13836=DIRECTION('ref_axis',(-1.,0.,0.));
#13837=DIRECTION('center_axis',(0.,0.,-1.));
#13838=DIRECTION('ref_axis',(-1.,0.,0.));
#13839=DIRECTION('',(0.,0.,-1.));
#13840=DIRECTION('center_axis',(1.,0.,0.));
#13841=DIRECTION('ref_axis',(0.,-1.,0.));
#13842=DIRECTION('',(0.,1.,0.));
#13843=DIRECTION('',(0.,-1.,0.));
#13844=DIRECTION('',(0.,0.,-1.));
#13845=DIRECTION('center_axis',(0.,0.,-1.));
#13846=DIRECTION('ref_axis',(1.,0.,0.));
#13847=DIRECTION('center_axis',(0.,0.,1.));
#13848=DIRECTION('ref_axis',(1.,0.,0.));
#13849=DIRECTION('center_axis',(0.,0.,-1.));
#13850=DIRECTION('ref_axis',(1.,0.,0.));
#13851=DIRECTION('center_axis',(-1.,0.,0.));
#13852=DIRECTION('ref_axis',(0.,1.,0.));
#13853=DIRECTION('',(0.,-1.,0.));
#13854=DIRECTION('',(0.,0.,-1.));
#13855=DIRECTION('',(0.,1.,0.));
#13856=DIRECTION('',(0.,0.,-1.));
#13857=DIRECTION('center_axis',(0.,0.,-1.));
#13858=DIRECTION('ref_axis',(-1.,0.,0.));
#13859=DIRECTION('center_axis',(0.,0.,1.));
#13860=DIRECTION('ref_axis',(-1.,0.,0.));
#13861=DIRECTION('center_axis',(0.,0.,-1.));
#13862=DIRECTION('ref_axis',(-1.,0.,0.));
#13863=DIRECTION('',(0.,0.,-1.));
#13864=DIRECTION('center_axis',(1.,0.,0.));
#13865=DIRECTION('ref_axis',(0.,-1.,0.));
#13866=DIRECTION('',(0.,1.,0.));
#13867=DIRECTION('',(0.,-1.,0.));
#13868=DIRECTION('',(0.,0.,-1.));
#13869=DIRECTION('center_axis',(0.,0.,-1.));
#13870=DIRECTION('ref_axis',(1.,0.,0.));
#13871=DIRECTION('center_axis',(0.,0.,1.));
#13872=DIRECTION('ref_axis',(1.,0.,0.));
#13873=DIRECTION('center_axis',(0.,0.,-1.));
#13874=DIRECTION('ref_axis',(1.,0.,0.));
#13875=DIRECTION('center_axis',(0.,0.,-1.));
#13876=DIRECTION('ref_axis',(-1.,0.,0.));
#13877=DIRECTION('center_axis',(0.,0.,-1.));
#13878=DIRECTION('ref_axis',(-1.,0.,0.));
#13879=DIRECTION('',(0.,0.,-1.));
#13880=DIRECTION('center_axis',(0.,0.,1.));
#13881=DIRECTION('ref_axis',(-1.,0.,0.));
#13882=DIRECTION('center_axis',(0.,0.,-1.));
#13883=DIRECTION('ref_axis',(-1.,0.,0.));
#13884=DIRECTION('center_axis',(0.,0.,-1.));
#13885=DIRECTION('ref_axis',(-1.,0.,0.));
#13886=DIRECTION('',(0.,0.,-1.));
#13887=DIRECTION('center_axis',(0.,0.,1.));
#13888=DIRECTION('ref_axis',(-1.,0.,0.));
#13889=DIRECTION('center_axis',(0.,0.,-1.));
#13890=DIRECTION('ref_axis',(-1.,0.,0.));
#13891=DIRECTION('center_axis',(0.,0.,-1.));
#13892=DIRECTION('ref_axis',(-1.,0.,0.));
#13893=DIRECTION('',(0.,0.,-1.));
#13894=DIRECTION('center_axis',(0.,0.,1.));
#13895=DIRECTION('ref_axis',(-1.,0.,0.));
#13896=DIRECTION('center_axis',(0.,0.,-1.));
#13897=DIRECTION('ref_axis',(-1.,0.,0.));
#13898=DIRECTION('center_axis',(0.,0.,-1.));
#13899=DIRECTION('ref_axis',(-1.,0.,0.));
#13900=DIRECTION('',(0.,0.,-1.));
#13901=DIRECTION('center_axis',(0.,0.,1.));
#13902=DIRECTION('ref_axis',(-1.,0.,0.));
#13903=DIRECTION('center_axis',(0.,0.,-1.));
#13904=DIRECTION('ref_axis',(-1.,0.,0.));
#13905=DIRECTION('center_axis',(0.,0.,-1.));
#13906=DIRECTION('ref_axis',(-1.,0.,0.));
#13907=DIRECTION('',(0.,0.,-1.));
#13908=DIRECTION('center_axis',(0.,0.,1.));
#13909=DIRECTION('ref_axis',(-1.,0.,0.));
#13910=DIRECTION('center_axis',(-1.,0.,0.));
#13911=DIRECTION('ref_axis',(0.,1.,0.));
#13912=DIRECTION('',(0.,-1.,0.));
#13913=DIRECTION('',(0.,0.,-1.));
#13914=DIRECTION('',(0.,1.,0.));
#13915=DIRECTION('',(0.,0.,-1.));
#13916=DIRECTION('center_axis',(0.,0.,-1.));
#13917=DIRECTION('ref_axis',(-1.,0.,0.));
#13918=DIRECTION('center_axis',(0.,0.,1.));
#13919=DIRECTION('ref_axis',(-1.,0.,0.));
#13920=DIRECTION('center_axis',(0.,0.,-1.));
#13921=DIRECTION('ref_axis',(-1.,0.,0.));
#13922=DIRECTION('',(0.,0.,-1.));
#13923=DIRECTION('center_axis',(1.,0.,0.));
#13924=DIRECTION('ref_axis',(0.,-1.,0.));
#13925=DIRECTION('',(0.,1.,0.));
#13926=DIRECTION('',(0.,-1.,0.));
#13927=DIRECTION('',(0.,0.,-1.));
#13928=DIRECTION('center_axis',(0.,0.,-1.));
#13929=DIRECTION('ref_axis',(1.,0.,0.));
#13930=DIRECTION('center_axis',(0.,0.,1.));
#13931=DIRECTION('ref_axis',(1.,0.,0.));
#13932=DIRECTION('center_axis',(0.,0.,-1.));
#13933=DIRECTION('ref_axis',(1.,0.,0.));
#13934=DIRECTION('center_axis',(-1.,0.,0.));
#13935=DIRECTION('ref_axis',(0.,1.,0.));
#13936=DIRECTION('',(0.,-1.,0.));
#13937=DIRECTION('',(0.,0.,-1.));
#13938=DIRECTION('',(0.,1.,0.));
#13939=DIRECTION('',(0.,0.,-1.));
#13940=DIRECTION('center_axis',(0.,0.,-1.));
#13941=DIRECTION('ref_axis',(-1.,0.,0.));
#13942=DIRECTION('center_axis',(0.,0.,1.));
#13943=DIRECTION('ref_axis',(-1.,0.,0.));
#13944=DIRECTION('center_axis',(0.,0.,-1.));
#13945=DIRECTION('ref_axis',(-1.,0.,0.));
#13946=DIRECTION('',(0.,0.,-1.));
#13947=DIRECTION('center_axis',(1.,0.,0.));
#13948=DIRECTION('ref_axis',(0.,-1.,0.));
#13949=DIRECTION('',(0.,1.,0.));
#13950=DIRECTION('',(0.,-1.,0.));
#13951=DIRECTION('',(0.,0.,-1.));
#13952=DIRECTION('center_axis',(0.,0.,-1.));
#13953=DIRECTION('ref_axis',(1.,0.,0.));
#13954=DIRECTION('center_axis',(0.,0.,1.));
#13955=DIRECTION('ref_axis',(1.,0.,0.));
#13956=DIRECTION('center_axis',(0.,0.,-1.));
#13957=DIRECTION('ref_axis',(1.,0.,0.));
#13958=DIRECTION('center_axis',(0.,0.,-1.));
#13959=DIRECTION('ref_axis',(-1.,0.,0.));
#13960=DIRECTION('center_axis',(0.,0.,-1.));
#13961=DIRECTION('ref_axis',(-1.,0.,0.));
#13962=DIRECTION('',(0.,0.,-1.));
#13963=DIRECTION('center_axis',(0.,0.,1.));
#13964=DIRECTION('ref_axis',(-1.,0.,0.));
#13965=DIRECTION('center_axis',(0.,0.,-1.));
#13966=DIRECTION('ref_axis',(-1.,0.,0.));
#13967=DIRECTION('center_axis',(0.,0.,-1.));
#13968=DIRECTION('ref_axis',(-1.,0.,0.));
#13969=DIRECTION('',(0.,0.,-1.));
#13970=DIRECTION('center_axis',(0.,0.,1.));
#13971=DIRECTION('ref_axis',(-1.,0.,0.));
#13972=DIRECTION('center_axis',(0.,0.,-1.));
#13973=DIRECTION('ref_axis',(-1.,0.,0.));
#13974=DIRECTION('center_axis',(0.,0.,-1.));
#13975=DIRECTION('ref_axis',(-1.,0.,0.));
#13976=DIRECTION('',(0.,0.,-1.));
#13977=DIRECTION('center_axis',(0.,0.,1.));
#13978=DIRECTION('ref_axis',(-1.,0.,0.));
#13979=DIRECTION('center_axis',(0.,0.,-1.));
#13980=DIRECTION('ref_axis',(-1.,0.,0.));
#13981=DIRECTION('center_axis',(0.,0.,-1.));
#13982=DIRECTION('ref_axis',(-1.,0.,0.));
#13983=DIRECTION('',(0.,0.,-1.));
#13984=DIRECTION('center_axis',(0.,0.,1.));
#13985=DIRECTION('ref_axis',(-1.,0.,0.));
#13986=DIRECTION('center_axis',(0.,0.,-1.));
#13987=DIRECTION('ref_axis',(-1.,0.,0.));
#13988=DIRECTION('center_axis',(0.,0.,-1.));
#13989=DIRECTION('ref_axis',(-1.,0.,0.));
#13990=DIRECTION('',(0.,0.,-1.));
#13991=DIRECTION('center_axis',(0.,0.,1.));
#13992=DIRECTION('ref_axis',(-1.,0.,0.));
#13993=DIRECTION('center_axis',(-1.,0.,0.));
#13994=DIRECTION('ref_axis',(0.,1.,0.));
#13995=DIRECTION('',(0.,-1.,0.));
#13996=DIRECTION('',(0.,0.,-1.));
#13997=DIRECTION('',(0.,1.,0.));
#13998=DIRECTION('',(0.,0.,-1.));
#13999=DIRECTION('center_axis',(0.,0.,-1.));
#14000=DIRECTION('ref_axis',(-1.,0.,0.));
#14001=DIRECTION('center_axis',(0.,0.,1.));
#14002=DIRECTION('ref_axis',(-1.,0.,0.));
#14003=DIRECTION('center_axis',(0.,0.,-1.));
#14004=DIRECTION('ref_axis',(-1.,0.,0.));
#14005=DIRECTION('',(0.,0.,-1.));
#14006=DIRECTION('center_axis',(1.,0.,0.));
#14007=DIRECTION('ref_axis',(0.,-1.,0.));
#14008=DIRECTION('',(0.,1.,0.));
#14009=DIRECTION('',(0.,-1.,0.));
#14010=DIRECTION('',(0.,0.,-1.));
#14011=DIRECTION('center_axis',(0.,0.,-1.));
#14012=DIRECTION('ref_axis',(1.,0.,0.));
#14013=DIRECTION('center_axis',(0.,0.,1.));
#14014=DIRECTION('ref_axis',(1.,0.,0.));
#14015=DIRECTION('center_axis',(0.,0.,-1.));
#14016=DIRECTION('ref_axis',(1.,0.,0.));
#14017=DIRECTION('center_axis',(-1.,0.,0.));
#14018=DIRECTION('ref_axis',(0.,1.,0.));
#14019=DIRECTION('',(0.,-1.,0.));
#14020=DIRECTION('',(0.,0.,-1.));
#14021=DIRECTION('',(0.,1.,0.));
#14022=DIRECTION('',(0.,0.,-1.));
#14023=DIRECTION('center_axis',(0.,0.,-1.));
#14024=DIRECTION('ref_axis',(-1.,0.,0.));
#14025=DIRECTION('center_axis',(0.,0.,1.));
#14026=DIRECTION('ref_axis',(-1.,0.,0.));
#14027=DIRECTION('center_axis',(0.,0.,-1.));
#14028=DIRECTION('ref_axis',(-1.,0.,0.));
#14029=DIRECTION('',(0.,0.,-1.));
#14030=DIRECTION('center_axis',(1.,0.,0.));
#14031=DIRECTION('ref_axis',(0.,-1.,0.));
#14032=DIRECTION('',(0.,1.,0.));
#14033=DIRECTION('',(0.,-1.,0.));
#14034=DIRECTION('',(0.,0.,-1.));
#14035=DIRECTION('center_axis',(0.,0.,-1.));
#14036=DIRECTION('ref_axis',(1.,0.,0.));
#14037=DIRECTION('center_axis',(0.,0.,1.));
#14038=DIRECTION('ref_axis',(1.,0.,0.));
#14039=DIRECTION('center_axis',(0.,0.,-1.));
#14040=DIRECTION('ref_axis',(1.,0.,0.));
#14041=DIRECTION('center_axis',(0.,0.,-1.));
#14042=DIRECTION('ref_axis',(-1.,0.,0.));
#14043=DIRECTION('center_axis',(0.,0.,-1.));
#14044=DIRECTION('ref_axis',(-1.,0.,0.));
#14045=DIRECTION('',(0.,0.,-1.));
#14046=DIRECTION('center_axis',(0.,0.,1.));
#14047=DIRECTION('ref_axis',(-1.,0.,0.));
#14048=DIRECTION('center_axis',(0.,0.,-1.));
#14049=DIRECTION('ref_axis',(-1.,0.,0.));
#14050=DIRECTION('center_axis',(0.,0.,-1.));
#14051=DIRECTION('ref_axis',(-1.,0.,0.));
#14052=DIRECTION('',(0.,0.,-1.));
#14053=DIRECTION('center_axis',(0.,0.,1.));
#14054=DIRECTION('ref_axis',(-1.,0.,0.));
#14055=DIRECTION('center_axis',(0.,0.,-1.));
#14056=DIRECTION('ref_axis',(-1.,0.,0.));
#14057=DIRECTION('center_axis',(0.,0.,-1.));
#14058=DIRECTION('ref_axis',(-1.,0.,0.));
#14059=DIRECTION('',(0.,0.,-1.));
#14060=DIRECTION('center_axis',(0.,0.,1.));
#14061=DIRECTION('ref_axis',(-1.,0.,0.));
#14062=DIRECTION('center_axis',(0.,0.,-1.));
#14063=DIRECTION('ref_axis',(-1.,0.,0.));
#14064=DIRECTION('center_axis',(0.,0.,-1.));
#14065=DIRECTION('ref_axis',(-1.,0.,0.));
#14066=DIRECTION('',(0.,0.,-1.));
#14067=DIRECTION('center_axis',(0.,0.,1.));
#14068=DIRECTION('ref_axis',(-1.,0.,0.));
#14069=DIRECTION('center_axis',(0.,0.,-1.));
#14070=DIRECTION('ref_axis',(-1.,0.,0.));
#14071=DIRECTION('center_axis',(0.,0.,-1.));
#14072=DIRECTION('ref_axis',(-1.,0.,0.));
#14073=DIRECTION('',(0.,0.,-1.));
#14074=DIRECTION('center_axis',(0.,0.,1.));
#14075=DIRECTION('ref_axis',(-1.,0.,0.));
#14076=DIRECTION('center_axis',(-1.,0.,0.));
#14077=DIRECTION('ref_axis',(0.,1.,0.));
#14078=DIRECTION('',(0.,-1.,0.));
#14079=DIRECTION('',(0.,0.,-1.));
#14080=DIRECTION('',(0.,1.,0.));
#14081=DIRECTION('',(0.,0.,-1.));
#14082=DIRECTION('center_axis',(0.,0.,-1.));
#14083=DIRECTION('ref_axis',(-1.,0.,0.));
#14084=DIRECTION('center_axis',(0.,0.,1.));
#14085=DIRECTION('ref_axis',(-1.,0.,0.));
#14086=DIRECTION('center_axis',(0.,0.,-1.));
#14087=DIRECTION('ref_axis',(-1.,0.,0.));
#14088=DIRECTION('',(0.,0.,-1.));
#14089=DIRECTION('center_axis',(1.,0.,0.));
#14090=DIRECTION('ref_axis',(0.,-1.,0.));
#14091=DIRECTION('',(0.,1.,0.));
#14092=DIRECTION('',(0.,-1.,0.));
#14093=DIRECTION('',(0.,0.,-1.));
#14094=DIRECTION('center_axis',(0.,0.,-1.));
#14095=DIRECTION('ref_axis',(1.,0.,0.));
#14096=DIRECTION('center_axis',(0.,0.,1.));
#14097=DIRECTION('ref_axis',(1.,0.,0.));
#14098=DIRECTION('center_axis',(0.,0.,-1.));
#14099=DIRECTION('ref_axis',(1.,0.,0.));
#14100=DIRECTION('center_axis',(-1.,0.,0.));
#14101=DIRECTION('ref_axis',(0.,1.,0.));
#14102=DIRECTION('',(0.,-1.,0.));
#14103=DIRECTION('',(0.,0.,-1.));
#14104=DIRECTION('',(0.,1.,0.));
#14105=DIRECTION('',(0.,0.,-1.));
#14106=DIRECTION('center_axis',(0.,0.,-1.));
#14107=DIRECTION('ref_axis',(-1.,0.,0.));
#14108=DIRECTION('center_axis',(0.,0.,1.));
#14109=DIRECTION('ref_axis',(-1.,0.,0.));
#14110=DIRECTION('center_axis',(0.,0.,-1.));
#14111=DIRECTION('ref_axis',(-1.,0.,0.));
#14112=DIRECTION('',(0.,0.,-1.));
#14113=DIRECTION('center_axis',(1.,0.,0.));
#14114=DIRECTION('ref_axis',(0.,-1.,0.));
#14115=DIRECTION('',(0.,1.,0.));
#14116=DIRECTION('',(0.,-1.,0.));
#14117=DIRECTION('',(0.,0.,-1.));
#14118=DIRECTION('center_axis',(0.,0.,-1.));
#14119=DIRECTION('ref_axis',(1.,0.,0.));
#14120=DIRECTION('center_axis',(0.,0.,1.));
#14121=DIRECTION('ref_axis',(1.,0.,0.));
#14122=DIRECTION('center_axis',(0.,0.,-1.));
#14123=DIRECTION('ref_axis',(1.,0.,0.));
#14124=DIRECTION('center_axis',(0.,0.,-1.));
#14125=DIRECTION('ref_axis',(-1.,0.,0.));
#14126=DIRECTION('center_axis',(0.,0.,-1.));
#14127=DIRECTION('ref_axis',(-1.,0.,0.));
#14128=DIRECTION('',(0.,0.,-1.));
#14129=DIRECTION('center_axis',(0.,0.,1.));
#14130=DIRECTION('ref_axis',(-1.,0.,0.));
#14131=DIRECTION('center_axis',(0.,0.,-1.));
#14132=DIRECTION('ref_axis',(-1.,0.,0.));
#14133=DIRECTION('center_axis',(0.,0.,-1.));
#14134=DIRECTION('ref_axis',(-1.,0.,0.));
#14135=DIRECTION('',(0.,0.,-1.));
#14136=DIRECTION('center_axis',(0.,0.,1.));
#14137=DIRECTION('ref_axis',(-1.,0.,0.));
#14138=DIRECTION('center_axis',(0.,0.,-1.));
#14139=DIRECTION('ref_axis',(-1.,0.,0.));
#14140=DIRECTION('center_axis',(0.,0.,-1.));
#14141=DIRECTION('ref_axis',(-1.,0.,0.));
#14142=DIRECTION('',(0.,0.,-1.));
#14143=DIRECTION('center_axis',(0.,0.,1.));
#14144=DIRECTION('ref_axis',(-1.,0.,0.));
#14145=DIRECTION('center_axis',(0.,0.,-1.));
#14146=DIRECTION('ref_axis',(-1.,0.,0.));
#14147=DIRECTION('center_axis',(0.,0.,-1.));
#14148=DIRECTION('ref_axis',(-1.,0.,0.));
#14149=DIRECTION('',(0.,0.,-1.));
#14150=DIRECTION('center_axis',(0.,0.,1.));
#14151=DIRECTION('ref_axis',(-1.,0.,0.));
#14152=DIRECTION('center_axis',(0.,0.,-1.));
#14153=DIRECTION('ref_axis',(-1.,0.,0.));
#14154=DIRECTION('center_axis',(0.,0.,-1.));
#14155=DIRECTION('ref_axis',(-1.,0.,0.));
#14156=DIRECTION('',(0.,0.,-1.));
#14157=DIRECTION('center_axis',(0.,0.,1.));
#14158=DIRECTION('ref_axis',(-1.,0.,0.));
#14159=DIRECTION('center_axis',(-1.,0.,0.));
#14160=DIRECTION('ref_axis',(0.,1.,0.));
#14161=DIRECTION('',(0.,-1.,0.));
#14162=DIRECTION('',(0.,0.,-1.));
#14163=DIRECTION('',(0.,1.,0.));
#14164=DIRECTION('',(0.,0.,-1.));
#14165=DIRECTION('center_axis',(0.,0.,-1.));
#14166=DIRECTION('ref_axis',(-1.,0.,0.));
#14167=DIRECTION('center_axis',(0.,0.,1.));
#14168=DIRECTION('ref_axis',(-1.,0.,0.));
#14169=DIRECTION('center_axis',(0.,0.,-1.));
#14170=DIRECTION('ref_axis',(-1.,0.,0.));
#14171=DIRECTION('',(0.,0.,-1.));
#14172=DIRECTION('center_axis',(1.,0.,0.));
#14173=DIRECTION('ref_axis',(0.,-1.,0.));
#14174=DIRECTION('',(0.,1.,0.));
#14175=DIRECTION('',(0.,-1.,0.));
#14176=DIRECTION('',(0.,0.,-1.));
#14177=DIRECTION('center_axis',(0.,0.,-1.));
#14178=DIRECTION('ref_axis',(1.,0.,0.));
#14179=DIRECTION('center_axis',(0.,0.,1.));
#14180=DIRECTION('ref_axis',(1.,0.,0.));
#14181=DIRECTION('center_axis',(0.,0.,-1.));
#14182=DIRECTION('ref_axis',(1.,0.,0.));
#14183=DIRECTION('center_axis',(-1.,0.,0.));
#14184=DIRECTION('ref_axis',(0.,1.,0.));
#14185=DIRECTION('',(0.,-1.,0.));
#14186=DIRECTION('',(0.,0.,-1.));
#14187=DIRECTION('',(0.,1.,0.));
#14188=DIRECTION('',(0.,0.,-1.));
#14189=DIRECTION('center_axis',(0.,0.,-1.));
#14190=DIRECTION('ref_axis',(-1.,0.,0.));
#14191=DIRECTION('center_axis',(0.,0.,1.));
#14192=DIRECTION('ref_axis',(-1.,0.,0.));
#14193=DIRECTION('center_axis',(0.,0.,-1.));
#14194=DIRECTION('ref_axis',(-1.,0.,0.));
#14195=DIRECTION('',(0.,0.,-1.));
#14196=DIRECTION('center_axis',(1.,0.,0.));
#14197=DIRECTION('ref_axis',(0.,-1.,0.));
#14198=DIRECTION('',(0.,1.,0.));
#14199=DIRECTION('',(0.,-1.,0.));
#14200=DIRECTION('',(0.,0.,-1.));
#14201=DIRECTION('center_axis',(0.,0.,-1.));
#14202=DIRECTION('ref_axis',(1.,0.,0.));
#14203=DIRECTION('center_axis',(0.,0.,1.));
#14204=DIRECTION('ref_axis',(1.,0.,0.));
#14205=DIRECTION('center_axis',(0.,0.,-1.));
#14206=DIRECTION('ref_axis',(1.,0.,0.));
#14207=DIRECTION('center_axis',(0.,0.,-1.));
#14208=DIRECTION('ref_axis',(-1.,0.,0.));
#14209=DIRECTION('center_axis',(0.,0.,-1.));
#14210=DIRECTION('ref_axis',(-1.,0.,0.));
#14211=DIRECTION('',(0.,0.,-1.));
#14212=DIRECTION('center_axis',(0.,0.,1.));
#14213=DIRECTION('ref_axis',(-1.,0.,0.));
#14214=DIRECTION('center_axis',(0.,0.,-1.));
#14215=DIRECTION('ref_axis',(-1.,0.,0.));
#14216=DIRECTION('center_axis',(0.,0.,-1.));
#14217=DIRECTION('ref_axis',(-1.,0.,0.));
#14218=DIRECTION('',(0.,0.,-1.));
#14219=DIRECTION('center_axis',(0.,0.,1.));
#14220=DIRECTION('ref_axis',(-1.,0.,0.));
#14221=DIRECTION('center_axis',(-1.,0.,0.));
#14222=DIRECTION('ref_axis',(0.,1.,0.));
#14223=DIRECTION('',(0.,-1.,0.));
#14224=DIRECTION('',(0.,0.,-1.));
#14225=DIRECTION('',(0.,1.,0.));
#14226=DIRECTION('',(0.,0.,-1.));
#14227=DIRECTION('center_axis',(0.,0.,-1.));
#14228=DIRECTION('ref_axis',(-1.,0.,0.));
#14229=DIRECTION('center_axis',(0.,0.,1.));
#14230=DIRECTION('ref_axis',(-1.,0.,0.));
#14231=DIRECTION('center_axis',(0.,0.,-1.));
#14232=DIRECTION('ref_axis',(-1.,0.,0.));
#14233=DIRECTION('',(0.,0.,-1.));
#14234=DIRECTION('center_axis',(1.,0.,0.));
#14235=DIRECTION('ref_axis',(0.,-1.,0.));
#14236=DIRECTION('',(0.,1.,0.));
#14237=DIRECTION('',(0.,-1.,0.));
#14238=DIRECTION('',(0.,0.,-1.));
#14239=DIRECTION('center_axis',(0.,0.,-1.));
#14240=DIRECTION('ref_axis',(1.,0.,0.));
#14241=DIRECTION('center_axis',(0.,0.,1.));
#14242=DIRECTION('ref_axis',(1.,0.,0.));
#14243=DIRECTION('center_axis',(0.,0.,-1.));
#14244=DIRECTION('ref_axis',(1.,0.,0.));
#14245=DIRECTION('center_axis',(-1.,0.,0.));
#14246=DIRECTION('ref_axis',(0.,1.,0.));
#14247=DIRECTION('',(0.,-1.,0.));
#14248=DIRECTION('',(0.,0.,-1.));
#14249=DIRECTION('',(0.,1.,0.));
#14250=DIRECTION('',(0.,0.,-1.));
#14251=DIRECTION('center_axis',(0.,0.,-1.));
#14252=DIRECTION('ref_axis',(-1.,0.,0.));
#14253=DIRECTION('center_axis',(0.,0.,1.));
#14254=DIRECTION('ref_axis',(-1.,0.,0.));
#14255=DIRECTION('center_axis',(0.,0.,-1.));
#14256=DIRECTION('ref_axis',(-1.,0.,0.));
#14257=DIRECTION('',(0.,0.,-1.));
#14258=DIRECTION('center_axis',(1.,0.,0.));
#14259=DIRECTION('ref_axis',(0.,-1.,0.));
#14260=DIRECTION('',(0.,1.,0.));
#14261=DIRECTION('',(0.,-1.,0.));
#14262=DIRECTION('',(0.,0.,-1.));
#14263=DIRECTION('center_axis',(0.,0.,-1.));
#14264=DIRECTION('ref_axis',(1.,0.,0.));
#14265=DIRECTION('center_axis',(0.,0.,1.));
#14266=DIRECTION('ref_axis',(1.,0.,0.));
#14267=DIRECTION('center_axis',(0.,0.,-1.));
#14268=DIRECTION('ref_axis',(1.,0.,0.));
#14269=DIRECTION('center_axis',(0.,0.,-1.));
#14270=DIRECTION('ref_axis',(-1.,0.,0.));
#14271=DIRECTION('center_axis',(0.,0.,-1.));
#14272=DIRECTION('ref_axis',(-1.,0.,0.));
#14273=DIRECTION('',(0.,0.,-1.));
#14274=DIRECTION('center_axis',(0.,0.,1.));
#14275=DIRECTION('ref_axis',(-1.,0.,0.));
#14276=DIRECTION('center_axis',(0.,0.,-1.));
#14277=DIRECTION('ref_axis',(-1.,0.,0.));
#14278=DIRECTION('center_axis',(0.,0.,-1.));
#14279=DIRECTION('ref_axis',(-1.,0.,0.));
#14280=DIRECTION('',(0.,0.,-1.));
#14281=DIRECTION('center_axis',(0.,0.,1.));
#14282=DIRECTION('ref_axis',(-1.,0.,0.));
#14283=DIRECTION('center_axis',(0.,0.,-1.));
#14284=DIRECTION('ref_axis',(-1.,0.,0.));
#14285=DIRECTION('center_axis',(0.,0.,-1.));
#14286=DIRECTION('ref_axis',(-1.,0.,0.));
#14287=DIRECTION('',(0.,0.,-1.));
#14288=DIRECTION('center_axis',(0.,0.,1.));
#14289=DIRECTION('ref_axis',(-1.,0.,0.));
#14290=DIRECTION('center_axis',(1.,0.,0.));
#14291=DIRECTION('ref_axis',(0.,-0.707106781186547,0.707106781186548));
#14292=DIRECTION('center_axis',(-1.,0.,0.));
#14293=DIRECTION('ref_axis',(0.,-0.707106781186547,0.707106781186548));
#14294=DIRECTION('',(1.,0.,0.));
#14295=DIRECTION('center_axis',(1.,0.,0.));
#14296=DIRECTION('ref_axis',(0.,-0.707106781186547,0.707106781186548));
#14297=DIRECTION('',(-1.,0.,0.));
#14298=DIRECTION('center_axis',(0.,0.,-1.));
#14299=DIRECTION('ref_axis',(-1.,0.,0.));
#14300=DIRECTION('',(0.,1.,0.));
#14301=DIRECTION('',(-1.,0.,0.));
#14302=DIRECTION('',(0.,1.,0.));
#14303=DIRECTION('center_axis',(1.,0.,0.));
#14304=DIRECTION('ref_axis',(0.,0.70710678118654,0.707106781186555));
#14305=DIRECTION('center_axis',(-1.,0.,0.));
#14306=DIRECTION('ref_axis',(0.,0.70710678118654,0.707106781186555));
#14307=DIRECTION('',(1.,0.,0.));
#14308=DIRECTION('center_axis',(1.,0.,0.));
#14309=DIRECTION('ref_axis',(0.,0.70710678118654,0.707106781186555));
#14310=DIRECTION('center_axis',(0.,1.,0.));
#14311=DIRECTION('ref_axis',(1.,0.,0.));
#14312=DIRECTION('',(0.,0.,-1.));
#14313=DIRECTION('',(1.,0.,0.));
#14314=DIRECTION('',(0.,0.,1.));
#14315=DIRECTION('center_axis',(0.,-1.,0.));
#14316=DIRECTION('ref_axis',(1.,0.,0.));
#14317=DIRECTION('center_axis',(0.,-1.,0.));
#14318=DIRECTION('ref_axis',(1.,0.,0.));
#14319=DIRECTION('center_axis',(0.,-1.,0.));
#14320=DIRECTION('ref_axis',(1.,0.,0.));
#14321=DIRECTION('center_axis',(0.,-1.,0.));
#14322=DIRECTION('ref_axis',(1.,0.,0.));
#14323=DIRECTION('center_axis',(0.,-1.,0.));
#14324=DIRECTION('ref_axis',(1.,0.,0.));
#14325=DIRECTION('center_axis',(0.,-1.,0.));
#14326=DIRECTION('ref_axis',(1.,0.,0.));
#14327=DIRECTION('center_axis',(0.,-1.,0.));
#14328=DIRECTION('ref_axis',(1.,0.,0.));
#14329=DIRECTION('center_axis',(0.,-1.,0.));
#14330=DIRECTION('ref_axis',(1.,0.,0.));
#14331=DIRECTION('center_axis',(0.,-1.,0.));
#14332=DIRECTION('ref_axis',(1.,0.,0.));
#14333=DIRECTION('center_axis',(0.,-1.,0.));
#14334=DIRECTION('ref_axis',(1.,0.,0.));
#14335=DIRECTION('center_axis',(0.,-1.,0.));
#14336=DIRECTION('ref_axis',(1.,0.,0.));
#14337=DIRECTION('center_axis',(0.,-1.,0.));
#14338=DIRECTION('ref_axis',(1.,0.,0.));
#14339=DIRECTION('center_axis',(0.,-1.,0.));
#14340=DIRECTION('ref_axis',(1.,0.,0.));
#14341=DIRECTION('center_axis',(0.,-1.,0.));
#14342=DIRECTION('ref_axis',(1.,0.,0.));
#14343=DIRECTION('center_axis',(0.,-1.,0.));
#14344=DIRECTION('ref_axis',(1.,0.,0.));
#14345=DIRECTION('center_axis',(0.,-1.,0.));
#14346=DIRECTION('ref_axis',(1.,0.,0.));
#14347=DIRECTION('center_axis',(0.,-1.,0.));
#14348=DIRECTION('ref_axis',(1.,0.,0.));
#14349=DIRECTION('center_axis',(0.,-1.,0.));
#14350=DIRECTION('ref_axis',(1.,0.,0.));
#14351=DIRECTION('center_axis',(0.,-1.,0.));
#14352=DIRECTION('ref_axis',(1.,0.,0.));
#14353=DIRECTION('center_axis',(0.,-1.,0.));
#14354=DIRECTION('ref_axis',(1.,0.,0.));
#14355=DIRECTION('center_axis',(0.,-1.,0.));
#14356=DIRECTION('ref_axis',(1.,0.,0.));
#14357=DIRECTION('center_axis',(0.,-1.,0.));
#14358=DIRECTION('ref_axis',(1.,0.,0.));
#14359=DIRECTION('center_axis',(0.,-1.,0.));
#14360=DIRECTION('ref_axis',(1.,0.,0.));
#14361=DIRECTION('center_axis',(0.,-1.,0.));
#14362=DIRECTION('ref_axis',(1.,0.,0.));
#14363=DIRECTION('center_axis',(0.,-1.,0.));
#14364=DIRECTION('ref_axis',(1.,0.,0.));
#14365=DIRECTION('center_axis',(0.,-1.,0.));
#14366=DIRECTION('ref_axis',(1.,0.,0.));
#14367=DIRECTION('center_axis',(0.,-1.,0.));
#14368=DIRECTION('ref_axis',(1.,0.,0.));
#14369=DIRECTION('center_axis',(0.,-1.,0.));
#14370=DIRECTION('ref_axis',(1.,0.,0.));
#14371=DIRECTION('center_axis',(0.,-1.,0.));
#14372=DIRECTION('ref_axis',(1.,0.,0.));
#14373=DIRECTION('center_axis',(0.,-1.,0.));
#14374=DIRECTION('ref_axis',(1.,0.,0.));
#14375=DIRECTION('center_axis',(0.,-1.,0.));
#14376=DIRECTION('ref_axis',(1.,0.,0.));
#14377=DIRECTION('center_axis',(0.,-1.,0.));
#14378=DIRECTION('ref_axis',(1.,0.,0.));
#14379=DIRECTION('center_axis',(0.,-1.,0.));
#14380=DIRECTION('ref_axis',(1.,0.,0.));
#14381=DIRECTION('center_axis',(0.,-1.,0.));
#14382=DIRECTION('ref_axis',(1.,0.,0.));
#14383=DIRECTION('center_axis',(0.,-1.,0.));
#14384=DIRECTION('ref_axis',(1.,0.,0.));
#14385=DIRECTION('center_axis',(0.,-1.,0.));
#14386=DIRECTION('ref_axis',(1.,0.,0.));
#14387=DIRECTION('center_axis',(0.,-1.,0.));
#14388=DIRECTION('ref_axis',(1.,0.,0.));
#14389=DIRECTION('center_axis',(0.,-1.,0.));
#14390=DIRECTION('ref_axis',(1.,0.,0.));
#14391=DIRECTION('center_axis',(0.,-1.,0.));
#14392=DIRECTION('ref_axis',(1.,0.,0.));
#14393=DIRECTION('center_axis',(0.,-1.,0.));
#14394=DIRECTION('ref_axis',(1.,0.,0.));
#14395=DIRECTION('center_axis',(0.,-1.,0.));
#14396=DIRECTION('ref_axis',(1.,0.,0.));
#14397=DIRECTION('center_axis',(0.,-1.,0.));
#14398=DIRECTION('ref_axis',(1.,0.,0.));
#14399=DIRECTION('center_axis',(0.,-1.,0.));
#14400=DIRECTION('ref_axis',(1.,0.,0.));
#14401=DIRECTION('center_axis',(0.,-1.,0.));
#14402=DIRECTION('ref_axis',(1.,0.,0.));
#14403=DIRECTION('center_axis',(0.,-1.,0.));
#14404=DIRECTION('ref_axis',(1.,0.,0.));
#14405=DIRECTION('center_axis',(0.,-1.,0.));
#14406=DIRECTION('ref_axis',(1.,0.,0.));
#14407=DIRECTION('center_axis',(0.,-1.,0.));
#14408=DIRECTION('ref_axis',(1.,0.,0.));
#14409=DIRECTION('center_axis',(1.,0.,0.));
#14410=DIRECTION('ref_axis',(0.,0.70710678118655,0.707106781186545));
#14411=DIRECTION('center_axis',(-1.,0.,0.));
#14412=DIRECTION('ref_axis',(0.,0.70710678118655,0.707106781186545));
#14413=DIRECTION('',(-1.,0.,0.));
#14414=DIRECTION('center_axis',(1.,0.,0.));
#14415=DIRECTION('ref_axis',(0.,0.70710678118655,0.707106781186545));
#14416=DIRECTION('',(1.,0.,0.));
#14417=DIRECTION('center_axis',(0.,0.,1.));
#14418=DIRECTION('ref_axis',(1.,0.,0.));
#14419=DIRECTION('',(0.,1.,0.));
#14420=DIRECTION('',(-1.,0.,0.));
#14421=DIRECTION('',(0.,1.,0.));
#14422=DIRECTION('center_axis',(-1.,0.,0.));
#14423=DIRECTION('ref_axis',(0.,0.,1.));
#14424=DIRECTION('',(0.,0.,1.));
#14425=DIRECTION('',(0.,1.,0.));
#14426=DIRECTION('',(0.,0.,1.));
#14427=DIRECTION('',(0.,1.,0.));
#14428=DIRECTION('',(0.,0.,-1.));
#14429=DIRECTION('center_axis',(1.,0.,0.));
#14430=DIRECTION('ref_axis',(0.,-0.707106781186548,0.707106781186547));
#14431=DIRECTION('center_axis',(1.,0.,0.));
#14432=DIRECTION('ref_axis',(0.,-0.707106781186548,0.707106781186547));
#14433=DIRECTION('center_axis',(-1.,0.,0.));
#14434=DIRECTION('ref_axis',(0.,-0.707106781186548,0.707106781186547));
#14435=DIRECTION('',(1.,0.,0.));
#14436=DIRECTION('center_axis',(0.,1.,0.));
#14437=DIRECTION('ref_axis',(1.,0.,0.));
#14438=DIRECTION('center_axis',(0.,-1.,0.));
#14439=DIRECTION('ref_axis',(1.,0.,0.));
#14440=DIRECTION('',(0.,-1.,0.));
#14441=DIRECTION('center_axis',(0.,1.,0.));
#14442=DIRECTION('ref_axis',(1.,0.,0.));
#14443=DIRECTION('center_axis',(0.,-1.,0.));
#14444=DIRECTION('ref_axis',(1.,0.,0.));
#14445=DIRECTION('',(0.,-1.,0.));
#14446=DIRECTION('center_axis',(0.,1.,0.));
#14447=DIRECTION('ref_axis',(1.,0.,0.));
#14448=DIRECTION('center_axis',(0.,-1.,0.));
#14449=DIRECTION('ref_axis',(1.,0.,0.));
#14450=DIRECTION('',(0.,-1.,0.));
#14451=DIRECTION('center_axis',(0.,1.,0.));
#14452=DIRECTION('ref_axis',(1.,0.,0.));
#14453=DIRECTION('center_axis',(0.,-1.,0.));
#14454=DIRECTION('ref_axis',(1.,0.,0.));
#14455=DIRECTION('',(0.,-1.,0.));
#14456=DIRECTION('center_axis',(0.,1.,0.));
#14457=DIRECTION('ref_axis',(1.,0.,0.));
#14458=DIRECTION('center_axis',(0.,-1.,0.));
#14459=DIRECTION('ref_axis',(1.,0.,0.));
#14460=DIRECTION('',(0.,-1.,0.));
#14461=DIRECTION('center_axis',(0.,1.,0.));
#14462=DIRECTION('ref_axis',(1.,0.,0.));
#14463=DIRECTION('center_axis',(0.,-1.,0.));
#14464=DIRECTION('ref_axis',(1.,0.,0.));
#14465=DIRECTION('',(0.,-1.,0.));
#14466=DIRECTION('center_axis',(0.,1.,0.));
#14467=DIRECTION('ref_axis',(1.,0.,0.));
#14468=DIRECTION('center_axis',(0.,-1.,0.));
#14469=DIRECTION('ref_axis',(1.,0.,0.));
#14470=DIRECTION('',(0.,-1.,0.));
#14471=DIRECTION('center_axis',(0.,1.,0.));
#14472=DIRECTION('ref_axis',(1.,0.,0.));
#14473=DIRECTION('center_axis',(0.,-1.,0.));
#14474=DIRECTION('ref_axis',(1.,0.,0.));
#14475=DIRECTION('',(0.,-1.,0.));
#14476=DIRECTION('center_axis',(0.,1.,0.));
#14477=DIRECTION('ref_axis',(1.,0.,0.));
#14478=DIRECTION('center_axis',(0.,-1.,0.));
#14479=DIRECTION('ref_axis',(1.,0.,0.));
#14480=DIRECTION('',(0.,-1.,0.));
#14481=DIRECTION('center_axis',(0.,1.,0.));
#14482=DIRECTION('ref_axis',(1.,0.,0.));
#14483=DIRECTION('center_axis',(0.,-1.,0.));
#14484=DIRECTION('ref_axis',(1.,0.,0.));
#14485=DIRECTION('',(0.,-1.,0.));
#14486=DIRECTION('center_axis',(0.,1.,0.));
#14487=DIRECTION('ref_axis',(1.,0.,0.));
#14488=DIRECTION('center_axis',(0.,-1.,0.));
#14489=DIRECTION('ref_axis',(1.,0.,0.));
#14490=DIRECTION('',(0.,-1.,0.));
#14491=DIRECTION('center_axis',(0.,1.,0.));
#14492=DIRECTION('ref_axis',(1.,0.,0.));
#14493=DIRECTION('center_axis',(0.,-1.,0.));
#14494=DIRECTION('ref_axis',(1.,0.,0.));
#14495=DIRECTION('',(0.,-1.,0.));
#14496=DIRECTION('center_axis',(0.,1.,0.));
#14497=DIRECTION('ref_axis',(1.,0.,0.));
#14498=DIRECTION('center_axis',(0.,-1.,0.));
#14499=DIRECTION('ref_axis',(1.,0.,0.));
#14500=DIRECTION('',(0.,-1.,0.));
#14501=DIRECTION('center_axis',(0.,1.,0.));
#14502=DIRECTION('ref_axis',(1.,0.,0.));
#14503=DIRECTION('center_axis',(0.,-1.,0.));
#14504=DIRECTION('ref_axis',(1.,0.,0.));
#14505=DIRECTION('',(0.,-1.,0.));
#14506=DIRECTION('center_axis',(0.,1.,0.));
#14507=DIRECTION('ref_axis',(1.,0.,0.));
#14508=DIRECTION('center_axis',(0.,-1.,0.));
#14509=DIRECTION('ref_axis',(1.,0.,0.));
#14510=DIRECTION('',(0.,-1.,0.));
#14511=DIRECTION('center_axis',(0.,1.,0.));
#14512=DIRECTION('ref_axis',(1.,0.,0.));
#14513=DIRECTION('center_axis',(0.,-1.,0.));
#14514=DIRECTION('ref_axis',(1.,0.,0.));
#14515=DIRECTION('',(0.,-1.,0.));
#14516=DIRECTION('center_axis',(0.,1.,0.));
#14517=DIRECTION('ref_axis',(1.,0.,0.));
#14518=DIRECTION('center_axis',(0.,-1.,0.));
#14519=DIRECTION('ref_axis',(1.,0.,0.));
#14520=DIRECTION('',(0.,-1.,0.));
#14521=DIRECTION('center_axis',(0.,1.,0.));
#14522=DIRECTION('ref_axis',(1.,0.,0.));
#14523=DIRECTION('center_axis',(0.,-1.,0.));
#14524=DIRECTION('ref_axis',(1.,0.,0.));
#14525=DIRECTION('',(0.,-1.,0.));
#14526=DIRECTION('center_axis',(0.,1.,0.));
#14527=DIRECTION('ref_axis',(1.,0.,0.));
#14528=DIRECTION('center_axis',(0.,-1.,0.));
#14529=DIRECTION('ref_axis',(1.,0.,0.));
#14530=DIRECTION('',(0.,-1.,0.));
#14531=DIRECTION('center_axis',(0.,1.,0.));
#14532=DIRECTION('ref_axis',(1.,0.,0.));
#14533=DIRECTION('center_axis',(0.,-1.,0.));
#14534=DIRECTION('ref_axis',(1.,0.,0.));
#14535=DIRECTION('',(0.,-1.,0.));
#14536=DIRECTION('center_axis',(0.,1.,0.));
#14537=DIRECTION('ref_axis',(1.,0.,0.));
#14538=DIRECTION('center_axis',(0.,-1.,0.));
#14539=DIRECTION('ref_axis',(1.,0.,0.));
#14540=DIRECTION('',(0.,-1.,0.));
#14541=DIRECTION('center_axis',(0.,1.,0.));
#14542=DIRECTION('ref_axis',(1.,0.,0.));
#14543=DIRECTION('center_axis',(0.,-1.,0.));
#14544=DIRECTION('ref_axis',(1.,0.,0.));
#14545=DIRECTION('',(0.,-1.,0.));
#14546=DIRECTION('center_axis',(0.,1.,0.));
#14547=DIRECTION('ref_axis',(1.,0.,0.));
#14548=DIRECTION('center_axis',(0.,-1.,0.));
#14549=DIRECTION('ref_axis',(1.,0.,0.));
#14550=DIRECTION('',(0.,-1.,0.));
#14551=DIRECTION('center_axis',(0.,1.,0.));
#14552=DIRECTION('ref_axis',(1.,0.,0.));
#14553=DIRECTION('center_axis',(0.,-1.,0.));
#14554=DIRECTION('ref_axis',(1.,0.,0.));
#14555=DIRECTION('',(0.,-1.,0.));
#14556=DIRECTION('center_axis',(0.,1.,0.));
#14557=DIRECTION('ref_axis',(1.,0.,0.));
#14558=DIRECTION('center_axis',(0.,-1.,0.));
#14559=DIRECTION('ref_axis',(1.,0.,0.));
#14560=DIRECTION('',(0.,-1.,0.));
#14561=DIRECTION('center_axis',(0.,1.,0.));
#14562=DIRECTION('ref_axis',(1.,0.,0.));
#14563=DIRECTION('center_axis',(0.,-1.,0.));
#14564=DIRECTION('ref_axis',(1.,0.,0.));
#14565=DIRECTION('',(0.,-1.,0.));
#14566=DIRECTION('center_axis',(0.,1.,0.));
#14567=DIRECTION('ref_axis',(1.,0.,0.));
#14568=DIRECTION('center_axis',(0.,-1.,0.));
#14569=DIRECTION('ref_axis',(1.,0.,0.));
#14570=DIRECTION('',(0.,-1.,0.));
#14571=DIRECTION('center_axis',(0.,1.,0.));
#14572=DIRECTION('ref_axis',(1.,0.,0.));
#14573=DIRECTION('center_axis',(0.,-1.,0.));
#14574=DIRECTION('ref_axis',(1.,0.,0.));
#14575=DIRECTION('',(0.,-1.,0.));
#14576=DIRECTION('center_axis',(0.,1.,0.));
#14577=DIRECTION('ref_axis',(1.,0.,0.));
#14578=DIRECTION('center_axis',(0.,-1.,0.));
#14579=DIRECTION('ref_axis',(1.,0.,0.));
#14580=DIRECTION('',(0.,-1.,0.));
#14581=DIRECTION('center_axis',(0.,1.,0.));
#14582=DIRECTION('ref_axis',(1.,0.,0.));
#14583=DIRECTION('center_axis',(0.,-1.,0.));
#14584=DIRECTION('ref_axis',(1.,0.,0.));
#14585=DIRECTION('',(0.,-1.,0.));
#14586=DIRECTION('center_axis',(0.,1.,0.));
#14587=DIRECTION('ref_axis',(1.,0.,0.));
#14588=DIRECTION('center_axis',(0.,-1.,0.));
#14589=DIRECTION('ref_axis',(1.,0.,0.));
#14590=DIRECTION('',(0.,-1.,0.));
#14591=DIRECTION('center_axis',(0.,1.,0.));
#14592=DIRECTION('ref_axis',(1.,0.,0.));
#14593=DIRECTION('center_axis',(0.,-1.,0.));
#14594=DIRECTION('ref_axis',(1.,0.,0.));
#14595=DIRECTION('',(0.,-1.,0.));
#14596=DIRECTION('center_axis',(0.,1.,0.));
#14597=DIRECTION('ref_axis',(1.,0.,0.));
#14598=DIRECTION('center_axis',(0.,-1.,0.));
#14599=DIRECTION('ref_axis',(1.,0.,0.));
#14600=DIRECTION('',(0.,-1.,0.));
#14601=DIRECTION('center_axis',(0.,1.,0.));
#14602=DIRECTION('ref_axis',(1.,0.,0.));
#14603=DIRECTION('center_axis',(0.,-1.,0.));
#14604=DIRECTION('ref_axis',(1.,0.,0.));
#14605=DIRECTION('',(0.,-1.,0.));
#14606=DIRECTION('center_axis',(0.,1.,0.));
#14607=DIRECTION('ref_axis',(1.,0.,0.));
#14608=DIRECTION('center_axis',(0.,-1.,0.));
#14609=DIRECTION('ref_axis',(1.,0.,0.));
#14610=DIRECTION('',(0.,-1.,0.));
#14611=DIRECTION('center_axis',(0.,1.,0.));
#14612=DIRECTION('ref_axis',(1.,0.,0.));
#14613=DIRECTION('center_axis',(0.,-1.,0.));
#14614=DIRECTION('ref_axis',(1.,0.,0.));
#14615=DIRECTION('',(0.,-1.,0.));
#14616=DIRECTION('center_axis',(0.,1.,0.));
#14617=DIRECTION('ref_axis',(1.,0.,0.));
#14618=DIRECTION('center_axis',(0.,-1.,0.));
#14619=DIRECTION('ref_axis',(1.,0.,0.));
#14620=DIRECTION('',(0.,-1.,0.));
#14621=DIRECTION('center_axis',(0.,1.,0.));
#14622=DIRECTION('ref_axis',(1.,0.,0.));
#14623=DIRECTION('center_axis',(0.,-1.,0.));
#14624=DIRECTION('ref_axis',(1.,0.,0.));
#14625=DIRECTION('',(0.,-1.,0.));
#14626=DIRECTION('center_axis',(0.,1.,0.));
#14627=DIRECTION('ref_axis',(1.,0.,0.));
#14628=DIRECTION('center_axis',(0.,-1.,0.));
#14629=DIRECTION('ref_axis',(1.,0.,0.));
#14630=DIRECTION('',(0.,-1.,0.));
#14631=DIRECTION('center_axis',(0.,1.,0.));
#14632=DIRECTION('ref_axis',(1.,0.,0.));
#14633=DIRECTION('center_axis',(0.,-1.,0.));
#14634=DIRECTION('ref_axis',(1.,0.,0.));
#14635=DIRECTION('',(0.,-1.,0.));
#14636=DIRECTION('center_axis',(0.,1.,0.));
#14637=DIRECTION('ref_axis',(1.,0.,0.));
#14638=DIRECTION('center_axis',(0.,-1.,0.));
#14639=DIRECTION('ref_axis',(1.,0.,0.));
#14640=DIRECTION('',(0.,-1.,0.));
#14641=DIRECTION('center_axis',(0.,1.,0.));
#14642=DIRECTION('ref_axis',(1.,0.,0.));
#14643=DIRECTION('center_axis',(0.,-1.,0.));
#14644=DIRECTION('ref_axis',(1.,0.,0.));
#14645=DIRECTION('',(0.,-1.,0.));
#14646=DIRECTION('center_axis',(0.,1.,0.));
#14647=DIRECTION('ref_axis',(1.,0.,0.));
#14648=DIRECTION('center_axis',(0.,-1.,0.));
#14649=DIRECTION('ref_axis',(1.,0.,0.));
#14650=DIRECTION('',(0.,-1.,0.));
#14651=DIRECTION('center_axis',(0.,1.,0.));
#14652=DIRECTION('ref_axis',(1.,0.,0.));
#14653=DIRECTION('center_axis',(0.,-1.,0.));
#14654=DIRECTION('ref_axis',(1.,0.,0.));
#14655=DIRECTION('',(0.,-1.,0.));
#14656=DIRECTION('center_axis',(0.,1.,0.));
#14657=DIRECTION('ref_axis',(1.,0.,0.));
#14658=DIRECTION('center_axis',(0.,-1.,0.));
#14659=DIRECTION('ref_axis',(1.,0.,0.));
#14660=DIRECTION('',(0.,-1.,0.));
#14661=DIRECTION('center_axis',(0.,1.,0.));
#14662=DIRECTION('ref_axis',(1.,0.,0.));
#14663=DIRECTION('center_axis',(0.,-1.,0.));
#14664=DIRECTION('ref_axis',(1.,0.,0.));
#14665=DIRECTION('',(0.,-1.,0.));
#14666=DIRECTION('center_axis',(0.,1.,0.));
#14667=DIRECTION('ref_axis',(1.,0.,0.));
#14668=DIRECTION('center_axis',(0.,-1.,0.));
#14669=DIRECTION('ref_axis',(1.,0.,0.));
#14670=DIRECTION('',(0.,-1.,0.));
#14671=DIRECTION('center_axis',(0.,0.,-1.));
#14672=DIRECTION('ref_axis',(-1.,0.,0.));
#14673=DIRECTION('',(-1.,0.,0.));
#14674=DIRECTION('',(0.,1.,0.));
#14675=DIRECTION('center_axis',(0.,1.,0.));
#14676=DIRECTION('ref_axis',(0.,0.,1.));
#14677=DIRECTION('',(0.,0.,-1.));
#14678=DIRECTION('center_axis',(0.,1.,0.));
#14679=DIRECTION('ref_axis',(1.,0.,0.));
#14680=DIRECTION('center_axis',(0.,-1.,0.));
#14681=DIRECTION('ref_axis',(1.,0.,0.));
#14682=DIRECTION('',(0.,-1.,0.));
#14683=DIRECTION('center_axis',(0.,-1.,0.));
#14684=DIRECTION('ref_axis',(1.,0.,0.));
#14685=DIRECTION('center_axis',(0.,1.,0.));
#14686=DIRECTION('ref_axis',(1.,0.,0.));
#14687=DIRECTION('center_axis',(0.,-1.,0.));
#14688=DIRECTION('ref_axis',(1.,0.,0.));
#14689=DIRECTION('',(0.,-1.,0.));
#14690=DIRECTION('center_axis',(0.,-1.,0.));
#14691=DIRECTION('ref_axis',(1.,0.,0.));
#14692=DIRECTION('center_axis',(0.,1.,0.));
#14693=DIRECTION('ref_axis',(1.,0.,0.));
#14694=DIRECTION('center_axis',(0.,-1.,0.));
#14695=DIRECTION('ref_axis',(1.,0.,0.));
#14696=DIRECTION('',(0.,-1.,0.));
#14697=DIRECTION('center_axis',(0.,-1.,0.));
#14698=DIRECTION('ref_axis',(1.,0.,0.));
#14699=DIRECTION('center_axis',(0.,1.,0.));
#14700=DIRECTION('ref_axis',(1.,0.,0.));
#14701=DIRECTION('center_axis',(0.,-1.,0.));
#14702=DIRECTION('ref_axis',(1.,0.,0.));
#14703=DIRECTION('',(0.,-1.,0.));
#14704=DIRECTION('center_axis',(0.,-1.,0.));
#14705=DIRECTION('ref_axis',(1.,0.,0.));
#14706=DIRECTION('center_axis',(0.,1.,0.));
#14707=DIRECTION('ref_axis',(1.,0.,0.));
#14708=DIRECTION('center_axis',(0.,-1.,0.));
#14709=DIRECTION('ref_axis',(1.,0.,0.));
#14710=DIRECTION('',(0.,-1.,0.));
#14711=DIRECTION('center_axis',(0.,-1.,0.));
#14712=DIRECTION('ref_axis',(1.,0.,0.));
#14713=DIRECTION('center_axis',(0.,1.,0.));
#14714=DIRECTION('ref_axis',(1.,0.,0.));
#14715=DIRECTION('center_axis',(0.,-1.,0.));
#14716=DIRECTION('ref_axis',(1.,0.,0.));
#14717=DIRECTION('',(0.,-1.,0.));
#14718=DIRECTION('center_axis',(0.,-1.,0.));
#14719=DIRECTION('ref_axis',(1.,0.,0.));
#14720=DIRECTION('center_axis',(0.,1.,0.));
#14721=DIRECTION('ref_axis',(1.,0.,0.));
#14722=DIRECTION('center_axis',(0.,-1.,0.));
#14723=DIRECTION('ref_axis',(1.,0.,0.));
#14724=DIRECTION('',(0.,-1.,0.));
#14725=DIRECTION('center_axis',(0.,-1.,0.));
#14726=DIRECTION('ref_axis',(1.,0.,0.));
#14727=DIRECTION('center_axis',(0.,1.,0.));
#14728=DIRECTION('ref_axis',(1.,0.,0.));
#14729=DIRECTION('center_axis',(0.,-1.,0.));
#14730=DIRECTION('ref_axis',(1.,0.,0.));
#14731=DIRECTION('',(0.,-1.,0.));
#14732=DIRECTION('center_axis',(0.,-1.,0.));
#14733=DIRECTION('ref_axis',(1.,0.,0.));
#14734=DIRECTION('center_axis',(0.,1.,0.));
#14735=DIRECTION('ref_axis',(1.,0.,0.));
#14736=DIRECTION('center_axis',(0.,-1.,0.));
#14737=DIRECTION('ref_axis',(1.,0.,0.));
#14738=DIRECTION('',(0.,-1.,0.));
#14739=DIRECTION('center_axis',(0.,-1.,0.));
#14740=DIRECTION('ref_axis',(1.,0.,0.));
#14741=DIRECTION('center_axis',(0.,1.,0.));
#14742=DIRECTION('ref_axis',(1.,0.,0.));
#14743=DIRECTION('center_axis',(0.,-1.,0.));
#14744=DIRECTION('ref_axis',(1.,0.,0.));
#14745=DIRECTION('',(0.,-1.,0.));
#14746=DIRECTION('center_axis',(0.,-1.,0.));
#14747=DIRECTION('ref_axis',(1.,0.,0.));
#14748=DIRECTION('center_axis',(0.,1.,0.));
#14749=DIRECTION('ref_axis',(1.,0.,0.));
#14750=DIRECTION('center_axis',(0.,-1.,0.));
#14751=DIRECTION('ref_axis',(1.,0.,0.));
#14752=DIRECTION('',(0.,-1.,0.));
#14753=DIRECTION('center_axis',(0.,-1.,0.));
#14754=DIRECTION('ref_axis',(1.,0.,0.));
#14755=DIRECTION('center_axis',(0.,1.,0.));
#14756=DIRECTION('ref_axis',(1.,0.,0.));
#14757=DIRECTION('center_axis',(0.,-1.,0.));
#14758=DIRECTION('ref_axis',(1.,0.,0.));
#14759=DIRECTION('',(0.,-1.,0.));
#14760=DIRECTION('center_axis',(0.,-1.,0.));
#14761=DIRECTION('ref_axis',(1.,0.,0.));
#14762=DIRECTION('center_axis',(0.,1.,0.));
#14763=DIRECTION('ref_axis',(1.,0.,0.));
#14764=DIRECTION('center_axis',(0.,-1.,0.));
#14765=DIRECTION('ref_axis',(1.,0.,0.));
#14766=DIRECTION('',(0.,-1.,0.));
#14767=DIRECTION('center_axis',(0.,-1.,0.));
#14768=DIRECTION('ref_axis',(1.,0.,0.));
#14769=DIRECTION('center_axis',(0.,1.,0.));
#14770=DIRECTION('ref_axis',(1.,0.,0.));
#14771=DIRECTION('center_axis',(0.,-1.,0.));
#14772=DIRECTION('ref_axis',(1.,0.,0.));
#14773=DIRECTION('',(0.,-1.,0.));
#14774=DIRECTION('center_axis',(0.,-1.,0.));
#14775=DIRECTION('ref_axis',(1.,0.,0.));
#14776=DIRECTION('center_axis',(0.,1.,0.));
#14777=DIRECTION('ref_axis',(1.,0.,0.));
#14778=DIRECTION('center_axis',(0.,-1.,0.));
#14779=DIRECTION('ref_axis',(1.,0.,0.));
#14780=DIRECTION('',(0.,-1.,0.));
#14781=DIRECTION('center_axis',(0.,-1.,0.));
#14782=DIRECTION('ref_axis',(1.,0.,0.));
#14783=DIRECTION('center_axis',(0.,1.,0.));
#14784=DIRECTION('ref_axis',(1.,0.,0.));
#14785=DIRECTION('center_axis',(0.,-1.,0.));
#14786=DIRECTION('ref_axis',(1.,0.,0.));
#14787=DIRECTION('',(0.,-1.,0.));
#14788=DIRECTION('center_axis',(0.,-1.,0.));
#14789=DIRECTION('ref_axis',(1.,0.,0.));
#14790=DIRECTION('center_axis',(0.,1.,0.));
#14791=DIRECTION('ref_axis',(1.,0.,0.));
#14792=DIRECTION('center_axis',(0.,-1.,0.));
#14793=DIRECTION('ref_axis',(1.,0.,0.));
#14794=DIRECTION('',(0.,-1.,0.));
#14795=DIRECTION('center_axis',(0.,-1.,0.));
#14796=DIRECTION('ref_axis',(1.,0.,0.));
#14797=DIRECTION('center_axis',(0.,1.,0.));
#14798=DIRECTION('ref_axis',(1.,0.,0.));
#14799=DIRECTION('center_axis',(0.,-1.,0.));
#14800=DIRECTION('ref_axis',(1.,0.,0.));
#14801=DIRECTION('',(0.,-1.,0.));
#14802=DIRECTION('center_axis',(0.,-1.,0.));
#14803=DIRECTION('ref_axis',(1.,0.,0.));
#14804=DIRECTION('center_axis',(0.,1.,0.));
#14805=DIRECTION('ref_axis',(1.,0.,0.));
#14806=DIRECTION('center_axis',(0.,-1.,0.));
#14807=DIRECTION('ref_axis',(1.,0.,0.));
#14808=DIRECTION('',(0.,-1.,0.));
#14809=DIRECTION('center_axis',(0.,-1.,0.));
#14810=DIRECTION('ref_axis',(1.,0.,0.));
#14811=DIRECTION('center_axis',(0.,1.,0.));
#14812=DIRECTION('ref_axis',(1.,0.,0.));
#14813=DIRECTION('center_axis',(0.,-1.,0.));
#14814=DIRECTION('ref_axis',(1.,0.,0.));
#14815=DIRECTION('',(0.,-1.,0.));
#14816=DIRECTION('center_axis',(0.,-1.,0.));
#14817=DIRECTION('ref_axis',(1.,0.,0.));
#14818=DIRECTION('center_axis',(0.,1.,0.));
#14819=DIRECTION('ref_axis',(1.,0.,0.));
#14820=DIRECTION('center_axis',(0.,-1.,0.));
#14821=DIRECTION('ref_axis',(1.,0.,0.));
#14822=DIRECTION('',(0.,-1.,0.));
#14823=DIRECTION('center_axis',(0.,-1.,0.));
#14824=DIRECTION('ref_axis',(1.,0.,0.));
#14825=DIRECTION('center_axis',(0.,1.,0.));
#14826=DIRECTION('ref_axis',(1.,0.,0.));
#14827=DIRECTION('center_axis',(0.,-1.,0.));
#14828=DIRECTION('ref_axis',(1.,0.,0.));
#14829=DIRECTION('',(0.,-1.,0.));
#14830=DIRECTION('center_axis',(0.,-1.,0.));
#14831=DIRECTION('ref_axis',(1.,0.,0.));
#14832=DIRECTION('center_axis',(0.,1.,0.));
#14833=DIRECTION('ref_axis',(1.,0.,0.));
#14834=DIRECTION('center_axis',(0.,-1.,0.));
#14835=DIRECTION('ref_axis',(1.,0.,0.));
#14836=DIRECTION('',(0.,-1.,0.));
#14837=DIRECTION('center_axis',(0.,-1.,0.));
#14838=DIRECTION('ref_axis',(1.,0.,0.));
#14839=DIRECTION('center_axis',(0.,1.,0.));
#14840=DIRECTION('ref_axis',(1.,0.,0.));
#14841=DIRECTION('center_axis',(0.,-1.,0.));
#14842=DIRECTION('ref_axis',(1.,0.,0.));
#14843=DIRECTION('',(0.,-1.,0.));
#14844=DIRECTION('center_axis',(0.,-1.,0.));
#14845=DIRECTION('ref_axis',(1.,0.,0.));
#14846=DIRECTION('center_axis',(0.,1.,0.));
#14847=DIRECTION('ref_axis',(1.,0.,0.));
#14848=DIRECTION('center_axis',(0.,-1.,0.));
#14849=DIRECTION('ref_axis',(1.,0.,0.));
#14850=DIRECTION('',(0.,-1.,0.));
#14851=DIRECTION('center_axis',(0.,-1.,0.));
#14852=DIRECTION('ref_axis',(1.,0.,0.));
#14853=DIRECTION('center_axis',(0.,1.,0.));
#14854=DIRECTION('ref_axis',(1.,0.,0.));
#14855=DIRECTION('center_axis',(0.,-1.,0.));
#14856=DIRECTION('ref_axis',(1.,0.,0.));
#14857=DIRECTION('',(0.,-1.,0.));
#14858=DIRECTION('center_axis',(0.,-1.,0.));
#14859=DIRECTION('ref_axis',(1.,0.,0.));
#14860=DIRECTION('center_axis',(0.,1.,0.));
#14861=DIRECTION('ref_axis',(1.,0.,0.));
#14862=DIRECTION('center_axis',(0.,-1.,0.));
#14863=DIRECTION('ref_axis',(1.,0.,0.));
#14864=DIRECTION('',(0.,-1.,0.));
#14865=DIRECTION('center_axis',(0.,-1.,0.));
#14866=DIRECTION('ref_axis',(1.,0.,0.));
#14867=DIRECTION('center_axis',(0.,1.,0.));
#14868=DIRECTION('ref_axis',(1.,0.,0.));
#14869=DIRECTION('center_axis',(0.,-1.,0.));
#14870=DIRECTION('ref_axis',(1.,0.,0.));
#14871=DIRECTION('',(0.,-1.,0.));
#14872=DIRECTION('center_axis',(0.,-1.,0.));
#14873=DIRECTION('ref_axis',(1.,0.,0.));
#14874=DIRECTION('center_axis',(0.,1.,0.));
#14875=DIRECTION('ref_axis',(1.,0.,0.));
#14876=DIRECTION('center_axis',(0.,-1.,0.));
#14877=DIRECTION('ref_axis',(1.,0.,0.));
#14878=DIRECTION('',(0.,-1.,0.));
#14879=DIRECTION('center_axis',(0.,-1.,0.));
#14880=DIRECTION('ref_axis',(1.,0.,0.));
#14881=DIRECTION('center_axis',(0.,1.,0.));
#14882=DIRECTION('ref_axis',(1.,0.,0.));
#14883=DIRECTION('center_axis',(0.,-1.,0.));
#14884=DIRECTION('ref_axis',(1.,0.,0.));
#14885=DIRECTION('',(0.,-1.,0.));
#14886=DIRECTION('center_axis',(0.,-1.,0.));
#14887=DIRECTION('ref_axis',(1.,0.,0.));
#14888=DIRECTION('center_axis',(0.,1.,0.));
#14889=DIRECTION('ref_axis',(1.,0.,0.));
#14890=DIRECTION('center_axis',(0.,-1.,0.));
#14891=DIRECTION('ref_axis',(1.,0.,0.));
#14892=DIRECTION('',(0.,-1.,0.));
#14893=DIRECTION('center_axis',(0.,-1.,0.));
#14894=DIRECTION('ref_axis',(1.,0.,0.));
#14895=DIRECTION('center_axis',(0.,1.,0.));
#14896=DIRECTION('ref_axis',(1.,0.,0.));
#14897=DIRECTION('center_axis',(0.,-1.,0.));
#14898=DIRECTION('ref_axis',(1.,0.,0.));
#14899=DIRECTION('',(0.,-1.,0.));
#14900=DIRECTION('center_axis',(0.,-1.,0.));
#14901=DIRECTION('ref_axis',(1.,0.,0.));
#14902=DIRECTION('center_axis',(0.,1.,0.));
#14903=DIRECTION('ref_axis',(1.,0.,0.));
#14904=DIRECTION('center_axis',(0.,-1.,0.));
#14905=DIRECTION('ref_axis',(1.,0.,0.));
#14906=DIRECTION('',(0.,-1.,0.));
#14907=DIRECTION('center_axis',(0.,-1.,0.));
#14908=DIRECTION('ref_axis',(1.,0.,0.));
#14909=DIRECTION('center_axis',(0.,1.,0.));
#14910=DIRECTION('ref_axis',(1.,0.,0.));
#14911=DIRECTION('center_axis',(0.,-1.,0.));
#14912=DIRECTION('ref_axis',(1.,0.,0.));
#14913=DIRECTION('',(0.,-1.,0.));
#14914=DIRECTION('center_axis',(0.,-1.,0.));
#14915=DIRECTION('ref_axis',(1.,0.,0.));
#14916=DIRECTION('center_axis',(0.,1.,0.));
#14917=DIRECTION('ref_axis',(1.,0.,0.));
#14918=DIRECTION('center_axis',(0.,-1.,0.));
#14919=DIRECTION('ref_axis',(1.,0.,0.));
#14920=DIRECTION('',(0.,-1.,0.));
#14921=DIRECTION('center_axis',(0.,-1.,0.));
#14922=DIRECTION('ref_axis',(1.,0.,0.));
#14923=DIRECTION('center_axis',(0.,1.,0.));
#14924=DIRECTION('ref_axis',(1.,0.,0.));
#14925=DIRECTION('center_axis',(0.,-1.,0.));
#14926=DIRECTION('ref_axis',(1.,0.,0.));
#14927=DIRECTION('',(0.,-1.,0.));
#14928=DIRECTION('center_axis',(0.,-1.,0.));
#14929=DIRECTION('ref_axis',(1.,0.,0.));
#14930=DIRECTION('center_axis',(0.,1.,0.));
#14931=DIRECTION('ref_axis',(1.,0.,0.));
#14932=DIRECTION('center_axis',(0.,-1.,0.));
#14933=DIRECTION('ref_axis',(1.,0.,0.));
#14934=DIRECTION('',(0.,-1.,0.));
#14935=DIRECTION('center_axis',(0.,-1.,0.));
#14936=DIRECTION('ref_axis',(1.,0.,0.));
#14937=DIRECTION('center_axis',(0.,1.,0.));
#14938=DIRECTION('ref_axis',(1.,0.,0.));
#14939=DIRECTION('center_axis',(0.,-1.,0.));
#14940=DIRECTION('ref_axis',(1.,0.,0.));
#14941=DIRECTION('',(0.,-1.,0.));
#14942=DIRECTION('center_axis',(0.,-1.,0.));
#14943=DIRECTION('ref_axis',(1.,0.,0.));
#14944=DIRECTION('center_axis',(0.,1.,0.));
#14945=DIRECTION('ref_axis',(1.,0.,0.));
#14946=DIRECTION('center_axis',(0.,-1.,0.));
#14947=DIRECTION('ref_axis',(1.,0.,0.));
#14948=DIRECTION('',(0.,-1.,0.));
#14949=DIRECTION('center_axis',(0.,-1.,0.));
#14950=DIRECTION('ref_axis',(1.,0.,0.));
#14951=DIRECTION('center_axis',(0.,1.,0.));
#14952=DIRECTION('ref_axis',(1.,0.,0.));
#14953=DIRECTION('center_axis',(0.,-1.,0.));
#14954=DIRECTION('ref_axis',(1.,0.,0.));
#14955=DIRECTION('',(0.,-1.,0.));
#14956=DIRECTION('center_axis',(0.,-1.,0.));
#14957=DIRECTION('ref_axis',(1.,0.,0.));
#14958=DIRECTION('center_axis',(0.,1.,0.));
#14959=DIRECTION('ref_axis',(1.,0.,0.));
#14960=DIRECTION('center_axis',(0.,-1.,0.));
#14961=DIRECTION('ref_axis',(1.,0.,0.));
#14962=DIRECTION('',(0.,-1.,0.));
#14963=DIRECTION('center_axis',(0.,-1.,0.));
#14964=DIRECTION('ref_axis',(1.,0.,0.));
#14965=DIRECTION('center_axis',(0.,1.,0.));
#14966=DIRECTION('ref_axis',(1.,0.,0.));
#14967=DIRECTION('center_axis',(0.,-1.,0.));
#14968=DIRECTION('ref_axis',(1.,0.,0.));
#14969=DIRECTION('',(0.,-1.,0.));
#14970=DIRECTION('center_axis',(0.,-1.,0.));
#14971=DIRECTION('ref_axis',(1.,0.,0.));
#14972=DIRECTION('center_axis',(0.,1.,0.));
#14973=DIRECTION('ref_axis',(1.,0.,0.));
#14974=DIRECTION('center_axis',(0.,-1.,0.));
#14975=DIRECTION('ref_axis',(1.,0.,0.));
#14976=DIRECTION('',(0.,-1.,0.));
#14977=DIRECTION('center_axis',(0.,-1.,0.));
#14978=DIRECTION('ref_axis',(1.,0.,0.));
#14979=DIRECTION('center_axis',(0.,1.,0.));
#14980=DIRECTION('ref_axis',(1.,0.,0.));
#14981=DIRECTION('center_axis',(0.,-1.,0.));
#14982=DIRECTION('ref_axis',(1.,0.,0.));
#14983=DIRECTION('',(0.,-1.,0.));
#14984=DIRECTION('center_axis',(0.,-1.,0.));
#14985=DIRECTION('ref_axis',(1.,0.,0.));
#14986=DIRECTION('center_axis',(0.,1.,0.));
#14987=DIRECTION('ref_axis',(1.,0.,0.));
#14988=DIRECTION('center_axis',(0.,-1.,0.));
#14989=DIRECTION('ref_axis',(1.,0.,0.));
#14990=DIRECTION('',(0.,-1.,0.));
#14991=DIRECTION('center_axis',(0.,-1.,0.));
#14992=DIRECTION('ref_axis',(1.,0.,0.));
#14993=DIRECTION('center_axis',(0.,1.,0.));
#14994=DIRECTION('ref_axis',(1.,0.,0.));
#14995=DIRECTION('center_axis',(0.,-1.,0.));
#14996=DIRECTION('ref_axis',(1.,0.,0.));
#14997=DIRECTION('',(0.,-1.,0.));
#14998=DIRECTION('center_axis',(0.,-1.,0.));
#14999=DIRECTION('ref_axis',(1.,0.,0.));
#15000=DIRECTION('center_axis',(0.,1.,0.));
#15001=DIRECTION('ref_axis',(1.,0.,0.));
#15002=DIRECTION('center_axis',(0.,-1.,0.));
#15003=DIRECTION('ref_axis',(1.,0.,0.));
#15004=DIRECTION('',(0.,-1.,0.));
#15005=DIRECTION('center_axis',(0.,-1.,0.));
#15006=DIRECTION('ref_axis',(1.,0.,0.));
#15007=DIRECTION('center_axis',(0.,0.,-1.));
#15008=DIRECTION('ref_axis',(-1.,0.,0.));
#15009=DIRECTION('',(1.,0.,0.));
#15010=DIRECTION('',(-1.,0.,0.));
#15011=DIRECTION('',(0.,1.,0.));
#15012=DIRECTION('center_axis',(1.,0.,0.));
#15013=DIRECTION('ref_axis',(0.,0.,-1.));
#15014=DIRECTION('',(0.,0.,1.));
#15015=DIRECTION('',(0.,0.,-1.));
#15016=DIRECTION('center_axis',(0.,1.,0.));
#15017=DIRECTION('ref_axis',(1.,0.,0.));
#15018=DIRECTION('center_axis',(0.,1.,0.));
#15019=DIRECTION('ref_axis',(1.,0.,0.));
#16741=CARTESIAN_POINT('',(0.,0.,0.));
#16742=CARTESIAN_POINT('Origin',(351.940084821141,11.70240347792,12.));
#16743=CARTESIAN_POINT('',(354.440084821141,11.70240347792,12.));
#16744=CARTESIAN_POINT('Origin',(351.940084821141,11.70240347792,12.));
#16745=CARTESIAN_POINT('',(354.440084821141,11.70240347792,10.));
#16746=CARTESIAN_POINT('',(354.440084821141,11.70240347792,12.));
#16747=CARTESIAN_POINT('Origin',(351.940084821141,11.70240347792,10.));
#16748=CARTESIAN_POINT('Origin',(378.352975097007,11.70240347792,12.));
#16749=CARTESIAN_POINT('',(380.852975097007,11.70240347792,12.));
#16750=CARTESIAN_POINT('Origin',(378.352975097007,11.70240347792,12.));
#16751=CARTESIAN_POINT('',(380.852975097007,11.70240347792,10.));
#16752=CARTESIAN_POINT('',(380.852975097007,11.70240347792,12.));
#16753=CARTESIAN_POINT('Origin',(378.352975097007,11.70240347792,10.));
#16754=CARTESIAN_POINT('Origin',(378.352975097007,38.29759652208,12.));
#16755=CARTESIAN_POINT('',(380.852975097007,38.29759652208,12.));
#16756=CARTESIAN_POINT('Origin',(378.352975097007,38.29759652208,12.));
#16757=CARTESIAN_POINT('',(380.852975097007,38.29759652208,10.));
#16758=CARTESIAN_POINT('',(380.852975097007,38.29759652208,12.));
#16759=CARTESIAN_POINT('Origin',(378.352975097007,38.29759652208,10.));
#16760=CARTESIAN_POINT('Origin',(351.940084821141,38.29759652208,12.));
#16761=CARTESIAN_POINT('',(354.440084821141,38.29759652208,12.));
#16762=CARTESIAN_POINT('Origin',(351.940084821141,38.29759652208,12.));
#16763=CARTESIAN_POINT('',(354.440084821141,38.29759652208,10.));
#16764=CARTESIAN_POINT('',(354.440084821141,38.29759652208,12.));
#16765=CARTESIAN_POINT('Origin',(351.940084821141,38.29759652208,10.));
#16766=CARTESIAN_POINT('Origin',(365.146529959074,25.,12.));
#16767=CARTESIAN_POINT('',(375.146529959074,25.,12.));
#16768=CARTESIAN_POINT('Origin',(365.146529959074,25.,12.));
#16769=CARTESIAN_POINT('',(375.146529959074,25.,10.));
#16770=CARTESIAN_POINT('',(375.146529959074,25.,12.));
#16771=CARTESIAN_POINT('Origin',(365.146529959074,25.,10.));
#16772=CARTESIAN_POINT('Origin',(363.646529959074,39.8065050734778,12.));
#16773=CARTESIAN_POINT('',(363.646529959074,44.7051656728289,10.));
#16774=CARTESIAN_POINT('',(363.646529959074,39.8065050734778,10.));
#16775=CARTESIAN_POINT('',(363.646529959074,19.9032525367389,10.));
#16776=CARTESIAN_POINT('',(363.646529959074,44.7051656728289,12.));
#16777=CARTESIAN_POINT('',(363.646529959074,44.7051656728289,12.));
#16778=CARTESIAN_POINT('',(363.646529959074,39.8065050734778,12.));
#16779=CARTESIAN_POINT('',(363.646529959074,19.9032525367389,12.));
#16780=CARTESIAN_POINT('',(363.646529959074,39.8065050734778,12.));
#16781=CARTESIAN_POINT('Origin',(365.146529959074,39.8065050734778,12.));
#16782=CARTESIAN_POINT('',(366.646529959074,39.8065050734778,10.));
#16783=CARTESIAN_POINT('Origin',(365.146529959074,39.8065050734778,10.));
#16784=CARTESIAN_POINT('',(366.646529959074,39.8065050734778,12.));
#16785=CARTESIAN_POINT('Origin',(365.146529959074,39.8065050734778,12.));
#16786=CARTESIAN_POINT('',(366.646529959074,39.8065050734778,12.));
#16787=CARTESIAN_POINT('Origin',(366.646529959074,44.7051656728289,12.));
#16788=CARTESIAN_POINT('',(366.646529959074,44.7051656728289,10.));
#16789=CARTESIAN_POINT('',(366.646529959074,22.3525828364145,10.));
#16790=CARTESIAN_POINT('',(366.646529959074,44.7051656728289,12.));
#16791=CARTESIAN_POINT('',(366.646529959074,22.3525828364145,12.));
#16792=CARTESIAN_POINT('',(366.646529959074,44.7051656728289,12.));
#16793=CARTESIAN_POINT('Origin',(365.146529959074,44.7051656728289,12.));
#16794=CARTESIAN_POINT('Origin',(365.146529959074,44.7051656728289,10.));
#16795=CARTESIAN_POINT('Origin',(365.146529959074,44.7051656728289,12.));
#16796=CARTESIAN_POINT('Origin',(363.646529959074,5.29483432717106,12.));
#16797=CARTESIAN_POINT('',(363.646529959074,10.1934949265222,10.));
#16798=CARTESIAN_POINT('',(363.646529959074,5.29483432717106,10.));
#16799=CARTESIAN_POINT('',(363.646529959074,2.64741716358553,10.));
#16800=CARTESIAN_POINT('',(363.646529959074,10.1934949265222,12.));
#16801=CARTESIAN_POINT('',(363.646529959074,10.1934949265222,12.));
#16802=CARTESIAN_POINT('',(363.646529959074,5.29483432717106,12.));
#16803=CARTESIAN_POINT('',(363.646529959074,2.64741716358553,12.));
#16804=CARTESIAN_POINT('',(363.646529959074,5.29483432717106,12.));
#16805=CARTESIAN_POINT('Origin',(365.146529959074,5.29483432717106,12.));
#16806=CARTESIAN_POINT('',(366.646529959074,5.29483432717106,10.));
#16807=CARTESIAN_POINT('Origin',(365.146529959074,5.29483432717106,10.));
#16808=CARTESIAN_POINT('',(366.646529959074,5.29483432717106,12.));
#16809=CARTESIAN_POINT('Origin',(365.146529959074,5.29483432717106,12.));
#16810=CARTESIAN_POINT('',(366.646529959074,5.29483432717106,12.));
#16811=CARTESIAN_POINT('Origin',(366.646529959074,10.1934949265222,12.));
#16812=CARTESIAN_POINT('',(366.646529959074,10.1934949265222,10.));
#16813=CARTESIAN_POINT('',(366.646529959074,5.09674746326108,10.));
#16814=CARTESIAN_POINT('',(366.646529959074,10.1934949265222,12.));
#16815=CARTESIAN_POINT('',(366.646529959074,5.09674746326108,12.));
#16816=CARTESIAN_POINT('',(366.646529959074,10.1934949265222,12.));
#16817=CARTESIAN_POINT('Origin',(365.146529959074,10.1934949265222,12.));
#16818=CARTESIAN_POINT('Origin',(365.146529959074,10.1934949265222,10.));
#16819=CARTESIAN_POINT('Origin',(365.146529959074,10.1934949265222,12.));
#16820=CARTESIAN_POINT('Origin',(313.495640376696,11.70240347792,12.));
#16821=CARTESIAN_POINT('',(315.995640376696,11.70240347792,12.));
#16822=CARTESIAN_POINT('Origin',(313.495640376696,11.70240347792,12.));
#16823=CARTESIAN_POINT('',(315.995640376696,11.70240347792,10.));
#16824=CARTESIAN_POINT('',(315.995640376696,11.70240347792,12.));
#16825=CARTESIAN_POINT('Origin',(313.495640376696,11.70240347792,10.));
#16826=CARTESIAN_POINT('Origin',(339.908530652563,11.70240347792,12.));
#16827=CARTESIAN_POINT('',(342.408530652563,11.70240347792,12.));
#16828=CARTESIAN_POINT('Origin',(339.908530652563,11.70240347792,12.));
#16829=CARTESIAN_POINT('',(342.408530652563,11.70240347792,10.));
#16830=CARTESIAN_POINT('',(342.408530652563,11.70240347792,12.));
#16831=CARTESIAN_POINT('Origin',(339.908530652563,11.70240347792,10.));
#16832=CARTESIAN_POINT('Origin',(339.908530652563,38.29759652208,12.));
#16833=CARTESIAN_POINT('',(342.408530652563,38.29759652208,12.));
#16834=CARTESIAN_POINT('Origin',(339.908530652563,38.29759652208,12.));
#16835=CARTESIAN_POINT('',(342.408530652563,38.29759652208,10.));
#16836=CARTESIAN_POINT('',(342.408530652563,38.29759652208,12.));
#16837=CARTESIAN_POINT('Origin',(339.908530652563,38.29759652208,10.));
#16838=CARTESIAN_POINT('Origin',(313.495640376696,38.29759652208,12.));
#16839=CARTESIAN_POINT('',(315.995640376696,38.29759652208,12.));
#16840=CARTESIAN_POINT('Origin',(313.495640376696,38.29759652208,12.));
#16841=CARTESIAN_POINT('',(315.995640376696,38.29759652208,10.));
#16842=CARTESIAN_POINT('',(315.995640376696,38.29759652208,12.));
#16843=CARTESIAN_POINT('Origin',(313.495640376696,38.29759652208,10.));
#16844=CARTESIAN_POINT('Origin',(326.70208551463,25.,12.));
#16845=CARTESIAN_POINT('',(336.70208551463,25.,12.));
#16846=CARTESIAN_POINT('Origin',(326.70208551463,25.,12.));
#16847=CARTESIAN_POINT('',(336.70208551463,25.,10.));
#16848=CARTESIAN_POINT('',(336.70208551463,25.,12.));
#16849=CARTESIAN_POINT('Origin',(326.70208551463,25.,10.));
#16850=CARTESIAN_POINT('Origin',(325.20208551463,39.8065050734778,12.));
#16851=CARTESIAN_POINT('',(325.20208551463,44.7051656728289,10.));
#16852=CARTESIAN_POINT('',(325.20208551463,39.8065050734778,10.));
#16853=CARTESIAN_POINT('',(325.20208551463,19.9032525367389,10.));
#16854=CARTESIAN_POINT('',(325.20208551463,44.7051656728289,12.));
#16855=CARTESIAN_POINT('',(325.20208551463,44.7051656728289,12.));
#16856=CARTESIAN_POINT('',(325.20208551463,39.8065050734778,12.));
#16857=CARTESIAN_POINT('',(325.20208551463,19.9032525367389,12.));
#16858=CARTESIAN_POINT('',(325.20208551463,39.8065050734778,12.));
#16859=CARTESIAN_POINT('Origin',(326.70208551463,39.8065050734778,12.));
#16860=CARTESIAN_POINT('',(328.20208551463,39.8065050734778,10.));
#16861=CARTESIAN_POINT('Origin',(326.70208551463,39.8065050734778,10.));
#16862=CARTESIAN_POINT('',(328.20208551463,39.8065050734778,12.));
#16863=CARTESIAN_POINT('Origin',(326.70208551463,39.8065050734778,12.));
#16864=CARTESIAN_POINT('',(328.20208551463,39.8065050734778,12.));
#16865=CARTESIAN_POINT('Origin',(328.20208551463,44.7051656728289,12.));
#16866=CARTESIAN_POINT('',(328.20208551463,44.7051656728289,10.));
#16867=CARTESIAN_POINT('',(328.20208551463,22.3525828364145,10.));
#16868=CARTESIAN_POINT('',(328.20208551463,44.7051656728289,12.));
#16869=CARTESIAN_POINT('',(328.20208551463,22.3525828364145,12.));
#16870=CARTESIAN_POINT('',(328.20208551463,44.7051656728289,12.));
#16871=CARTESIAN_POINT('Origin',(326.70208551463,44.7051656728289,12.));
#16872=CARTESIAN_POINT('Origin',(326.70208551463,44.7051656728289,10.));
#16873=CARTESIAN_POINT('Origin',(326.70208551463,44.7051656728289,12.));
#16874=CARTESIAN_POINT('Origin',(325.20208551463,5.29483432717106,12.));
#16875=CARTESIAN_POINT('',(325.20208551463,10.1934949265222,10.));
#16876=CARTESIAN_POINT('',(325.20208551463,5.29483432717106,10.));
#16877=CARTESIAN_POINT('',(325.20208551463,2.64741716358553,10.));
#16878=CARTESIAN_POINT('',(325.20208551463,10.1934949265222,12.));
#16879=CARTESIAN_POINT('',(325.20208551463,10.1934949265222,12.));
#16880=CARTESIAN_POINT('',(325.20208551463,5.29483432717106,12.));
#16881=CARTESIAN_POINT('',(325.20208551463,2.64741716358553,12.));
#16882=CARTESIAN_POINT('',(325.20208551463,5.29483432717106,12.));
#16883=CARTESIAN_POINT('Origin',(326.70208551463,5.29483432717106,12.));
#16884=CARTESIAN_POINT('',(328.20208551463,5.29483432717106,10.));
#16885=CARTESIAN_POINT('Origin',(326.70208551463,5.29483432717106,10.));
#16886=CARTESIAN_POINT('',(328.20208551463,5.29483432717106,12.));
#16887=CARTESIAN_POINT('Origin',(326.70208551463,5.29483432717106,12.));
#16888=CARTESIAN_POINT('',(328.20208551463,5.29483432717106,12.));
#16889=CARTESIAN_POINT('Origin',(328.20208551463,10.1934949265222,12.));
#16890=CARTESIAN_POINT('',(328.20208551463,10.1934949265222,10.));
#16891=CARTESIAN_POINT('',(328.20208551463,5.09674746326108,10.));
#16892=CARTESIAN_POINT('',(328.20208551463,10.1934949265222,12.));
#16893=CARTESIAN_POINT('',(328.20208551463,5.09674746326108,12.));
#16894=CARTESIAN_POINT('',(328.20208551463,10.1934949265222,12.));
#16895=CARTESIAN_POINT('Origin',(326.70208551463,10.1934949265222,12.));
#16896=CARTESIAN_POINT('Origin',(326.70208551463,10.1934949265222,10.));
#16897=CARTESIAN_POINT('Origin',(326.70208551463,10.1934949265222,12.));
#16898=CARTESIAN_POINT('Origin',(275.051195932252,11.70240347792,12.));
#16899=CARTESIAN_POINT('',(277.551195932252,11.70240347792,12.));
#16900=CARTESIAN_POINT('Origin',(275.051195932252,11.70240347792,12.));
#16901=CARTESIAN_POINT('',(277.551195932252,11.70240347792,10.));
#16902=CARTESIAN_POINT('',(277.551195932252,11.70240347792,12.));
#16903=CARTESIAN_POINT('Origin',(275.051195932252,11.70240347792,10.));
#16904=CARTESIAN_POINT('Origin',(301.464086208118,11.70240347792,12.));
#16905=CARTESIAN_POINT('',(303.964086208118,11.70240347792,12.));
#16906=CARTESIAN_POINT('Origin',(301.464086208118,11.70240347792,12.));
#16907=CARTESIAN_POINT('',(303.964086208118,11.70240347792,10.));
#16908=CARTESIAN_POINT('',(303.964086208118,11.70240347792,12.));
#16909=CARTESIAN_POINT('Origin',(301.464086208118,11.70240347792,10.));
#16910=CARTESIAN_POINT('Origin',(301.464086208118,38.29759652208,12.));
#16911=CARTESIAN_POINT('',(303.964086208118,38.29759652208,12.));
#16912=CARTESIAN_POINT('Origin',(301.464086208118,38.29759652208,12.));
#16913=CARTESIAN_POINT('',(303.964086208118,38.29759652208,10.));
#16914=CARTESIAN_POINT('',(303.964086208118,38.29759652208,12.));
#16915=CARTESIAN_POINT('Origin',(301.464086208118,38.29759652208,10.));
#16916=CARTESIAN_POINT('Origin',(275.051195932252,38.29759652208,12.));
#16917=CARTESIAN_POINT('',(277.551195932252,38.29759652208,12.));
#16918=CARTESIAN_POINT('Origin',(275.051195932252,38.29759652208,12.));
#16919=CARTESIAN_POINT('',(277.551195932252,38.29759652208,10.));
#16920=CARTESIAN_POINT('',(277.551195932252,38.29759652208,12.));
#16921=CARTESIAN_POINT('Origin',(275.051195932252,38.29759652208,10.));
#16922=CARTESIAN_POINT('Origin',(288.257641070185,25.,12.));
#16923=CARTESIAN_POINT('',(298.257641070185,25.,12.));
#16924=CARTESIAN_POINT('Origin',(288.257641070185,25.,12.));
#16925=CARTESIAN_POINT('',(298.257641070185,25.,10.));
#16926=CARTESIAN_POINT('',(298.257641070185,25.,12.));
#16927=CARTESIAN_POINT('Origin',(288.257641070185,25.,10.));
#16928=CARTESIAN_POINT('Origin',(286.757641070185,39.8065050734778,12.));
#16929=CARTESIAN_POINT('',(286.757641070185,44.7051656728289,10.));
#16930=CARTESIAN_POINT('',(286.757641070185,39.8065050734778,10.));
#16931=CARTESIAN_POINT('',(286.757641070185,19.9032525367389,10.));
#16932=CARTESIAN_POINT('',(286.757641070185,44.7051656728289,12.));
#16933=CARTESIAN_POINT('',(286.757641070185,44.7051656728289,12.));
#16934=CARTESIAN_POINT('',(286.757641070185,39.8065050734778,12.));
#16935=CARTESIAN_POINT('',(286.757641070185,19.9032525367389,12.));
#16936=CARTESIAN_POINT('',(286.757641070185,39.8065050734778,12.));
#16937=CARTESIAN_POINT('Origin',(288.257641070185,39.8065050734778,12.));
#16938=CARTESIAN_POINT('',(289.757641070185,39.8065050734778,10.));
#16939=CARTESIAN_POINT('Origin',(288.257641070185,39.8065050734778,10.));
#16940=CARTESIAN_POINT('',(289.757641070185,39.8065050734778,12.));
#16941=CARTESIAN_POINT('Origin',(288.257641070185,39.8065050734778,12.));
#16942=CARTESIAN_POINT('',(289.757641070185,39.8065050734778,12.));
#16943=CARTESIAN_POINT('Origin',(289.757641070185,44.7051656728289,12.));
#16944=CARTESIAN_POINT('',(289.757641070185,44.7051656728289,10.));
#16945=CARTESIAN_POINT('',(289.757641070185,22.3525828364145,10.));
#16946=CARTESIAN_POINT('',(289.757641070185,44.7051656728289,12.));
#16947=CARTESIAN_POINT('',(289.757641070185,22.3525828364145,12.));
#16948=CARTESIAN_POINT('',(289.757641070185,44.7051656728289,12.));
#16949=CARTESIAN_POINT('Origin',(288.257641070185,44.7051656728289,12.));
#16950=CARTESIAN_POINT('Origin',(288.257641070185,44.7051656728289,10.));
#16951=CARTESIAN_POINT('Origin',(288.257641070185,44.7051656728289,12.));
#16952=CARTESIAN_POINT('Origin',(286.757641070185,5.29483432717106,12.));
#16953=CARTESIAN_POINT('',(286.757641070185,10.1934949265222,10.));
#16954=CARTESIAN_POINT('',(286.757641070185,5.29483432717106,10.));
#16955=CARTESIAN_POINT('',(286.757641070185,2.64741716358553,10.));
#16956=CARTESIAN_POINT('',(286.757641070185,10.1934949265222,12.));
#16957=CARTESIAN_POINT('',(286.757641070185,10.1934949265222,12.));
#16958=CARTESIAN_POINT('',(286.757641070185,5.29483432717106,12.));
#16959=CARTESIAN_POINT('',(286.757641070185,2.64741716358553,12.));
#16960=CARTESIAN_POINT('',(286.757641070185,5.29483432717106,12.));
#16961=CARTESIAN_POINT('Origin',(288.257641070185,5.29483432717106,12.));
#16962=CARTESIAN_POINT('',(289.757641070185,5.29483432717106,10.));
#16963=CARTESIAN_POINT('Origin',(288.257641070185,5.29483432717106,10.));
#16964=CARTESIAN_POINT('',(289.757641070185,5.29483432717106,12.));
#16965=CARTESIAN_POINT('Origin',(288.257641070185,5.29483432717106,12.));
#16966=CARTESIAN_POINT('',(289.757641070185,5.29483432717106,12.));
#16967=CARTESIAN_POINT('Origin',(289.757641070185,10.1934949265222,12.));
#16968=CARTESIAN_POINT('',(289.757641070185,10.1934949265222,10.));
#16969=CARTESIAN_POINT('',(289.757641070185,5.09674746326108,10.));
#16970=CARTESIAN_POINT('',(289.757641070185,10.1934949265222,12.));
#16971=CARTESIAN_POINT('',(289.757641070185,5.09674746326108,12.));
#16972=CARTESIAN_POINT('',(289.757641070185,10.1934949265222,12.));
#16973=CARTESIAN_POINT('Origin',(288.257641070185,10.1934949265222,12.));
#16974=CARTESIAN_POINT('Origin',(288.257641070185,10.1934949265222,10.));
#16975=CARTESIAN_POINT('Origin',(288.257641070185,10.1934949265222,12.));
#16976=CARTESIAN_POINT('Origin',(236.606751487807,11.70240347792,12.));
#16977=CARTESIAN_POINT('',(239.106751487807,11.70240347792,12.));
#16978=CARTESIAN_POINT('Origin',(236.606751487807,11.70240347792,12.));
#16979=CARTESIAN_POINT('',(239.106751487807,11.70240347792,10.));
#16980=CARTESIAN_POINT('',(239.106751487807,11.70240347792,12.));
#16981=CARTESIAN_POINT('Origin',(236.606751487807,11.70240347792,10.));
#16982=CARTESIAN_POINT('Origin',(263.019641763674,11.70240347792,12.));
#16983=CARTESIAN_POINT('',(265.519641763674,11.70240347792,12.));
#16984=CARTESIAN_POINT('Origin',(263.019641763674,11.70240347792,12.));
#16985=CARTESIAN_POINT('',(265.519641763674,11.70240347792,10.));
#16986=CARTESIAN_POINT('',(265.519641763674,11.70240347792,12.));
#16987=CARTESIAN_POINT('Origin',(263.019641763674,11.70240347792,10.));
#16988=CARTESIAN_POINT('Origin',(263.019641763674,38.29759652208,12.));
#16989=CARTESIAN_POINT('',(265.519641763674,38.29759652208,12.));
#16990=CARTESIAN_POINT('Origin',(263.019641763674,38.29759652208,12.));
#16991=CARTESIAN_POINT('',(265.519641763674,38.29759652208,10.));
#16992=CARTESIAN_POINT('',(265.519641763674,38.29759652208,12.));
#16993=CARTESIAN_POINT('Origin',(263.019641763674,38.29759652208,10.));
#16994=CARTESIAN_POINT('Origin',(236.606751487807,38.29759652208,12.));
#16995=CARTESIAN_POINT('',(239.106751487807,38.29759652208,12.));
#16996=CARTESIAN_POINT('Origin',(236.606751487807,38.29759652208,12.));
#16997=CARTESIAN_POINT('',(239.106751487807,38.29759652208,10.));
#16998=CARTESIAN_POINT('',(239.106751487807,38.29759652208,12.));
#16999=CARTESIAN_POINT('Origin',(236.606751487807,38.29759652208,10.));
#17000=CARTESIAN_POINT('Origin',(249.813196625741,25.,12.));
#17001=CARTESIAN_POINT('',(259.813196625741,25.,12.));
#17002=CARTESIAN_POINT('Origin',(249.813196625741,25.,12.));
#17003=CARTESIAN_POINT('',(259.813196625741,25.,10.));
#17004=CARTESIAN_POINT('',(259.813196625741,25.,12.));
#17005=CARTESIAN_POINT('Origin',(249.813196625741,25.,10.));
#17006=CARTESIAN_POINT('Origin',(248.313196625741,39.8065050734778,12.));
#17007=CARTESIAN_POINT('',(248.313196625741,44.7051656728289,10.));
#17008=CARTESIAN_POINT('',(248.313196625741,39.8065050734778,10.));
#17009=CARTESIAN_POINT('',(248.313196625741,19.9032525367389,10.));
#17010=CARTESIAN_POINT('',(248.313196625741,44.7051656728289,12.));
#17011=CARTESIAN_POINT('',(248.313196625741,44.7051656728289,12.));
#17012=CARTESIAN_POINT('',(248.313196625741,39.8065050734778,12.));
#17013=CARTESIAN_POINT('',(248.313196625741,19.9032525367389,12.));
#17014=CARTESIAN_POINT('',(248.313196625741,39.8065050734778,12.));
#17015=CARTESIAN_POINT('Origin',(249.813196625741,39.8065050734778,12.));
#17016=CARTESIAN_POINT('',(251.313196625741,39.8065050734778,10.));
#17017=CARTESIAN_POINT('Origin',(249.813196625741,39.8065050734778,10.));
#17018=CARTESIAN_POINT('',(251.313196625741,39.8065050734778,12.));
#17019=CARTESIAN_POINT('Origin',(249.813196625741,39.8065050734778,12.));
#17020=CARTESIAN_POINT('',(251.313196625741,39.8065050734778,12.));
#17021=CARTESIAN_POINT('Origin',(251.313196625741,44.7051656728289,12.));
#17022=CARTESIAN_POINT('',(251.313196625741,44.7051656728289,10.));
#17023=CARTESIAN_POINT('',(251.313196625741,22.3525828364145,10.));
#17024=CARTESIAN_POINT('',(251.313196625741,44.7051656728289,12.));
#17025=CARTESIAN_POINT('',(251.313196625741,22.3525828364145,12.));
#17026=CARTESIAN_POINT('',(251.313196625741,44.7051656728289,12.));
#17027=CARTESIAN_POINT('Origin',(249.813196625741,44.7051656728289,12.));
#17028=CARTESIAN_POINT('Origin',(249.813196625741,44.7051656728289,10.));
#17029=CARTESIAN_POINT('Origin',(249.813196625741,44.7051656728289,12.));
#17030=CARTESIAN_POINT('Origin',(248.313196625741,5.29483432717106,12.));
#17031=CARTESIAN_POINT('',(248.313196625741,10.1934949265222,10.));
#17032=CARTESIAN_POINT('',(248.313196625741,5.29483432717106,10.));
#17033=CARTESIAN_POINT('',(248.313196625741,2.64741716358553,10.));
#17034=CARTESIAN_POINT('',(248.313196625741,10.1934949265222,12.));
#17035=CARTESIAN_POINT('',(248.313196625741,10.1934949265222,12.));
#17036=CARTESIAN_POINT('',(248.313196625741,5.29483432717106,12.));
#17037=CARTESIAN_POINT('',(248.313196625741,2.64741716358553,12.));
#17038=CARTESIAN_POINT('',(248.313196625741,5.29483432717106,12.));
#17039=CARTESIAN_POINT('Origin',(249.813196625741,5.29483432717106,12.));
#17040=CARTESIAN_POINT('',(251.313196625741,5.29483432717106,10.));
#17041=CARTESIAN_POINT('Origin',(249.813196625741,5.29483432717106,10.));
#17042=CARTESIAN_POINT('',(251.313196625741,5.29483432717106,12.));
#17043=CARTESIAN_POINT('Origin',(249.813196625741,5.29483432717106,12.));
#17044=CARTESIAN_POINT('',(251.313196625741,5.29483432717106,12.));
#17045=CARTESIAN_POINT('Origin',(251.313196625741,10.1934949265222,12.));
#17046=CARTESIAN_POINT('',(251.313196625741,10.1934949265222,10.));
#17047=CARTESIAN_POINT('',(251.313196625741,5.09674746326108,10.));
#17048=CARTESIAN_POINT('',(251.313196625741,10.1934949265222,12.));
#17049=CARTESIAN_POINT('',(251.313196625741,5.09674746326108,12.));
#17050=CARTESIAN_POINT('',(251.313196625741,10.1934949265222,12.));
#17051=CARTESIAN_POINT('Origin',(249.813196625741,10.1934949265222,12.));
#17052=CARTESIAN_POINT('Origin',(249.813196625741,10.1934949265222,10.));
#17053=CARTESIAN_POINT('Origin',(249.813196625741,10.1934949265222,12.));
#17054=CARTESIAN_POINT('Origin',(198.162307043363,11.70240347792,12.));
#17055=CARTESIAN_POINT('',(200.662307043363,11.70240347792,12.));
#17056=CARTESIAN_POINT('Origin',(198.162307043363,11.70240347792,12.));
#17057=CARTESIAN_POINT('',(200.662307043363,11.70240347792,10.));
#17058=CARTESIAN_POINT('',(200.662307043363,11.70240347792,12.));
#17059=CARTESIAN_POINT('Origin',(198.162307043363,11.70240347792,10.));
#17060=CARTESIAN_POINT('Origin',(224.575197319229,11.70240347792,12.));
#17061=CARTESIAN_POINT('',(227.075197319229,11.70240347792,12.));
#17062=CARTESIAN_POINT('Origin',(224.575197319229,11.70240347792,12.));
#17063=CARTESIAN_POINT('',(227.075197319229,11.70240347792,10.));
#17064=CARTESIAN_POINT('',(227.075197319229,11.70240347792,12.));
#17065=CARTESIAN_POINT('Origin',(224.575197319229,11.70240347792,10.));
#17066=CARTESIAN_POINT('Origin',(224.575197319229,38.29759652208,12.));
#17067=CARTESIAN_POINT('',(227.075197319229,38.29759652208,12.));
#17068=CARTESIAN_POINT('Origin',(224.575197319229,38.29759652208,12.));
#17069=CARTESIAN_POINT('',(227.075197319229,38.29759652208,10.));
#17070=CARTESIAN_POINT('',(227.075197319229,38.29759652208,12.));
#17071=CARTESIAN_POINT('Origin',(224.575197319229,38.29759652208,10.));
#17072=CARTESIAN_POINT('Origin',(198.162307043363,38.29759652208,12.));
#17073=CARTESIAN_POINT('',(200.662307043363,38.29759652208,12.));
#17074=CARTESIAN_POINT('Origin',(198.162307043363,38.29759652208,12.));
#17075=CARTESIAN_POINT('',(200.662307043363,38.29759652208,10.));
#17076=CARTESIAN_POINT('',(200.662307043363,38.29759652208,12.));
#17077=CARTESIAN_POINT('Origin',(198.162307043363,38.29759652208,10.));
#17078=CARTESIAN_POINT('Origin',(211.368752181296,25.,12.));
#17079=CARTESIAN_POINT('',(221.368752181296,25.,12.));
#17080=CARTESIAN_POINT('Origin',(211.368752181296,25.,12.));
#17081=CARTESIAN_POINT('',(221.368752181296,25.,10.));
#17082=CARTESIAN_POINT('',(221.368752181296,25.,12.));
#17083=CARTESIAN_POINT('Origin',(211.368752181296,25.,10.));
#17084=CARTESIAN_POINT('Origin',(209.868752181296,39.8065050734778,12.));
#17085=CARTESIAN_POINT('',(209.868752181296,44.7051656728289,10.));
#17086=CARTESIAN_POINT('',(209.868752181296,39.8065050734778,10.));
#17087=CARTESIAN_POINT('',(209.868752181296,19.9032525367389,10.));
#17088=CARTESIAN_POINT('',(209.868752181296,44.7051656728289,12.));
#17089=CARTESIAN_POINT('',(209.868752181296,44.7051656728289,12.));
#17090=CARTESIAN_POINT('',(209.868752181296,39.8065050734778,12.));
#17091=CARTESIAN_POINT('',(209.868752181296,19.9032525367389,12.));
#17092=CARTESIAN_POINT('',(209.868752181296,39.8065050734778,12.));
#17093=CARTESIAN_POINT('Origin',(211.368752181296,39.8065050734778,12.));
#17094=CARTESIAN_POINT('',(212.868752181296,39.8065050734778,10.));
#17095=CARTESIAN_POINT('Origin',(211.368752181296,39.8065050734778,10.));
#17096=CARTESIAN_POINT('',(212.868752181296,39.8065050734778,12.));
#17097=CARTESIAN_POINT('Origin',(211.368752181296,39.8065050734778,12.));
#17098=CARTESIAN_POINT('',(212.868752181296,39.8065050734778,12.));
#17099=CARTESIAN_POINT('Origin',(212.868752181296,44.7051656728289,12.));
#17100=CARTESIAN_POINT('',(212.868752181296,44.7051656728289,10.));
#17101=CARTESIAN_POINT('',(212.868752181296,22.3525828364145,10.));
#17102=CARTESIAN_POINT('',(212.868752181296,44.7051656728289,12.));
#17103=CARTESIAN_POINT('',(212.868752181296,22.3525828364145,12.));
#17104=CARTESIAN_POINT('',(212.868752181296,44.7051656728289,12.));
#17105=CARTESIAN_POINT('Origin',(211.368752181296,44.7051656728289,12.));
#17106=CARTESIAN_POINT('Origin',(211.368752181296,44.7051656728289,10.));
#17107=CARTESIAN_POINT('Origin',(211.368752181296,44.7051656728289,12.));
#17108=CARTESIAN_POINT('Origin',(209.868752181296,5.29483432717106,12.));
#17109=CARTESIAN_POINT('',(209.868752181296,10.1934949265222,10.));
#17110=CARTESIAN_POINT('',(209.868752181296,5.29483432717106,10.));
#17111=CARTESIAN_POINT('',(209.868752181296,2.64741716358553,10.));
#17112=CARTESIAN_POINT('',(209.868752181296,10.1934949265222,12.));
#17113=CARTESIAN_POINT('',(209.868752181296,10.1934949265222,12.));
#17114=CARTESIAN_POINT('',(209.868752181296,5.29483432717106,12.));
#17115=CARTESIAN_POINT('',(209.868752181296,2.64741716358553,12.));
#17116=CARTESIAN_POINT('',(209.868752181296,5.29483432717106,12.));
#17117=CARTESIAN_POINT('Origin',(211.368752181296,5.29483432717106,12.));
#17118=CARTESIAN_POINT('',(212.868752181296,5.29483432717106,10.));
#17119=CARTESIAN_POINT('Origin',(211.368752181296,5.29483432717106,10.));
#17120=CARTESIAN_POINT('',(212.868752181296,5.29483432717106,12.));
#17121=CARTESIAN_POINT('Origin',(211.368752181296,5.29483432717106,12.));
#17122=CARTESIAN_POINT('',(212.868752181296,5.29483432717106,12.));
#17123=CARTESIAN_POINT('Origin',(212.868752181296,10.1934949265222,12.));
#17124=CARTESIAN_POINT('',(212.868752181296,10.1934949265222,10.));
#17125=CARTESIAN_POINT('',(212.868752181296,5.09674746326108,10.));
#17126=CARTESIAN_POINT('',(212.868752181296,10.1934949265222,12.));
#17127=CARTESIAN_POINT('',(212.868752181296,5.09674746326108,12.));
#17128=CARTESIAN_POINT('',(212.868752181296,10.1934949265222,12.));
#17129=CARTESIAN_POINT('Origin',(211.368752181296,10.1934949265222,12.));
#17130=CARTESIAN_POINT('Origin',(211.368752181296,10.1934949265222,10.));
#17131=CARTESIAN_POINT('Origin',(211.368752181296,10.1934949265222,12.));
#17132=CARTESIAN_POINT('Origin',(159.717862598919,11.70240347792,12.));
#17133=CARTESIAN_POINT('',(162.217862598919,11.70240347792,12.));
#17134=CARTESIAN_POINT('Origin',(159.717862598919,11.70240347792,12.));
#17135=CARTESIAN_POINT('',(162.217862598919,11.70240347792,10.));
#17136=CARTESIAN_POINT('',(162.217862598919,11.70240347792,12.));
#17137=CARTESIAN_POINT('Origin',(159.717862598919,11.70240347792,10.));
#17138=CARTESIAN_POINT('Origin',(186.130752874785,11.70240347792,12.));
#17139=CARTESIAN_POINT('',(188.630752874785,11.70240347792,12.));
#17140=CARTESIAN_POINT('Origin',(186.130752874785,11.70240347792,12.));
#17141=CARTESIAN_POINT('',(188.630752874785,11.70240347792,10.));
#17142=CARTESIAN_POINT('',(188.630752874785,11.70240347792,12.));
#17143=CARTESIAN_POINT('Origin',(186.130752874785,11.70240347792,10.));
#17144=CARTESIAN_POINT('Origin',(186.130752874785,38.29759652208,12.));
#17145=CARTESIAN_POINT('',(188.630752874785,38.29759652208,12.));
#17146=CARTESIAN_POINT('Origin',(186.130752874785,38.29759652208,12.));
#17147=CARTESIAN_POINT('',(188.630752874785,38.29759652208,10.));
#17148=CARTESIAN_POINT('',(188.630752874785,38.29759652208,12.));
#17149=CARTESIAN_POINT('Origin',(186.130752874785,38.29759652208,10.));
#17150=CARTESIAN_POINT('Origin',(159.717862598919,38.29759652208,12.));
#17151=CARTESIAN_POINT('',(162.217862598919,38.29759652208,12.));
#17152=CARTESIAN_POINT('Origin',(159.717862598919,38.29759652208,12.));
#17153=CARTESIAN_POINT('',(162.217862598919,38.29759652208,10.));
#17154=CARTESIAN_POINT('',(162.217862598919,38.29759652208,12.));
#17155=CARTESIAN_POINT('Origin',(159.717862598919,38.29759652208,10.));
#17156=CARTESIAN_POINT('Origin',(172.924307736852,25.,12.));
#17157=CARTESIAN_POINT('',(182.924307736852,25.,12.));
#17158=CARTESIAN_POINT('Origin',(172.924307736852,25.,12.));
#17159=CARTESIAN_POINT('',(182.924307736852,25.,10.));
#17160=CARTESIAN_POINT('',(182.924307736852,25.,12.));
#17161=CARTESIAN_POINT('Origin',(172.924307736852,25.,10.));
#17162=CARTESIAN_POINT('Origin',(171.424307736852,39.8065050734778,12.));
#17163=CARTESIAN_POINT('',(171.424307736852,44.7051656728289,10.));
#17164=CARTESIAN_POINT('',(171.424307736852,39.8065050734778,10.));
#17165=CARTESIAN_POINT('',(171.424307736852,19.9032525367389,10.));
#17166=CARTESIAN_POINT('',(171.424307736852,44.7051656728289,12.));
#17167=CARTESIAN_POINT('',(171.424307736852,44.7051656728289,12.));
#17168=CARTESIAN_POINT('',(171.424307736852,39.8065050734778,12.));
#17169=CARTESIAN_POINT('',(171.424307736852,19.9032525367389,12.));
#17170=CARTESIAN_POINT('',(171.424307736852,39.8065050734778,12.));
#17171=CARTESIAN_POINT('Origin',(172.924307736852,39.8065050734778,12.));
#17172=CARTESIAN_POINT('',(174.424307736852,39.8065050734778,10.));
#17173=CARTESIAN_POINT('Origin',(172.924307736852,39.8065050734778,10.));
#17174=CARTESIAN_POINT('',(174.424307736852,39.8065050734778,12.));
#17175=CARTESIAN_POINT('Origin',(172.924307736852,39.8065050734778,12.));
#17176=CARTESIAN_POINT('',(174.424307736852,39.8065050734778,12.));
#17177=CARTESIAN_POINT('Origin',(174.424307736852,44.7051656728289,12.));
#17178=CARTESIAN_POINT('',(174.424307736852,44.7051656728289,10.));
#17179=CARTESIAN_POINT('',(174.424307736852,22.3525828364145,10.));
#17180=CARTESIAN_POINT('',(174.424307736852,44.7051656728289,12.));
#17181=CARTESIAN_POINT('',(174.424307736852,22.3525828364145,12.));
#17182=CARTESIAN_POINT('',(174.424307736852,44.7051656728289,12.));
#17183=CARTESIAN_POINT('Origin',(172.924307736852,44.7051656728289,12.));
#17184=CARTESIAN_POINT('Origin',(172.924307736852,44.7051656728289,10.));
#17185=CARTESIAN_POINT('Origin',(172.924307736852,44.7051656728289,12.));
#17186=CARTESIAN_POINT('Origin',(171.424307736852,5.29483432717106,12.));
#17187=CARTESIAN_POINT('',(171.424307736852,10.1934949265222,10.));
#17188=CARTESIAN_POINT('',(171.424307736852,5.29483432717106,10.));
#17189=CARTESIAN_POINT('',(171.424307736852,2.64741716358553,10.));
#17190=CARTESIAN_POINT('',(171.424307736852,10.1934949265222,12.));
#17191=CARTESIAN_POINT('',(171.424307736852,10.1934949265222,12.));
#17192=CARTESIAN_POINT('',(171.424307736852,5.29483432717106,12.));
#17193=CARTESIAN_POINT('',(171.424307736852,2.64741716358553,12.));
#17194=CARTESIAN_POINT('',(171.424307736852,5.29483432717106,12.));
#17195=CARTESIAN_POINT('Origin',(172.924307736852,5.29483432717106,12.));
#17196=CARTESIAN_POINT('',(174.424307736852,5.29483432717106,10.));
#17197=CARTESIAN_POINT('Origin',(172.924307736852,5.29483432717106,10.));
#17198=CARTESIAN_POINT('',(174.424307736852,5.29483432717106,12.));
#17199=CARTESIAN_POINT('Origin',(172.924307736852,5.29483432717106,12.));
#17200=CARTESIAN_POINT('',(174.424307736852,5.29483432717106,12.));
#17201=CARTESIAN_POINT('Origin',(174.424307736852,10.1934949265222,12.));
#17202=CARTESIAN_POINT('',(174.424307736852,10.1934949265222,10.));
#17203=CARTESIAN_POINT('',(174.424307736852,5.09674746326108,10.));
#17204=CARTESIAN_POINT('',(174.424307736852,10.1934949265222,12.));
#17205=CARTESIAN_POINT('',(174.424307736852,5.09674746326108,12.));
#17206=CARTESIAN_POINT('',(174.424307736852,10.1934949265222,12.));
#17207=CARTESIAN_POINT('Origin',(172.924307736852,10.1934949265222,12.));
#17208=CARTESIAN_POINT('Origin',(172.924307736852,10.1934949265222,10.));
#17209=CARTESIAN_POINT('Origin',(172.924307736852,10.1934949265222,12.));
#17210=CARTESIAN_POINT('Origin',(121.273418154474,11.70240347792,12.));
#17211=CARTESIAN_POINT('',(123.773418154474,11.70240347792,12.));
#17212=CARTESIAN_POINT('Origin',(121.273418154474,11.70240347792,12.));
#17213=CARTESIAN_POINT('',(123.773418154474,11.70240347792,10.));
#17214=CARTESIAN_POINT('',(123.773418154474,11.70240347792,12.));
#17215=CARTESIAN_POINT('Origin',(121.273418154474,11.70240347792,10.));
#17216=CARTESIAN_POINT('Origin',(147.686308430341,11.70240347792,12.));
#17217=CARTESIAN_POINT('',(150.186308430341,11.70240347792,12.));
#17218=CARTESIAN_POINT('Origin',(147.686308430341,11.70240347792,12.));
#17219=CARTESIAN_POINT('',(150.186308430341,11.70240347792,10.));
#17220=CARTESIAN_POINT('',(150.186308430341,11.70240347792,12.));
#17221=CARTESIAN_POINT('Origin',(147.686308430341,11.70240347792,10.));
#17222=CARTESIAN_POINT('Origin',(147.686308430341,38.29759652208,12.));
#17223=CARTESIAN_POINT('',(150.186308430341,38.29759652208,12.));
#17224=CARTESIAN_POINT('Origin',(147.686308430341,38.29759652208,12.));
#17225=CARTESIAN_POINT('',(150.186308430341,38.29759652208,10.));
#17226=CARTESIAN_POINT('',(150.186308430341,38.29759652208,12.));
#17227=CARTESIAN_POINT('Origin',(147.686308430341,38.29759652208,10.));
#17228=CARTESIAN_POINT('Origin',(121.273418154474,38.29759652208,12.));
#17229=CARTESIAN_POINT('',(123.773418154474,38.29759652208,12.));
#17230=CARTESIAN_POINT('Origin',(121.273418154474,38.29759652208,12.));
#17231=CARTESIAN_POINT('',(123.773418154474,38.29759652208,10.));
#17232=CARTESIAN_POINT('',(123.773418154474,38.29759652208,12.));
#17233=CARTESIAN_POINT('Origin',(121.273418154474,38.29759652208,10.));
#17234=CARTESIAN_POINT('Origin',(134.479863292407,25.,12.));
#17235=CARTESIAN_POINT('',(144.479863292407,25.,12.));
#17236=CARTESIAN_POINT('Origin',(134.479863292407,25.,12.));
#17237=CARTESIAN_POINT('',(144.479863292407,25.,10.));
#17238=CARTESIAN_POINT('',(144.479863292407,25.,12.));
#17239=CARTESIAN_POINT('Origin',(134.479863292407,25.,10.));
#17240=CARTESIAN_POINT('Origin',(132.979863292407,39.8065050734778,12.));
#17241=CARTESIAN_POINT('',(132.979863292407,44.7051656728289,10.));
#17242=CARTESIAN_POINT('',(132.979863292407,39.8065050734778,10.));
#17243=CARTESIAN_POINT('',(132.979863292407,19.9032525367389,10.));
#17244=CARTESIAN_POINT('',(132.979863292407,44.7051656728289,12.));
#17245=CARTESIAN_POINT('',(132.979863292407,44.7051656728289,12.));
#17246=CARTESIAN_POINT('',(132.979863292407,39.8065050734778,12.));
#17247=CARTESIAN_POINT('',(132.979863292407,19.9032525367389,12.));
#17248=CARTESIAN_POINT('',(132.979863292407,39.8065050734778,12.));
#17249=CARTESIAN_POINT('Origin',(134.479863292407,39.8065050734778,12.));
#17250=CARTESIAN_POINT('',(135.979863292407,39.8065050734778,10.));
#17251=CARTESIAN_POINT('Origin',(134.479863292407,39.8065050734778,10.));
#17252=CARTESIAN_POINT('',(135.979863292407,39.8065050734778,12.));
#17253=CARTESIAN_POINT('Origin',(134.479863292407,39.8065050734778,12.));
#17254=CARTESIAN_POINT('',(135.979863292407,39.8065050734778,12.));
#17255=CARTESIAN_POINT('Origin',(135.979863292407,44.7051656728289,12.));
#17256=CARTESIAN_POINT('',(135.979863292407,44.7051656728289,10.));
#17257=CARTESIAN_POINT('',(135.979863292407,22.3525828364145,10.));
#17258=CARTESIAN_POINT('',(135.979863292407,44.7051656728289,12.));
#17259=CARTESIAN_POINT('',(135.979863292407,22.3525828364145,12.));
#17260=CARTESIAN_POINT('',(135.979863292407,44.7051656728289,12.));
#17261=CARTESIAN_POINT('Origin',(134.479863292407,44.7051656728289,12.));
#17262=CARTESIAN_POINT('Origin',(134.479863292407,44.7051656728289,10.));
#17263=CARTESIAN_POINT('Origin',(134.479863292407,44.7051656728289,12.));
#17264=CARTESIAN_POINT('Origin',(132.979863292407,5.29483432717106,12.));
#17265=CARTESIAN_POINT('',(132.979863292407,10.1934949265222,10.));
#17266=CARTESIAN_POINT('',(132.979863292407,5.29483432717106,10.));
#17267=CARTESIAN_POINT('',(132.979863292407,2.64741716358553,10.));
#17268=CARTESIAN_POINT('',(132.979863292407,10.1934949265222,12.));
#17269=CARTESIAN_POINT('',(132.979863292407,10.1934949265222,12.));
#17270=CARTESIAN_POINT('',(132.979863292407,5.29483432717106,12.));
#17271=CARTESIAN_POINT('',(132.979863292407,2.64741716358553,12.));
#17272=CARTESIAN_POINT('',(132.979863292407,5.29483432717106,12.));
#17273=CARTESIAN_POINT('Origin',(134.479863292407,5.29483432717106,12.));
#17274=CARTESIAN_POINT('',(135.979863292407,5.29483432717106,10.));
#17275=CARTESIAN_POINT('Origin',(134.479863292407,5.29483432717106,10.));
#17276=CARTESIAN_POINT('',(135.979863292407,5.29483432717106,12.));
#17277=CARTESIAN_POINT('Origin',(134.479863292407,5.29483432717106,12.));
#17278=CARTESIAN_POINT('',(135.979863292407,5.29483432717106,12.));
#17279=CARTESIAN_POINT('Origin',(135.979863292407,10.1934949265222,12.));
#17280=CARTESIAN_POINT('',(135.979863292407,10.1934949265222,10.));
#17281=CARTESIAN_POINT('',(135.979863292407,5.09674746326108,10.));
#17282=CARTESIAN_POINT('',(135.979863292407,10.1934949265222,12.));
#17283=CARTESIAN_POINT('',(135.979863292407,5.09674746326108,12.));
#17284=CARTESIAN_POINT('',(135.979863292407,10.1934949265222,12.));
#17285=CARTESIAN_POINT('Origin',(134.479863292407,10.1934949265222,12.));
#17286=CARTESIAN_POINT('Origin',(134.479863292407,10.1934949265222,10.));
#17287=CARTESIAN_POINT('Origin',(134.479863292407,10.1934949265222,12.));
#17288=CARTESIAN_POINT('Origin',(82.8289737100297,11.70240347792,12.));
#17289=CARTESIAN_POINT('',(85.3289737100297,11.70240347792,12.));
#17290=CARTESIAN_POINT('Origin',(82.8289737100297,11.70240347792,12.));
#17291=CARTESIAN_POINT('',(85.3289737100297,11.70240347792,10.));
#17292=CARTESIAN_POINT('',(85.3289737100297,11.70240347792,12.));
#17293=CARTESIAN_POINT('Origin',(82.8289737100297,11.70240347792,10.));
#17294=CARTESIAN_POINT('Origin',(109.241863985896,11.70240347792,12.));
#17295=CARTESIAN_POINT('',(111.741863985896,11.70240347792,12.));
#17296=CARTESIAN_POINT('Origin',(109.241863985896,11.70240347792,12.));
#17297=CARTESIAN_POINT('',(111.741863985896,11.70240347792,10.));
#17298=CARTESIAN_POINT('',(111.741863985896,11.70240347792,12.));
#17299=CARTESIAN_POINT('Origin',(109.241863985896,11.70240347792,10.));
#17300=CARTESIAN_POINT('Origin',(109.241863985896,38.29759652208,12.));
#17301=CARTESIAN_POINT('',(111.741863985896,38.29759652208,12.));
#17302=CARTESIAN_POINT('Origin',(109.241863985896,38.29759652208,12.));
#17303=CARTESIAN_POINT('',(111.741863985896,38.29759652208,10.));
#17304=CARTESIAN_POINT('',(111.741863985896,38.29759652208,12.));
#17305=CARTESIAN_POINT('Origin',(109.241863985896,38.29759652208,10.));
#17306=CARTESIAN_POINT('Origin',(82.8289737100297,38.29759652208,12.));
#17307=CARTESIAN_POINT('',(85.3289737100297,38.29759652208,12.));
#17308=CARTESIAN_POINT('Origin',(82.8289737100297,38.29759652208,12.));
#17309=CARTESIAN_POINT('',(85.3289737100297,38.29759652208,10.));
#17310=CARTESIAN_POINT('',(85.3289737100297,38.29759652208,12.));
#17311=CARTESIAN_POINT('Origin',(82.8289737100297,38.29759652208,10.));
#17312=CARTESIAN_POINT('Origin',(96.0354188479629,25.,12.));
#17313=CARTESIAN_POINT('',(106.035418847963,25.,12.));
#17314=CARTESIAN_POINT('Origin',(96.0354188479629,25.,12.));
#17315=CARTESIAN_POINT('',(106.035418847963,25.,10.));
#17316=CARTESIAN_POINT('',(106.035418847963,25.,12.));
#17317=CARTESIAN_POINT('Origin',(96.0354188479629,25.,10.));
#17318=CARTESIAN_POINT('Origin',(94.5354188479629,39.8065050734778,12.));
#17319=CARTESIAN_POINT('',(94.5354188479629,44.7051656728289,10.));
#17320=CARTESIAN_POINT('',(94.5354188479629,39.8065050734778,10.));
#17321=CARTESIAN_POINT('',(94.5354188479629,19.9032525367389,10.));
#17322=CARTESIAN_POINT('',(94.5354188479629,44.7051656728289,12.));
#17323=CARTESIAN_POINT('',(94.5354188479629,44.7051656728289,12.));
#17324=CARTESIAN_POINT('',(94.5354188479629,39.8065050734778,12.));
#17325=CARTESIAN_POINT('',(94.5354188479629,19.9032525367389,12.));
#17326=CARTESIAN_POINT('',(94.5354188479629,39.8065050734778,12.));
#17327=CARTESIAN_POINT('Origin',(96.0354188479629,39.8065050734778,12.));
#17328=CARTESIAN_POINT('',(97.5354188479629,39.8065050734778,10.));
#17329=CARTESIAN_POINT('Origin',(96.0354188479629,39.8065050734778,10.));
#17330=CARTESIAN_POINT('',(97.5354188479629,39.8065050734778,12.));
#17331=CARTESIAN_POINT('Origin',(96.0354188479629,39.8065050734778,12.));
#17332=CARTESIAN_POINT('',(97.5354188479629,39.8065050734778,12.));
#17333=CARTESIAN_POINT('Origin',(97.5354188479629,44.7051656728289,12.));
#17334=CARTESIAN_POINT('',(97.5354188479629,44.7051656728289,10.));
#17335=CARTESIAN_POINT('',(97.5354188479629,22.3525828364145,10.));
#17336=CARTESIAN_POINT('',(97.5354188479629,44.7051656728289,12.));
#17337=CARTESIAN_POINT('',(97.5354188479629,22.3525828364145,12.));
#17338=CARTESIAN_POINT('',(97.5354188479629,44.7051656728289,12.));
#17339=CARTESIAN_POINT('Origin',(96.0354188479629,44.7051656728289,12.));
#17340=CARTESIAN_POINT('Origin',(96.0354188479629,44.7051656728289,10.));
#17341=CARTESIAN_POINT('Origin',(96.0354188479629,44.7051656728289,12.));
#17342=CARTESIAN_POINT('Origin',(94.5354188479629,5.29483432717106,12.));
#17343=CARTESIAN_POINT('',(94.5354188479629,10.1934949265222,10.));
#17344=CARTESIAN_POINT('',(94.5354188479629,5.29483432717106,10.));
#17345=CARTESIAN_POINT('',(94.5354188479629,2.64741716358553,10.));
#17346=CARTESIAN_POINT('',(94.5354188479629,10.1934949265222,12.));
#17347=CARTESIAN_POINT('',(94.5354188479629,10.1934949265222,12.));
#17348=CARTESIAN_POINT('',(94.5354188479629,5.29483432717106,12.));
#17349=CARTESIAN_POINT('',(94.5354188479629,2.64741716358553,12.));
#17350=CARTESIAN_POINT('',(94.5354188479629,5.29483432717106,12.));
#17351=CARTESIAN_POINT('Origin',(96.0354188479629,5.29483432717106,12.));
#17352=CARTESIAN_POINT('',(97.5354188479629,5.29483432717106,10.));
#17353=CARTESIAN_POINT('Origin',(96.0354188479629,5.29483432717106,10.));
#17354=CARTESIAN_POINT('',(97.5354188479629,5.29483432717106,12.));
#17355=CARTESIAN_POINT('Origin',(96.0354188479629,5.29483432717106,12.));
#17356=CARTESIAN_POINT('',(97.5354188479629,5.29483432717106,12.));
#17357=CARTESIAN_POINT('Origin',(97.5354188479629,10.1934949265222,12.));
#17358=CARTESIAN_POINT('',(97.5354188479629,10.1934949265222,10.));
#17359=CARTESIAN_POINT('',(97.5354188479629,5.09674746326108,10.));
#17360=CARTESIAN_POINT('',(97.5354188479629,10.1934949265222,12.));
#17361=CARTESIAN_POINT('',(97.5354188479629,5.09674746326108,12.));
#17362=CARTESIAN_POINT('',(97.5354188479629,10.1934949265222,12.));
#17363=CARTESIAN_POINT('Origin',(96.0354188479629,10.1934949265222,12.));
#17364=CARTESIAN_POINT('Origin',(96.0354188479629,10.1934949265222,10.));
#17365=CARTESIAN_POINT('Origin',(96.0354188479629,10.1934949265222,12.));
#17366=CARTESIAN_POINT('Origin',(44.3845292655852,11.70240347792,12.));
#17367=CARTESIAN_POINT('',(46.8845292655852,11.70240347792,12.));
#17368=CARTESIAN_POINT('Origin',(44.3845292655852,11.70240347792,12.));
#17369=CARTESIAN_POINT('',(46.8845292655852,11.70240347792,10.));
#17370=CARTESIAN_POINT('',(46.8845292655852,11.70240347792,12.));
#17371=CARTESIAN_POINT('Origin',(44.3845292655852,11.70240347792,10.));
#17372=CARTESIAN_POINT('Origin',(70.7974195414516,11.70240347792,12.));
#17373=CARTESIAN_POINT('',(73.2974195414516,11.70240347792,12.));
#17374=CARTESIAN_POINT('Origin',(70.7974195414516,11.70240347792,12.));
#17375=CARTESIAN_POINT('',(73.2974195414516,11.70240347792,10.));
#17376=CARTESIAN_POINT('',(73.2974195414516,11.70240347792,12.));
#17377=CARTESIAN_POINT('Origin',(70.7974195414516,11.70240347792,10.));
#17378=CARTESIAN_POINT('Origin',(70.7974195414516,38.29759652208,12.));
#17379=CARTESIAN_POINT('',(73.2974195414516,38.29759652208,12.));
#17380=CARTESIAN_POINT('Origin',(70.7974195414516,38.29759652208,12.));
#17381=CARTESIAN_POINT('',(73.2974195414516,38.29759652208,10.));
#17382=CARTESIAN_POINT('',(73.2974195414516,38.29759652208,12.));
#17383=CARTESIAN_POINT('Origin',(70.7974195414516,38.29759652208,10.));
#17384=CARTESIAN_POINT('Origin',(44.3845292655852,38.29759652208,12.));
#17385=CARTESIAN_POINT('',(46.8845292655852,38.29759652208,12.));
#17386=CARTESIAN_POINT('Origin',(44.3845292655852,38.29759652208,12.));
#17387=CARTESIAN_POINT('',(46.8845292655852,38.29759652208,10.));
#17388=CARTESIAN_POINT('',(46.8845292655852,38.29759652208,12.));
#17389=CARTESIAN_POINT('Origin',(44.3845292655852,38.29759652208,10.));
#17390=CARTESIAN_POINT('Origin',(57.5909744035184,25.,12.));
#17391=CARTESIAN_POINT('',(67.5909744035184,25.,12.));
#17392=CARTESIAN_POINT('Origin',(57.5909744035184,25.,12.));
#17393=CARTESIAN_POINT('',(67.5909744035184,25.,10.));
#17394=CARTESIAN_POINT('',(67.5909744035184,25.,12.));
#17395=CARTESIAN_POINT('Origin',(57.5909744035184,25.,10.));
#17396=CARTESIAN_POINT('Origin',(56.0909744035184,39.8065050734778,12.));
#17397=CARTESIAN_POINT('',(56.0909744035184,44.7051656728289,10.));
#17398=CARTESIAN_POINT('',(56.0909744035184,39.8065050734778,10.));
#17399=CARTESIAN_POINT('',(56.0909744035185,19.9032525367389,10.));
#17400=CARTESIAN_POINT('',(56.0909744035184,44.7051656728289,12.));
#17401=CARTESIAN_POINT('',(56.0909744035184,44.7051656728289,12.));
#17402=CARTESIAN_POINT('',(56.0909744035184,39.8065050734778,12.));
#17403=CARTESIAN_POINT('',(56.0909744035184,19.9032525367389,12.));
#17404=CARTESIAN_POINT('',(56.0909744035184,39.8065050734778,12.));
#17405=CARTESIAN_POINT('Origin',(57.5909744035184,39.8065050734778,12.));
#17406=CARTESIAN_POINT('',(59.0909744035184,39.8065050734778,10.));
#17407=CARTESIAN_POINT('Origin',(57.5909744035184,39.8065050734778,10.));
#17408=CARTESIAN_POINT('',(59.0909744035184,39.8065050734778,12.));
#17409=CARTESIAN_POINT('Origin',(57.5909744035184,39.8065050734778,12.));
#17410=CARTESIAN_POINT('',(59.0909744035184,39.8065050734778,12.));
#17411=CARTESIAN_POINT('Origin',(59.0909744035184,44.7051656728289,12.));
#17412=CARTESIAN_POINT('',(59.0909744035184,44.7051656728289,10.));
#17413=CARTESIAN_POINT('',(59.0909744035184,22.3525828364145,10.));
#17414=CARTESIAN_POINT('',(59.0909744035184,44.7051656728289,12.));
#17415=CARTESIAN_POINT('',(59.0909744035184,22.3525828364145,12.));
#17416=CARTESIAN_POINT('',(59.0909744035184,44.7051656728289,12.));
#17417=CARTESIAN_POINT('Origin',(57.5909744035184,44.7051656728289,12.));
#17418=CARTESIAN_POINT('Origin',(57.5909744035184,44.7051656728289,10.));
#17419=CARTESIAN_POINT('Origin',(57.5909744035184,44.7051656728289,12.));
#17420=CARTESIAN_POINT('Origin',(56.0909744035184,5.29483432717106,12.));
#17421=CARTESIAN_POINT('',(56.0909744035184,10.1934949265222,10.));
#17422=CARTESIAN_POINT('',(56.0909744035184,5.29483432717106,10.));
#17423=CARTESIAN_POINT('',(56.0909744035185,2.64741716358553,10.));
#17424=CARTESIAN_POINT('',(56.0909744035184,10.1934949265222,12.));
#17425=CARTESIAN_POINT('',(56.0909744035184,10.1934949265222,12.));
#17426=CARTESIAN_POINT('',(56.0909744035184,5.29483432717106,12.));
#17427=CARTESIAN_POINT('',(56.0909744035184,2.64741716358553,12.));
#17428=CARTESIAN_POINT('',(56.0909744035184,5.29483432717106,12.));
#17429=CARTESIAN_POINT('Origin',(57.5909744035184,5.29483432717106,12.));
#17430=CARTESIAN_POINT('',(59.0909744035184,5.29483432717106,10.));
#17431=CARTESIAN_POINT('Origin',(57.5909744035184,5.29483432717106,10.));
#17432=CARTESIAN_POINT('',(59.0909744035184,5.29483432717106,12.));
#17433=CARTESIAN_POINT('Origin',(57.5909744035184,5.29483432717106,12.));
#17434=CARTESIAN_POINT('',(59.0909744035184,5.29483432717106,12.));
#17435=CARTESIAN_POINT('Origin',(59.0909744035184,10.1934949265222,12.));
#17436=CARTESIAN_POINT('',(59.0909744035184,10.1934949265222,10.));
#17437=CARTESIAN_POINT('',(59.0909744035184,5.09674746326108,10.));
#17438=CARTESIAN_POINT('',(59.0909744035184,10.1934949265222,12.));
#17439=CARTESIAN_POINT('',(59.0909744035184,5.09674746326108,12.));
#17440=CARTESIAN_POINT('',(59.0909744035184,10.1934949265222,12.));
#17441=CARTESIAN_POINT('Origin',(57.5909744035184,10.1934949265222,12.));
#17442=CARTESIAN_POINT('Origin',(57.5909744035184,10.1934949265222,10.));
#17443=CARTESIAN_POINT('Origin',(57.5909744035184,10.1934949265222,12.));
#17444=CARTESIAN_POINT('Origin',(32.3529750970072,11.70240347792,12.));
#17445=CARTESIAN_POINT('',(34.8529750970072,11.70240347792,12.));
#17446=CARTESIAN_POINT('Origin',(32.3529750970072,11.70240347792,12.));
#17447=CARTESIAN_POINT('',(34.8529750970072,11.70240347792,10.));
#17448=CARTESIAN_POINT('',(34.8529750970072,11.70240347792,12.));
#17449=CARTESIAN_POINT('Origin',(32.3529750970072,11.70240347792,10.));
#17450=CARTESIAN_POINT('Origin',(5.94008482114076,38.29759652208,12.));
#17451=CARTESIAN_POINT('',(8.44008482114076,38.29759652208,12.));
#17452=CARTESIAN_POINT('Origin',(5.94008482114076,38.29759652208,12.));
#17453=CARTESIAN_POINT('',(8.44008482114076,38.29759652208,10.));
#17454=CARTESIAN_POINT('',(8.44008482114076,38.29759652208,12.));
#17455=CARTESIAN_POINT('Origin',(5.94008482114076,38.29759652208,10.));
#17456=CARTESIAN_POINT('Origin',(17.646529959074,39.8065050734778,12.));
#17457=CARTESIAN_POINT('',(17.646529959074,44.7051656728289,10.));
#17458=CARTESIAN_POINT('',(17.646529959074,39.8065050734778,10.));
#17459=CARTESIAN_POINT('',(17.646529959074,19.9032525367389,10.));
#17460=CARTESIAN_POINT('',(17.646529959074,44.7051656728289,12.));
#17461=CARTESIAN_POINT('',(17.646529959074,44.7051656728289,12.));
#17462=CARTESIAN_POINT('',(17.646529959074,39.8065050734778,12.));
#17463=CARTESIAN_POINT('',(17.646529959074,19.9032525367389,12.));
#17464=CARTESIAN_POINT('',(17.646529959074,39.8065050734778,12.));
#17465=CARTESIAN_POINT('Origin',(19.146529959074,39.8065050734778,12.));
#17466=CARTESIAN_POINT('',(20.646529959074,39.8065050734778,10.));
#17467=CARTESIAN_POINT('Origin',(19.146529959074,39.8065050734778,10.));
#17468=CARTESIAN_POINT('',(20.646529959074,39.8065050734778,12.));
#17469=CARTESIAN_POINT('Origin',(19.146529959074,39.8065050734778,12.));
#17470=CARTESIAN_POINT('',(20.646529959074,39.8065050734778,12.));
#17471=CARTESIAN_POINT('Origin',(20.646529959074,44.7051656728289,12.));
#17472=CARTESIAN_POINT('',(20.646529959074,44.7051656728289,10.));
#17473=CARTESIAN_POINT('',(20.6465299590739,22.3525828364145,10.));
#17474=CARTESIAN_POINT('',(20.646529959074,44.7051656728289,12.));
#17475=CARTESIAN_POINT('',(20.646529959074,22.3525828364145,12.));
#17476=CARTESIAN_POINT('',(20.646529959074,44.7051656728289,12.));
#17477=CARTESIAN_POINT('Origin',(19.146529959074,44.7051656728289,12.));
#17478=CARTESIAN_POINT('Origin',(19.146529959074,44.7051656728289,10.));
#17479=CARTESIAN_POINT('Origin',(19.146529959074,44.7051656728289,12.));
#17480=CARTESIAN_POINT('Origin',(17.646529959074,5.29483432717106,12.));
#17481=CARTESIAN_POINT('',(17.646529959074,10.1934949265222,10.));
#17482=CARTESIAN_POINT('',(17.646529959074,5.29483432717106,10.));
#17483=CARTESIAN_POINT('',(17.646529959074,2.64741716358553,10.));
#17484=CARTESIAN_POINT('',(17.646529959074,10.1934949265222,12.));
#17485=CARTESIAN_POINT('',(17.646529959074,10.1934949265222,12.));
#17486=CARTESIAN_POINT('',(17.646529959074,5.29483432717106,12.));
#17487=CARTESIAN_POINT('',(17.646529959074,2.64741716358553,12.));
#17488=CARTESIAN_POINT('',(17.646529959074,5.29483432717106,12.));
#17489=CARTESIAN_POINT('Origin',(19.146529959074,5.29483432717106,12.));
#17490=CARTESIAN_POINT('',(20.646529959074,5.29483432717106,10.));
#17491=CARTESIAN_POINT('Origin',(19.146529959074,5.29483432717106,10.));
#17492=CARTESIAN_POINT('',(20.646529959074,5.29483432717106,12.));
#17493=CARTESIAN_POINT('Origin',(19.146529959074,5.29483432717106,12.));
#17494=CARTESIAN_POINT('',(20.646529959074,5.29483432717106,12.));
#17495=CARTESIAN_POINT('Origin',(20.646529959074,10.1934949265222,12.));
#17496=CARTESIAN_POINT('',(20.646529959074,10.1934949265222,10.));
#17497=CARTESIAN_POINT('',(20.6465299590739,5.09674746326108,10.));
#17498=CARTESIAN_POINT('',(20.646529959074,10.1934949265222,12.));
#17499=CARTESIAN_POINT('',(20.646529959074,5.09674746326108,12.));
#17500=CARTESIAN_POINT('',(20.646529959074,10.1934949265222,12.));
#17501=CARTESIAN_POINT('Origin',(19.146529959074,10.1934949265222,12.));
#17502=CARTESIAN_POINT('Origin',(19.146529959074,10.1934949265222,10.));
#17503=CARTESIAN_POINT('Origin',(19.146529959074,10.1934949265222,12.));
#17504=CARTESIAN_POINT('Origin',(19.146529959074,25.,12.));
#17505=CARTESIAN_POINT('',(29.146529959074,25.,12.));
#17506=CARTESIAN_POINT('Origin',(19.146529959074,25.,12.));
#17507=CARTESIAN_POINT('',(29.146529959074,25.,10.));
#17508=CARTESIAN_POINT('',(29.146529959074,25.,12.));
#17509=CARTESIAN_POINT('Origin',(19.146529959074,25.,10.));
#17510=CARTESIAN_POINT('Origin',(32.3529750970072,38.29759652208,12.));
#17511=CARTESIAN_POINT('',(34.8529750970072,38.29759652208,12.));
#17512=CARTESIAN_POINT('Origin',(32.3529750970072,38.29759652208,12.));
#17513=CARTESIAN_POINT('',(34.8529750970072,38.29759652208,10.));
#17514=CARTESIAN_POINT('',(34.8529750970072,38.29759652208,12.));
#17515=CARTESIAN_POINT('Origin',(32.3529750970072,38.29759652208,10.));
#17516=CARTESIAN_POINT('Origin',(5.94008482114076,11.70240347792,12.));
#17517=CARTESIAN_POINT('',(8.44008482114076,11.70240347792,12.));
#17518=CARTESIAN_POINT('Origin',(5.94008482114076,11.70240347792,12.));
#17519=CARTESIAN_POINT('',(8.44008482114076,11.70240347792,10.));
#17520=CARTESIAN_POINT('',(8.44008482114076,11.70240347792,12.));
#17521=CARTESIAN_POINT('Origin',(5.94008482114076,11.70240347792,10.));
#17522=CARTESIAN_POINT('Origin',(288.,2.5,9.5));
#17523=CARTESIAN_POINT('',(0.,2.,9.5));
#17524=CARTESIAN_POINT('',(0.,2.5,10.));
#17525=CARTESIAN_POINT('Origin',(0.,2.5,9.5));
#17526=CARTESIAN_POINT('',(384.,2.5,10.));
#17527=CARTESIAN_POINT('',(288.,2.5,10.));
#17528=CARTESIAN_POINT('',(384.,2.,9.5));
#17529=CARTESIAN_POINT('Origin',(384.,2.5,9.5));
#17530=CARTESIAN_POINT('',(288.,2.,9.5));
#17531=CARTESIAN_POINT('Origin',(384.,0.,10.));
#17532=CARTESIAN_POINT('',(0.,47.5,10.));
#17533=CARTESIAN_POINT('',(0.,0.,10.));
#17534=CARTESIAN_POINT('',(384.,47.5,10.));
#17535=CARTESIAN_POINT('',(288.,47.5,10.));
#17536=CARTESIAN_POINT('',(384.,0.,10.));
#17537=CARTESIAN_POINT('Origin',(288.,47.5,9.5));
#17538=CARTESIAN_POINT('',(0.,48.,9.5));
#17539=CARTESIAN_POINT('Origin',(0.,47.5,9.5));
#17540=CARTESIAN_POINT('',(384.,48.,9.5));
#17541=CARTESIAN_POINT('',(288.,48.,9.5));
#17542=CARTESIAN_POINT('Origin',(384.,47.5,9.5));
#17543=CARTESIAN_POINT('Origin',(192.,48.,5.));
#17544=CARTESIAN_POINT('',(0.,48.,0.));
#17545=CARTESIAN_POINT('',(0.,48.,12.));
#17546=CARTESIAN_POINT('',(384.,48.,0.));
#17547=CARTESIAN_POINT('',(0.,48.,0.));
#17548=CARTESIAN_POINT('',(384.,48.,0.));
#17549=CARTESIAN_POINT('',(6.02178569715406,48.,3.89451831659521));
#17550=CARTESIAN_POINT('Origin',(8.02178569715406,48.,3.89451831659521));
#17551=CARTESIAN_POINT('',(302.021785697154,48.,3.89451831659521));
#17552=CARTESIAN_POINT('Origin',(304.021785697154,48.,3.89451831659521));
#17553=CARTESIAN_POINT('',(358.021785697154,48.,3.89451831659521));
#17554=CARTESIAN_POINT('Origin',(360.021785697154,48.,3.89451831659521));
#17555=CARTESIAN_POINT('',(206.021785697154,48.,3.89451831659521));
#17556=CARTESIAN_POINT('Origin',(208.021785697154,48.,3.89451831659521));
#17557=CARTESIAN_POINT('',(374.021785697154,48.,3.89451831659521));
#17558=CARTESIAN_POINT('Origin',(376.021785697154,48.,3.89451831659521));
#17559=CARTESIAN_POINT('',(14.0217856971541,48.,3.89451831659521));
#17560=CARTESIAN_POINT('Origin',(16.0217856971541,48.,3.89451831659521));
#17561=CARTESIAN_POINT('',(182.021785697154,48.,3.89451831659521));
#17562=CARTESIAN_POINT('Origin',(184.021785697154,48.,3.89451831659521));
#17563=CARTESIAN_POINT('',(118.021785697154,48.,3.89451831659521));
#17564=CARTESIAN_POINT('Origin',(120.021785697154,48.,3.89451831659521));
#17565=CARTESIAN_POINT('',(126.021785697154,48.,3.89451831659521));
#17566=CARTESIAN_POINT('Origin',(128.021785697154,48.,3.89451831659521));
#17567=CARTESIAN_POINT('',(278.021785697154,48.,3.89451831659521));
#17568=CARTESIAN_POINT('Origin',(280.021785697154,48.,3.89451831659521));
#17569=CARTESIAN_POINT('',(94.0217856971541,48.,3.89451831659521));
#17570=CARTESIAN_POINT('Origin',(96.0217856971541,48.,3.89451831659521));
#17571=CARTESIAN_POINT('',(198.021785697154,48.,3.89451831659521));
#17572=CARTESIAN_POINT('Origin',(200.021785697154,48.,3.89451831659521));
#17573=CARTESIAN_POINT('',(70.0217856971541,48.,3.89451831659521));
#17574=CARTESIAN_POINT('Origin',(72.0217856971541,48.,3.89451831659521));
#17575=CARTESIAN_POINT('',(214.021785697154,48.,3.89451831659521));
#17576=CARTESIAN_POINT('Origin',(216.021785697154,48.,3.89451831659521));
#17577=CARTESIAN_POINT('',(246.021785697154,48.,3.89451831659521));
#17578=CARTESIAN_POINT('Origin',(248.021785697154,48.,3.89451831659521));
#17579=CARTESIAN_POINT('',(78.0217856971541,48.,3.89451831659521));
#17580=CARTESIAN_POINT('Origin',(80.0217856971541,48.,3.89451831659521));
#17581=CARTESIAN_POINT('',(262.021785697154,48.,3.89451831659521));
#17582=CARTESIAN_POINT('Origin',(264.021785697154,48.,3.89451831659521));
#17583=CARTESIAN_POINT('',(46.0217856971541,48.,3.89451831659521));
#17584=CARTESIAN_POINT('Origin',(48.0217856971541,48.,3.89451831659521));
#17585=CARTESIAN_POINT('',(30.0217856971541,48.,3.89451831659521));
#17586=CARTESIAN_POINT('Origin',(32.0217856971541,48.,3.89451831659521));
#17587=CARTESIAN_POINT('',(334.021785697154,48.,3.89451831659521));
#17588=CARTESIAN_POINT('Origin',(336.021785697154,48.,3.89451831659521));
#17589=CARTESIAN_POINT('',(38.0217856971541,48.,3.89451831659521));
#17590=CARTESIAN_POINT('Origin',(40.0217856971541,48.,3.89451831659521));
#17591=CARTESIAN_POINT('',(102.021785697154,48.,3.89451831659521));
#17592=CARTESIAN_POINT('Origin',(104.021785697154,48.,3.89451831659521));
#17593=CARTESIAN_POINT('',(62.0217856971541,48.,3.89451831659521));
#17594=CARTESIAN_POINT('Origin',(64.0217856971541,48.,3.89451831659521));
#17595=CARTESIAN_POINT('',(286.021785697154,48.,3.89451831659521));
#17596=CARTESIAN_POINT('Origin',(288.021785697154,48.,3.89451831659521));
#17597=CARTESIAN_POINT('',(134.021785697154,48.,3.89451831659521));
#17598=CARTESIAN_POINT('Origin',(136.021785697154,48.,3.89451831659521));
#17599=CARTESIAN_POINT('',(110.021785697154,48.,3.89451831659521));
#17600=CARTESIAN_POINT('Origin',(112.021785697154,48.,3.89451831659521));
#17601=CARTESIAN_POINT('',(174.021785697154,48.,3.89451831659521));
#17602=CARTESIAN_POINT('Origin',(176.021785697154,48.,3.89451831659521));
#17603=CARTESIAN_POINT('',(166.021785697154,48.,3.89451831659521));
#17604=CARTESIAN_POINT('Origin',(168.021785697154,48.,3.89451831659521));
#17605=CARTESIAN_POINT('',(158.021785697154,48.,3.89451831659521));
#17606=CARTESIAN_POINT('Origin',(160.021785697154,48.,3.89451831659521));
#17607=CARTESIAN_POINT('',(86.0217856971541,48.,3.89451831659521));
#17608=CARTESIAN_POINT('Origin',(88.0217856971541,48.,3.89451831659521));
#17609=CARTESIAN_POINT('',(22.0217856971541,48.,3.89451831659521));
#17610=CARTESIAN_POINT('Origin',(24.0217856971541,48.,3.89451831659521));
#17611=CARTESIAN_POINT('',(318.021785697154,48.,3.89451831659521));
#17612=CARTESIAN_POINT('Origin',(320.021785697154,48.,3.89451831659521));
#17613=CARTESIAN_POINT('',(190.021785697154,48.,3.89451831659521));
#17614=CARTESIAN_POINT('Origin',(192.021785697154,48.,3.89451831659521));
#17615=CARTESIAN_POINT('',(230.021785697154,48.,3.89451831659521));
#17616=CARTESIAN_POINT('Origin',(232.021785697154,48.,3.89451831659521));
#17617=CARTESIAN_POINT('',(270.021785697154,48.,3.89451831659521));
#17618=CARTESIAN_POINT('Origin',(272.021785697154,48.,3.89451831659521));
#17619=CARTESIAN_POINT('',(238.021785697154,48.,3.89451831659521));
#17620=CARTESIAN_POINT('Origin',(240.021785697154,48.,3.89451831659521));
#17621=CARTESIAN_POINT('',(54.0217856971541,48.,3.89451831659521));
#17622=CARTESIAN_POINT('Origin',(56.0217856971541,48.,3.89451831659521));
#17623=CARTESIAN_POINT('',(350.021785697154,48.,3.89451831659521));
#17624=CARTESIAN_POINT('Origin',(352.021785697154,48.,3.89451831659521));
#17625=CARTESIAN_POINT('',(342.021785697154,48.,3.89451831659521));
#17626=CARTESIAN_POINT('Origin',(344.021785697154,48.,3.89451831659521));
#17627=CARTESIAN_POINT('',(326.021785697154,48.,3.89451831659521));
#17628=CARTESIAN_POINT('Origin',(328.021785697154,48.,3.89451831659521));
#17629=CARTESIAN_POINT('',(142.021785697154,48.,3.89451831659521));
#17630=CARTESIAN_POINT('Origin',(144.021785697154,48.,3.89451831659521));
#17631=CARTESIAN_POINT('',(150.021785697154,48.,3.89451831659521));
#17632=CARTESIAN_POINT('Origin',(152.021785697154,48.,3.89451831659521));
#17633=CARTESIAN_POINT('',(254.021785697154,48.,3.89451831659521));
#17634=CARTESIAN_POINT('Origin',(256.021785697154,48.,3.89451831659521));
#17635=CARTESIAN_POINT('',(366.021785697154,48.,3.89451831659521));
#17636=CARTESIAN_POINT('Origin',(368.021785697154,48.,3.89451831659521));
#17637=CARTESIAN_POINT('',(294.021785697154,48.,3.89451831659521));
#17638=CARTESIAN_POINT('Origin',(296.021785697154,48.,3.89451831659521));
#17639=CARTESIAN_POINT('',(222.021785697154,48.,3.89451831659521));
#17640=CARTESIAN_POINT('Origin',(224.021785697154,48.,3.89451831659521));
#17641=CARTESIAN_POINT('',(310.021785697154,48.,3.89451831659521));
#17642=CARTESIAN_POINT('Origin',(312.021785697154,48.,3.89451831659521));
#17643=CARTESIAN_POINT('Origin',(96.,48.,10.));
#17644=CARTESIAN_POINT('',(384.,48.,12.));
#17645=CARTESIAN_POINT('',(384.,50.,10.));
#17646=CARTESIAN_POINT('Origin',(384.,48.,10.));
#17647=CARTESIAN_POINT('',(0.,50.,10.));
#17648=CARTESIAN_POINT('',(96.,50.,10.));
#17649=CARTESIAN_POINT('',(0.,48.,12.));
#17650=CARTESIAN_POINT('Origin',(0.,48.,10.));
#17651=CARTESIAN_POINT('',(96.,48.,12.));
#17652=CARTESIAN_POINT('Origin',(0.,0.,12.));
#17653=CARTESIAN_POINT('',(0.,2.,12.));
#17654=CARTESIAN_POINT('',(0.,0.,12.));
#17655=CARTESIAN_POINT('',(384.,2.,12.));
#17656=CARTESIAN_POINT('',(96.,2.,12.));
#17657=CARTESIAN_POINT('',(384.,0.,12.));
#17658=CARTESIAN_POINT('Origin',(0.,0.,0.));
#17659=CARTESIAN_POINT('',(0.,50.,0.));
#17660=CARTESIAN_POINT('',(0.,50.,12.));
#17661=CARTESIAN_POINT('',(0.,48.,0.));
#17662=CARTESIAN_POINT('',(0.,2.,0.));
#17663=CARTESIAN_POINT('',(0.,2.,12.));
#17664=CARTESIAN_POINT('',(0.,0.,0.));
#17665=CARTESIAN_POINT('',(0.,0.,0.));
#17666=CARTESIAN_POINT('',(0.,0.,10.));
#17667=CARTESIAN_POINT('',(0.,0.,12.));
#17668=CARTESIAN_POINT('Origin',(0.,2.,10.));
#17669=CARTESIAN_POINT('Origin',(96.,2.,10.));
#17670=CARTESIAN_POINT('',(384.,0.,10.));
#17671=CARTESIAN_POINT('Origin',(384.,2.,10.));
#17672=CARTESIAN_POINT('',(96.,0.,10.));
#17673=CARTESIAN_POINT('Origin',(8.02178569715406,48.,3.89451831659521));
#17674=CARTESIAN_POINT('',(6.02178569715406,50.,3.89451831659521));
#17675=CARTESIAN_POINT('Origin',(8.02178569715406,50.,3.89451831659521));
#17676=CARTESIAN_POINT('',(6.02178569715406,48.,3.89451831659521));
#17677=CARTESIAN_POINT('Origin',(304.021785697154,48.,3.89451831659521));
#17678=CARTESIAN_POINT('',(302.021785697154,50.,3.89451831659521));
#17679=CARTESIAN_POINT('Origin',(304.021785697154,50.,3.89451831659521));
#17680=CARTESIAN_POINT('',(302.021785697154,48.,3.89451831659521));
#17681=CARTESIAN_POINT('Origin',(360.021785697154,48.,3.89451831659521));
#17682=CARTESIAN_POINT('',(358.021785697154,50.,3.89451831659521));
#17683=CARTESIAN_POINT('Origin',(360.021785697154,50.,3.89451831659521));
#17684=CARTESIAN_POINT('',(358.021785697154,48.,3.89451831659521));
#17685=CARTESIAN_POINT('Origin',(208.021785697154,48.,3.89451831659521));
#17686=CARTESIAN_POINT('',(206.021785697154,50.,3.89451831659521));
#17687=CARTESIAN_POINT('Origin',(208.021785697154,50.,3.89451831659521));
#17688=CARTESIAN_POINT('',(206.021785697154,48.,3.89451831659521));
#17689=CARTESIAN_POINT('Origin',(376.021785697154,48.,3.89451831659521));
#17690=CARTESIAN_POINT('',(374.021785697154,50.,3.89451831659521));
#17691=CARTESIAN_POINT('Origin',(376.021785697154,50.,3.89451831659521));
#17692=CARTESIAN_POINT('',(374.021785697154,48.,3.89451831659521));
#17693=CARTESIAN_POINT('Origin',(16.0217856971541,48.,3.89451831659521));
#17694=CARTESIAN_POINT('',(14.0217856971541,50.,3.89451831659521));
#17695=CARTESIAN_POINT('Origin',(16.0217856971541,50.,3.89451831659521));
#17696=CARTESIAN_POINT('',(14.0217856971541,48.,3.89451831659521));
#17697=CARTESIAN_POINT('Origin',(184.021785697154,48.,3.89451831659521));
#17698=CARTESIAN_POINT('',(182.021785697154,50.,3.89451831659521));
#17699=CARTESIAN_POINT('Origin',(184.021785697154,50.,3.89451831659521));
#17700=CARTESIAN_POINT('',(182.021785697154,48.,3.89451831659521));
#17701=CARTESIAN_POINT('Origin',(120.021785697154,48.,3.89451831659521));
#17702=CARTESIAN_POINT('',(118.021785697154,50.,3.89451831659521));
#17703=CARTESIAN_POINT('Origin',(120.021785697154,50.,3.89451831659521));
#17704=CARTESIAN_POINT('',(118.021785697154,48.,3.89451831659521));
#17705=CARTESIAN_POINT('Origin',(128.021785697154,48.,3.89451831659521));
#17706=CARTESIAN_POINT('',(126.021785697154,50.,3.89451831659521));
#17707=CARTESIAN_POINT('Origin',(128.021785697154,50.,3.89451831659521));
#17708=CARTESIAN_POINT('',(126.021785697154,48.,3.89451831659521));
#17709=CARTESIAN_POINT('Origin',(280.021785697154,48.,3.89451831659521));
#17710=CARTESIAN_POINT('',(278.021785697154,50.,3.89451831659521));
#17711=CARTESIAN_POINT('Origin',(280.021785697154,50.,3.89451831659521));
#17712=CARTESIAN_POINT('',(278.021785697154,48.,3.89451831659521));
#17713=CARTESIAN_POINT('Origin',(96.0217856971541,48.,3.89451831659521));
#17714=CARTESIAN_POINT('',(94.0217856971541,50.,3.89451831659521));
#17715=CARTESIAN_POINT('Origin',(96.0217856971541,50.,3.89451831659521));
#17716=CARTESIAN_POINT('',(94.0217856971541,48.,3.89451831659521));
#17717=CARTESIAN_POINT('Origin',(200.021785697154,48.,3.89451831659521));
#17718=CARTESIAN_POINT('',(198.021785697154,50.,3.89451831659521));
#17719=CARTESIAN_POINT('Origin',(200.021785697154,50.,3.89451831659521));
#17720=CARTESIAN_POINT('',(198.021785697154,48.,3.89451831659521));
#17721=CARTESIAN_POINT('Origin',(72.0217856971541,48.,3.89451831659521));
#17722=CARTESIAN_POINT('',(70.0217856971541,50.,3.89451831659521));
#17723=CARTESIAN_POINT('Origin',(72.0217856971541,50.,3.89451831659521));
#17724=CARTESIAN_POINT('',(70.0217856971541,48.,3.89451831659521));
#17725=CARTESIAN_POINT('Origin',(216.021785697154,48.,3.89451831659521));
#17726=CARTESIAN_POINT('',(214.021785697154,50.,3.89451831659521));
#17727=CARTESIAN_POINT('Origin',(216.021785697154,50.,3.89451831659521));
#17728=CARTESIAN_POINT('',(214.021785697154,48.,3.89451831659521));
#17729=CARTESIAN_POINT('Origin',(248.021785697154,48.,3.89451831659521));
#17730=CARTESIAN_POINT('',(246.021785697154,50.,3.89451831659521));
#17731=CARTESIAN_POINT('Origin',(248.021785697154,50.,3.89451831659521));
#17732=CARTESIAN_POINT('',(246.021785697154,48.,3.89451831659521));
#17733=CARTESIAN_POINT('Origin',(80.0217856971541,48.,3.89451831659521));
#17734=CARTESIAN_POINT('',(78.0217856971541,50.,3.89451831659521));
#17735=CARTESIAN_POINT('Origin',(80.0217856971541,50.,3.89451831659521));
#17736=CARTESIAN_POINT('',(78.0217856971541,48.,3.89451831659521));
#17737=CARTESIAN_POINT('Origin',(264.021785697154,48.,3.89451831659521));
#17738=CARTESIAN_POINT('',(262.021785697154,50.,3.89451831659521));
#17739=CARTESIAN_POINT('Origin',(264.021785697154,50.,3.89451831659521));
#17740=CARTESIAN_POINT('',(262.021785697154,48.,3.89451831659521));
#17741=CARTESIAN_POINT('Origin',(48.0217856971541,48.,3.89451831659521));
#17742=CARTESIAN_POINT('',(46.0217856971541,50.,3.89451831659521));
#17743=CARTESIAN_POINT('Origin',(48.0217856971541,50.,3.89451831659521));
#17744=CARTESIAN_POINT('',(46.0217856971541,48.,3.89451831659521));
#17745=CARTESIAN_POINT('Origin',(32.0217856971541,48.,3.89451831659521));
#17746=CARTESIAN_POINT('',(30.0217856971541,50.,3.89451831659521));
#17747=CARTESIAN_POINT('Origin',(32.0217856971541,50.,3.89451831659521));
#17748=CARTESIAN_POINT('',(30.0217856971541,48.,3.89451831659521));
#17749=CARTESIAN_POINT('Origin',(336.021785697154,48.,3.89451831659521));
#17750=CARTESIAN_POINT('',(334.021785697154,50.,3.89451831659521));
#17751=CARTESIAN_POINT('Origin',(336.021785697154,50.,3.89451831659521));
#17752=CARTESIAN_POINT('',(334.021785697154,48.,3.89451831659521));
#17753=CARTESIAN_POINT('Origin',(40.0217856971541,48.,3.89451831659521));
#17754=CARTESIAN_POINT('',(38.0217856971541,50.,3.89451831659521));
#17755=CARTESIAN_POINT('Origin',(40.0217856971541,50.,3.89451831659521));
#17756=CARTESIAN_POINT('',(38.0217856971541,48.,3.89451831659521));
#17757=CARTESIAN_POINT('Origin',(104.021785697154,48.,3.89451831659521));
#17758=CARTESIAN_POINT('',(102.021785697154,50.,3.89451831659521));
#17759=CARTESIAN_POINT('Origin',(104.021785697154,50.,3.89451831659521));
#17760=CARTESIAN_POINT('',(102.021785697154,48.,3.89451831659521));
#17761=CARTESIAN_POINT('Origin',(64.0217856971541,48.,3.89451831659521));
#17762=CARTESIAN_POINT('',(62.0217856971541,50.,3.89451831659521));
#17763=CARTESIAN_POINT('Origin',(64.0217856971541,50.,3.89451831659521));
#17764=CARTESIAN_POINT('',(62.0217856971541,48.,3.89451831659521));
#17765=CARTESIAN_POINT('Origin',(288.021785697154,48.,3.89451831659521));
#17766=CARTESIAN_POINT('',(286.021785697154,50.,3.89451831659521));
#17767=CARTESIAN_POINT('Origin',(288.021785697154,50.,3.89451831659521));
#17768=CARTESIAN_POINT('',(286.021785697154,48.,3.89451831659521));
#17769=CARTESIAN_POINT('Origin',(136.021785697154,48.,3.89451831659521));
#17770=CARTESIAN_POINT('',(134.021785697154,50.,3.89451831659521));
#17771=CARTESIAN_POINT('Origin',(136.021785697154,50.,3.89451831659521));
#17772=CARTESIAN_POINT('',(134.021785697154,48.,3.89451831659521));
#17773=CARTESIAN_POINT('Origin',(112.021785697154,48.,3.89451831659521));
#17774=CARTESIAN_POINT('',(110.021785697154,50.,3.89451831659521));
#17775=CARTESIAN_POINT('Origin',(112.021785697154,50.,3.89451831659521));
#17776=CARTESIAN_POINT('',(110.021785697154,48.,3.89451831659521));
#17777=CARTESIAN_POINT('Origin',(176.021785697154,48.,3.89451831659521));
#17778=CARTESIAN_POINT('',(174.021785697154,50.,3.89451831659521));
#17779=CARTESIAN_POINT('Origin',(176.021785697154,50.,3.89451831659521));
#17780=CARTESIAN_POINT('',(174.021785697154,48.,3.89451831659521));
#17781=CARTESIAN_POINT('Origin',(168.021785697154,48.,3.89451831659521));
#17782=CARTESIAN_POINT('',(166.021785697154,50.,3.89451831659521));
#17783=CARTESIAN_POINT('Origin',(168.021785697154,50.,3.89451831659521));
#17784=CARTESIAN_POINT('',(166.021785697154,48.,3.89451831659521));
#17785=CARTESIAN_POINT('Origin',(160.021785697154,48.,3.89451831659521));
#17786=CARTESIAN_POINT('',(158.021785697154,50.,3.89451831659521));
#17787=CARTESIAN_POINT('Origin',(160.021785697154,50.,3.89451831659521));
#17788=CARTESIAN_POINT('',(158.021785697154,48.,3.89451831659521));
#17789=CARTESIAN_POINT('Origin',(88.0217856971541,48.,3.89451831659521));
#17790=CARTESIAN_POINT('',(86.0217856971541,50.,3.89451831659521));
#17791=CARTESIAN_POINT('Origin',(88.0217856971541,50.,3.89451831659521));
#17792=CARTESIAN_POINT('',(86.0217856971541,48.,3.89451831659521));
#17793=CARTESIAN_POINT('Origin',(24.0217856971541,48.,3.89451831659521));
#17794=CARTESIAN_POINT('',(22.0217856971541,50.,3.89451831659521));
#17795=CARTESIAN_POINT('Origin',(24.0217856971541,50.,3.89451831659521));
#17796=CARTESIAN_POINT('',(22.0217856971541,48.,3.89451831659521));
#17797=CARTESIAN_POINT('Origin',(320.021785697154,48.,3.89451831659521));
#17798=CARTESIAN_POINT('',(318.021785697154,50.,3.89451831659521));
#17799=CARTESIAN_POINT('Origin',(320.021785697154,50.,3.89451831659521));
#17800=CARTESIAN_POINT('',(318.021785697154,48.,3.89451831659521));
#17801=CARTESIAN_POINT('Origin',(192.021785697154,48.,3.89451831659521));
#17802=CARTESIAN_POINT('',(190.021785697154,50.,3.89451831659521));
#17803=CARTESIAN_POINT('Origin',(192.021785697154,50.,3.89451831659521));
#17804=CARTESIAN_POINT('',(190.021785697154,48.,3.89451831659521));
#17805=CARTESIAN_POINT('Origin',(232.021785697154,48.,3.89451831659521));
#17806=CARTESIAN_POINT('',(230.021785697154,50.,3.89451831659521));
#17807=CARTESIAN_POINT('Origin',(232.021785697154,50.,3.89451831659521));
#17808=CARTESIAN_POINT('',(230.021785697154,48.,3.89451831659521));
#17809=CARTESIAN_POINT('Origin',(272.021785697154,48.,3.89451831659521));
#17810=CARTESIAN_POINT('',(270.021785697154,50.,3.89451831659521));
#17811=CARTESIAN_POINT('Origin',(272.021785697154,50.,3.89451831659521));
#17812=CARTESIAN_POINT('',(270.021785697154,48.,3.89451831659521));
#17813=CARTESIAN_POINT('Origin',(240.021785697154,48.,3.89451831659521));
#17814=CARTESIAN_POINT('',(238.021785697154,50.,3.89451831659521));
#17815=CARTESIAN_POINT('Origin',(240.021785697154,50.,3.89451831659521));
#17816=CARTESIAN_POINT('',(238.021785697154,48.,3.89451831659521));
#17817=CARTESIAN_POINT('Origin',(56.0217856971541,48.,3.89451831659521));
#17818=CARTESIAN_POINT('',(54.0217856971541,50.,3.89451831659521));
#17819=CARTESIAN_POINT('Origin',(56.0217856971541,50.,3.89451831659521));
#17820=CARTESIAN_POINT('',(54.0217856971541,48.,3.89451831659521));
#17821=CARTESIAN_POINT('Origin',(352.021785697154,48.,3.89451831659521));
#17822=CARTESIAN_POINT('',(350.021785697154,50.,3.89451831659521));
#17823=CARTESIAN_POINT('Origin',(352.021785697154,50.,3.89451831659521));
#17824=CARTESIAN_POINT('',(350.021785697154,48.,3.89451831659521));
#17825=CARTESIAN_POINT('Origin',(344.021785697154,48.,3.89451831659521));
#17826=CARTESIAN_POINT('',(342.021785697154,50.,3.89451831659521));
#17827=CARTESIAN_POINT('Origin',(344.021785697154,50.,3.89451831659521));
#17828=CARTESIAN_POINT('',(342.021785697154,48.,3.89451831659521));
#17829=CARTESIAN_POINT('Origin',(328.021785697154,48.,3.89451831659521));
#17830=CARTESIAN_POINT('',(326.021785697154,50.,3.89451831659521));
#17831=CARTESIAN_POINT('Origin',(328.021785697154,50.,3.89451831659521));
#17832=CARTESIAN_POINT('',(326.021785697154,48.,3.89451831659521));
#17833=CARTESIAN_POINT('Origin',(144.021785697154,48.,3.89451831659521));
#17834=CARTESIAN_POINT('',(142.021785697154,50.,3.89451831659521));
#17835=CARTESIAN_POINT('Origin',(144.021785697154,50.,3.89451831659521));
#17836=CARTESIAN_POINT('',(142.021785697154,48.,3.89451831659521));
#17837=CARTESIAN_POINT('Origin',(152.021785697154,48.,3.89451831659521));
#17838=CARTESIAN_POINT('',(150.021785697154,50.,3.89451831659521));
#17839=CARTESIAN_POINT('Origin',(152.021785697154,50.,3.89451831659521));
#17840=CARTESIAN_POINT('',(150.021785697154,48.,3.89451831659521));
#17841=CARTESIAN_POINT('Origin',(256.021785697154,48.,3.89451831659521));
#17842=CARTESIAN_POINT('',(254.021785697154,50.,3.89451831659521));
#17843=CARTESIAN_POINT('Origin',(256.021785697154,50.,3.89451831659521));
#17844=CARTESIAN_POINT('',(254.021785697154,48.,3.89451831659521));
#17845=CARTESIAN_POINT('Origin',(368.021785697154,48.,3.89451831659521));
#17846=CARTESIAN_POINT('',(366.021785697154,50.,3.89451831659521));
#17847=CARTESIAN_POINT('Origin',(368.021785697154,50.,3.89451831659521));
#17848=CARTESIAN_POINT('',(366.021785697154,48.,3.89451831659521));
#17849=CARTESIAN_POINT('Origin',(296.021785697154,48.,3.89451831659521));
#17850=CARTESIAN_POINT('',(294.021785697154,50.,3.89451831659521));
#17851=CARTESIAN_POINT('Origin',(296.021785697154,50.,3.89451831659521));
#17852=CARTESIAN_POINT('',(294.021785697154,48.,3.89451831659521));
#17853=CARTESIAN_POINT('Origin',(224.021785697154,48.,3.89451831659521));
#17854=CARTESIAN_POINT('',(222.021785697154,50.,3.89451831659521));
#17855=CARTESIAN_POINT('Origin',(224.021785697154,50.,3.89451831659521));
#17856=CARTESIAN_POINT('',(222.021785697154,48.,3.89451831659521));
#17857=CARTESIAN_POINT('Origin',(312.021785697154,48.,3.89451831659521));
#17858=CARTESIAN_POINT('',(310.021785697154,50.,3.89451831659521));
#17859=CARTESIAN_POINT('Origin',(312.021785697154,50.,3.89451831659521));
#17860=CARTESIAN_POINT('',(310.021785697154,48.,3.89451831659521));
#17861=CARTESIAN_POINT('Origin',(384.,48.,0.));
#17862=CARTESIAN_POINT('',(384.,50.,0.));
#17863=CARTESIAN_POINT('',(0.,50.,0.));
#17864=CARTESIAN_POINT('',(384.,48.,0.));
#17865=CARTESIAN_POINT('Origin',(192.,50.,11.));
#17866=CARTESIAN_POINT('',(384.,50.,12.));
#17867=CARTESIAN_POINT('Origin',(8.02178569715406,0.,3.89451831659521));
#17868=CARTESIAN_POINT('',(6.02178569715406,2.,3.89451831659521));
#17869=CARTESIAN_POINT('Origin',(8.02178569715406,2.,3.89451831659521));
#17870=CARTESIAN_POINT('',(6.02178569715406,0.,3.89451831659521));
#17871=CARTESIAN_POINT('',(6.02178569715406,0.,3.89451831659521));
#17872=CARTESIAN_POINT('Origin',(8.02178569715406,0.,3.89451831659521));
#17873=CARTESIAN_POINT('Origin',(304.021785697154,0.,3.89451831659521));
#17874=CARTESIAN_POINT('',(302.021785697154,2.,3.89451831659521));
#17875=CARTESIAN_POINT('Origin',(304.021785697154,2.,3.89451831659521));
#17876=CARTESIAN_POINT('',(302.021785697154,0.,3.89451831659521));
#17877=CARTESIAN_POINT('',(302.021785697154,0.,3.89451831659521));
#17878=CARTESIAN_POINT('Origin',(304.021785697154,0.,3.89451831659521));
#17879=CARTESIAN_POINT('Origin',(360.021785697154,0.,3.89451831659521));
#17880=CARTESIAN_POINT('',(358.021785697154,2.,3.89451831659521));
#17881=CARTESIAN_POINT('Origin',(360.021785697154,2.,3.89451831659521));
#17882=CARTESIAN_POINT('',(358.021785697154,0.,3.89451831659521));
#17883=CARTESIAN_POINT('',(358.021785697154,0.,3.89451831659521));
#17884=CARTESIAN_POINT('Origin',(360.021785697154,0.,3.89451831659521));
#17885=CARTESIAN_POINT('Origin',(208.021785697154,0.,3.89451831659521));
#17886=CARTESIAN_POINT('',(206.021785697154,2.,3.89451831659521));
#17887=CARTESIAN_POINT('Origin',(208.021785697154,2.,3.89451831659521));
#17888=CARTESIAN_POINT('',(206.021785697154,0.,3.89451831659521));
#17889=CARTESIAN_POINT('',(206.021785697154,0.,3.89451831659521));
#17890=CARTESIAN_POINT('Origin',(208.021785697154,0.,3.89451831659521));
#17891=CARTESIAN_POINT('Origin',(376.021785697154,0.,3.89451831659521));
#17892=CARTESIAN_POINT('',(374.021785697154,2.,3.89451831659521));
#17893=CARTESIAN_POINT('Origin',(376.021785697154,2.,3.89451831659521));
#17894=CARTESIAN_POINT('',(374.021785697154,0.,3.89451831659521));
#17895=CARTESIAN_POINT('',(374.021785697154,0.,3.89451831659521));
#17896=CARTESIAN_POINT('Origin',(376.021785697154,0.,3.89451831659521));
#17897=CARTESIAN_POINT('Origin',(16.0217856971541,0.,3.89451831659521));
#17898=CARTESIAN_POINT('',(14.0217856971541,2.,3.89451831659521));
#17899=CARTESIAN_POINT('Origin',(16.0217856971541,2.,3.89451831659521));
#17900=CARTESIAN_POINT('',(14.0217856971541,0.,3.89451831659521));
#17901=CARTESIAN_POINT('',(14.0217856971541,0.,3.89451831659521));
#17902=CARTESIAN_POINT('Origin',(16.0217856971541,0.,3.89451831659521));
#17903=CARTESIAN_POINT('Origin',(184.021785697154,0.,3.89451831659521));
#17904=CARTESIAN_POINT('',(182.021785697154,2.,3.89451831659521));
#17905=CARTESIAN_POINT('Origin',(184.021785697154,2.,3.89451831659521));
#17906=CARTESIAN_POINT('',(182.021785697154,0.,3.89451831659521));
#17907=CARTESIAN_POINT('',(182.021785697154,0.,3.89451831659521));
#17908=CARTESIAN_POINT('Origin',(184.021785697154,0.,3.89451831659521));
#17909=CARTESIAN_POINT('Origin',(120.021785697154,0.,3.89451831659521));
#17910=CARTESIAN_POINT('',(118.021785697154,2.,3.89451831659521));
#17911=CARTESIAN_POINT('Origin',(120.021785697154,2.,3.89451831659521));
#17912=CARTESIAN_POINT('',(118.021785697154,0.,3.89451831659521));
#17913=CARTESIAN_POINT('',(118.021785697154,0.,3.89451831659521));
#17914=CARTESIAN_POINT('Origin',(120.021785697154,0.,3.89451831659521));
#17915=CARTESIAN_POINT('Origin',(128.021785697154,0.,3.89451831659521));
#17916=CARTESIAN_POINT('',(126.021785697154,2.,3.89451831659521));
#17917=CARTESIAN_POINT('Origin',(128.021785697154,2.,3.89451831659521));
#17918=CARTESIAN_POINT('',(126.021785697154,0.,3.89451831659521));
#17919=CARTESIAN_POINT('',(126.021785697154,0.,3.89451831659521));
#17920=CARTESIAN_POINT('Origin',(128.021785697154,0.,3.89451831659521));
#17921=CARTESIAN_POINT('Origin',(280.021785697154,0.,3.89451831659521));
#17922=CARTESIAN_POINT('',(278.021785697154,2.,3.89451831659521));
#17923=CARTESIAN_POINT('Origin',(280.021785697154,2.,3.89451831659521));
#17924=CARTESIAN_POINT('',(278.021785697154,0.,3.89451831659521));
#17925=CARTESIAN_POINT('',(278.021785697154,0.,3.89451831659521));
#17926=CARTESIAN_POINT('Origin',(280.021785697154,0.,3.89451831659521));
#17927=CARTESIAN_POINT('Origin',(96.0217856971541,0.,3.89451831659521));
#17928=CARTESIAN_POINT('',(94.0217856971541,2.,3.89451831659521));
#17929=CARTESIAN_POINT('Origin',(96.0217856971541,2.,3.89451831659521));
#17930=CARTESIAN_POINT('',(94.0217856971541,0.,3.89451831659521));
#17931=CARTESIAN_POINT('',(94.0217856971541,0.,3.89451831659521));
#17932=CARTESIAN_POINT('Origin',(96.0217856971541,0.,3.89451831659521));
#17933=CARTESIAN_POINT('Origin',(200.021785697154,0.,3.89451831659521));
#17934=CARTESIAN_POINT('',(198.021785697154,2.,3.89451831659521));
#17935=CARTESIAN_POINT('Origin',(200.021785697154,2.,3.89451831659521));
#17936=CARTESIAN_POINT('',(198.021785697154,0.,3.89451831659521));
#17937=CARTESIAN_POINT('',(198.021785697154,0.,3.89451831659521));
#17938=CARTESIAN_POINT('Origin',(200.021785697154,0.,3.89451831659521));
#17939=CARTESIAN_POINT('Origin',(72.0217856971541,0.,3.89451831659521));
#17940=CARTESIAN_POINT('',(70.0217856971541,2.,3.89451831659521));
#17941=CARTESIAN_POINT('Origin',(72.0217856971541,2.,3.89451831659521));
#17942=CARTESIAN_POINT('',(70.0217856971541,0.,3.89451831659521));
#17943=CARTESIAN_POINT('',(70.0217856971541,0.,3.89451831659521));
#17944=CARTESIAN_POINT('Origin',(72.0217856971541,0.,3.89451831659521));
#17945=CARTESIAN_POINT('Origin',(216.021785697154,0.,3.89451831659521));
#17946=CARTESIAN_POINT('',(214.021785697154,2.,3.89451831659521));
#17947=CARTESIAN_POINT('Origin',(216.021785697154,2.,3.89451831659521));
#17948=CARTESIAN_POINT('',(214.021785697154,0.,3.89451831659521));
#17949=CARTESIAN_POINT('',(214.021785697154,0.,3.89451831659521));
#17950=CARTESIAN_POINT('Origin',(216.021785697154,0.,3.89451831659521));
#17951=CARTESIAN_POINT('Origin',(248.021785697154,0.,3.89451831659521));
#17952=CARTESIAN_POINT('',(246.021785697154,2.,3.89451831659521));
#17953=CARTESIAN_POINT('Origin',(248.021785697154,2.,3.89451831659521));
#17954=CARTESIAN_POINT('',(246.021785697154,0.,3.89451831659521));
#17955=CARTESIAN_POINT('',(246.021785697154,0.,3.89451831659521));
#17956=CARTESIAN_POINT('Origin',(248.021785697154,0.,3.89451831659521));
#17957=CARTESIAN_POINT('Origin',(80.0217856971541,0.,3.89451831659521));
#17958=CARTESIAN_POINT('',(78.0217856971541,2.,3.89451831659521));
#17959=CARTESIAN_POINT('Origin',(80.0217856971541,2.,3.89451831659521));
#17960=CARTESIAN_POINT('',(78.0217856971541,0.,3.89451831659521));
#17961=CARTESIAN_POINT('',(78.0217856971541,0.,3.89451831659521));
#17962=CARTESIAN_POINT('Origin',(80.0217856971541,0.,3.89451831659521));
#17963=CARTESIAN_POINT('Origin',(264.021785697154,0.,3.89451831659521));
#17964=CARTESIAN_POINT('',(262.021785697154,2.,3.89451831659521));
#17965=CARTESIAN_POINT('Origin',(264.021785697154,2.,3.89451831659521));
#17966=CARTESIAN_POINT('',(262.021785697154,0.,3.89451831659521));
#17967=CARTESIAN_POINT('',(262.021785697154,0.,3.89451831659521));
#17968=CARTESIAN_POINT('Origin',(264.021785697154,0.,3.89451831659521));
#17969=CARTESIAN_POINT('Origin',(48.0217856971541,0.,3.89451831659521));
#17970=CARTESIAN_POINT('',(46.0217856971541,2.,3.89451831659521));
#17971=CARTESIAN_POINT('Origin',(48.0217856971541,2.,3.89451831659521));
#17972=CARTESIAN_POINT('',(46.0217856971541,0.,3.89451831659521));
#17973=CARTESIAN_POINT('',(46.0217856971541,0.,3.89451831659521));
#17974=CARTESIAN_POINT('Origin',(48.0217856971541,0.,3.89451831659521));
#17975=CARTESIAN_POINT('Origin',(32.0217856971541,0.,3.89451831659521));
#17976=CARTESIAN_POINT('',(30.0217856971541,2.,3.89451831659521));
#17977=CARTESIAN_POINT('Origin',(32.0217856971541,2.,3.89451831659521));
#17978=CARTESIAN_POINT('',(30.0217856971541,0.,3.89451831659521));
#17979=CARTESIAN_POINT('',(30.0217856971541,0.,3.89451831659521));
#17980=CARTESIAN_POINT('Origin',(32.0217856971541,0.,3.89451831659521));
#17981=CARTESIAN_POINT('Origin',(336.021785697154,0.,3.89451831659521));
#17982=CARTESIAN_POINT('',(334.021785697154,2.,3.89451831659521));
#17983=CARTESIAN_POINT('Origin',(336.021785697154,2.,3.89451831659521));
#17984=CARTESIAN_POINT('',(334.021785697154,0.,3.89451831659521));
#17985=CARTESIAN_POINT('',(334.021785697154,0.,3.89451831659521));
#17986=CARTESIAN_POINT('Origin',(336.021785697154,0.,3.89451831659521));
#17987=CARTESIAN_POINT('Origin',(40.0217856971541,0.,3.89451831659521));
#17988=CARTESIAN_POINT('',(38.0217856971541,2.,3.89451831659521));
#17989=CARTESIAN_POINT('Origin',(40.0217856971541,2.,3.89451831659521));
#17990=CARTESIAN_POINT('',(38.0217856971541,0.,3.89451831659521));
#17991=CARTESIAN_POINT('',(38.0217856971541,0.,3.89451831659521));
#17992=CARTESIAN_POINT('Origin',(40.0217856971541,0.,3.89451831659521));
#17993=CARTESIAN_POINT('Origin',(104.021785697154,0.,3.89451831659521));
#17994=CARTESIAN_POINT('',(102.021785697154,2.,3.89451831659521));
#17995=CARTESIAN_POINT('Origin',(104.021785697154,2.,3.89451831659521));
#17996=CARTESIAN_POINT('',(102.021785697154,0.,3.89451831659521));
#17997=CARTESIAN_POINT('',(102.021785697154,0.,3.89451831659521));
#17998=CARTESIAN_POINT('Origin',(104.021785697154,0.,3.89451831659521));
#17999=CARTESIAN_POINT('Origin',(64.0217856971541,0.,3.89451831659521));
#18000=CARTESIAN_POINT('',(62.0217856971541,2.,3.89451831659521));
#18001=CARTESIAN_POINT('Origin',(64.0217856971541,2.,3.89451831659521));
#18002=CARTESIAN_POINT('',(62.0217856971541,0.,3.89451831659521));
#18003=CARTESIAN_POINT('',(62.0217856971541,0.,3.89451831659521));
#18004=CARTESIAN_POINT('Origin',(64.0217856971541,0.,3.89451831659521));
#18005=CARTESIAN_POINT('Origin',(288.021785697154,0.,3.89451831659521));
#18006=CARTESIAN_POINT('',(286.021785697154,2.,3.89451831659521));
#18007=CARTESIAN_POINT('Origin',(288.021785697154,2.,3.89451831659521));
#18008=CARTESIAN_POINT('',(286.021785697154,0.,3.89451831659521));
#18009=CARTESIAN_POINT('',(286.021785697154,0.,3.89451831659521));
#18010=CARTESIAN_POINT('Origin',(288.021785697154,0.,3.89451831659521));
#18011=CARTESIAN_POINT('Origin',(136.021785697154,0.,3.89451831659521));
#18012=CARTESIAN_POINT('',(134.021785697154,2.,3.89451831659521));
#18013=CARTESIAN_POINT('Origin',(136.021785697154,2.,3.89451831659521));
#18014=CARTESIAN_POINT('',(134.021785697154,0.,3.89451831659521));
#18015=CARTESIAN_POINT('',(134.021785697154,0.,3.89451831659521));
#18016=CARTESIAN_POINT('Origin',(136.021785697154,0.,3.89451831659521));
#18017=CARTESIAN_POINT('Origin',(112.021785697154,0.,3.89451831659521));
#18018=CARTESIAN_POINT('',(110.021785697154,2.,3.89451831659521));
#18019=CARTESIAN_POINT('Origin',(112.021785697154,2.,3.89451831659521));
#18020=CARTESIAN_POINT('',(110.021785697154,0.,3.89451831659521));
#18021=CARTESIAN_POINT('',(110.021785697154,0.,3.89451831659521));
#18022=CARTESIAN_POINT('Origin',(112.021785697154,0.,3.89451831659521));
#18023=CARTESIAN_POINT('Origin',(176.021785697154,0.,3.89451831659521));
#18024=CARTESIAN_POINT('',(174.021785697154,2.,3.89451831659521));
#18025=CARTESIAN_POINT('Origin',(176.021785697154,2.,3.89451831659521));
#18026=CARTESIAN_POINT('',(174.021785697154,0.,3.89451831659521));
#18027=CARTESIAN_POINT('',(174.021785697154,0.,3.89451831659521));
#18028=CARTESIAN_POINT('Origin',(176.021785697154,0.,3.89451831659521));
#18029=CARTESIAN_POINT('Origin',(168.021785697154,0.,3.89451831659521));
#18030=CARTESIAN_POINT('',(166.021785697154,2.,3.89451831659521));
#18031=CARTESIAN_POINT('Origin',(168.021785697154,2.,3.89451831659521));
#18032=CARTESIAN_POINT('',(166.021785697154,0.,3.89451831659521));
#18033=CARTESIAN_POINT('',(166.021785697154,0.,3.89451831659521));
#18034=CARTESIAN_POINT('Origin',(168.021785697154,0.,3.89451831659521));
#18035=CARTESIAN_POINT('Origin',(160.021785697154,0.,3.89451831659521));
#18036=CARTESIAN_POINT('',(158.021785697154,2.,3.89451831659521));
#18037=CARTESIAN_POINT('Origin',(160.021785697154,2.,3.89451831659521));
#18038=CARTESIAN_POINT('',(158.021785697154,0.,3.89451831659521));
#18039=CARTESIAN_POINT('',(158.021785697154,0.,3.89451831659521));
#18040=CARTESIAN_POINT('Origin',(160.021785697154,0.,3.89451831659521));
#18041=CARTESIAN_POINT('Origin',(88.0217856971541,0.,3.89451831659521));
#18042=CARTESIAN_POINT('',(86.0217856971541,2.,3.89451831659521));
#18043=CARTESIAN_POINT('Origin',(88.0217856971541,2.,3.89451831659521));
#18044=CARTESIAN_POINT('',(86.0217856971541,0.,3.89451831659521));
#18045=CARTESIAN_POINT('',(86.0217856971541,0.,3.89451831659521));
#18046=CARTESIAN_POINT('Origin',(88.0217856971541,0.,3.89451831659521));
#18047=CARTESIAN_POINT('Origin',(24.0217856971541,0.,3.89451831659521));
#18048=CARTESIAN_POINT('',(22.0217856971541,2.,3.89451831659521));
#18049=CARTESIAN_POINT('Origin',(24.0217856971541,2.,3.89451831659521));
#18050=CARTESIAN_POINT('',(22.0217856971541,0.,3.89451831659521));
#18051=CARTESIAN_POINT('',(22.0217856971541,0.,3.89451831659521));
#18052=CARTESIAN_POINT('Origin',(24.0217856971541,0.,3.89451831659521));
#18053=CARTESIAN_POINT('Origin',(320.021785697154,0.,3.89451831659521));
#18054=CARTESIAN_POINT('',(318.021785697154,2.,3.89451831659521));
#18055=CARTESIAN_POINT('Origin',(320.021785697154,2.,3.89451831659521));
#18056=CARTESIAN_POINT('',(318.021785697154,0.,3.89451831659521));
#18057=CARTESIAN_POINT('',(318.021785697154,0.,3.89451831659521));
#18058=CARTESIAN_POINT('Origin',(320.021785697154,0.,3.89451831659521));
#18059=CARTESIAN_POINT('Origin',(192.021785697154,0.,3.89451831659521));
#18060=CARTESIAN_POINT('',(190.021785697154,2.,3.89451831659521));
#18061=CARTESIAN_POINT('Origin',(192.021785697154,2.,3.89451831659521));
#18062=CARTESIAN_POINT('',(190.021785697154,0.,3.89451831659521));
#18063=CARTESIAN_POINT('',(190.021785697154,0.,3.89451831659521));
#18064=CARTESIAN_POINT('Origin',(192.021785697154,0.,3.89451831659521));
#18065=CARTESIAN_POINT('Origin',(232.021785697154,0.,3.89451831659521));
#18066=CARTESIAN_POINT('',(230.021785697154,2.,3.89451831659521));
#18067=CARTESIAN_POINT('Origin',(232.021785697154,2.,3.89451831659521));
#18068=CARTESIAN_POINT('',(230.021785697154,0.,3.89451831659521));
#18069=CARTESIAN_POINT('',(230.021785697154,0.,3.89451831659521));
#18070=CARTESIAN_POINT('Origin',(232.021785697154,0.,3.89451831659521));
#18071=CARTESIAN_POINT('Origin',(272.021785697154,0.,3.89451831659521));
#18072=CARTESIAN_POINT('',(270.021785697154,2.,3.89451831659521));
#18073=CARTESIAN_POINT('Origin',(272.021785697154,2.,3.89451831659521));
#18074=CARTESIAN_POINT('',(270.021785697154,0.,3.89451831659521));
#18075=CARTESIAN_POINT('',(270.021785697154,0.,3.89451831659521));
#18076=CARTESIAN_POINT('Origin',(272.021785697154,0.,3.89451831659521));
#18077=CARTESIAN_POINT('Origin',(240.021785697154,0.,3.89451831659521));
#18078=CARTESIAN_POINT('',(238.021785697154,2.,3.89451831659521));
#18079=CARTESIAN_POINT('Origin',(240.021785697154,2.,3.89451831659521));
#18080=CARTESIAN_POINT('',(238.021785697154,0.,3.89451831659521));
#18081=CARTESIAN_POINT('',(238.021785697154,0.,3.89451831659521));
#18082=CARTESIAN_POINT('Origin',(240.021785697154,0.,3.89451831659521));
#18083=CARTESIAN_POINT('Origin',(56.0217856971541,0.,3.89451831659521));
#18084=CARTESIAN_POINT('',(54.0217856971541,2.,3.89451831659521));
#18085=CARTESIAN_POINT('Origin',(56.0217856971541,2.,3.89451831659521));
#18086=CARTESIAN_POINT('',(54.0217856971541,0.,3.89451831659521));
#18087=CARTESIAN_POINT('',(54.0217856971541,0.,3.89451831659521));
#18088=CARTESIAN_POINT('Origin',(56.0217856971541,0.,3.89451831659521));
#18089=CARTESIAN_POINT('Origin',(352.021785697154,0.,3.89451831659521));
#18090=CARTESIAN_POINT('',(350.021785697154,2.,3.89451831659521));
#18091=CARTESIAN_POINT('Origin',(352.021785697154,2.,3.89451831659521));
#18092=CARTESIAN_POINT('',(350.021785697154,0.,3.89451831659521));
#18093=CARTESIAN_POINT('',(350.021785697154,0.,3.89451831659521));
#18094=CARTESIAN_POINT('Origin',(352.021785697154,0.,3.89451831659521));
#18095=CARTESIAN_POINT('Origin',(344.021785697154,0.,3.89451831659521));
#18096=CARTESIAN_POINT('',(342.021785697154,2.,3.89451831659521));
#18097=CARTESIAN_POINT('Origin',(344.021785697154,2.,3.89451831659521));
#18098=CARTESIAN_POINT('',(342.021785697154,0.,3.89451831659521));
#18099=CARTESIAN_POINT('',(342.021785697154,0.,3.89451831659521));
#18100=CARTESIAN_POINT('Origin',(344.021785697154,0.,3.89451831659521));
#18101=CARTESIAN_POINT('Origin',(328.021785697154,0.,3.89451831659521));
#18102=CARTESIAN_POINT('',(326.021785697154,2.,3.89451831659521));
#18103=CARTESIAN_POINT('Origin',(328.021785697154,2.,3.89451831659521));
#18104=CARTESIAN_POINT('',(326.021785697154,0.,3.89451831659521));
#18105=CARTESIAN_POINT('',(326.021785697154,0.,3.89451831659521));
#18106=CARTESIAN_POINT('Origin',(328.021785697154,0.,3.89451831659521));
#18107=CARTESIAN_POINT('Origin',(144.021785697154,0.,3.89451831659521));
#18108=CARTESIAN_POINT('',(142.021785697154,2.,3.89451831659521));
#18109=CARTESIAN_POINT('Origin',(144.021785697154,2.,3.89451831659521));
#18110=CARTESIAN_POINT('',(142.021785697154,0.,3.89451831659521));
#18111=CARTESIAN_POINT('',(142.021785697154,0.,3.89451831659521));
#18112=CARTESIAN_POINT('Origin',(144.021785697154,0.,3.89451831659521));
#18113=CARTESIAN_POINT('Origin',(152.021785697154,0.,3.89451831659521));
#18114=CARTESIAN_POINT('',(150.021785697154,2.,3.89451831659521));
#18115=CARTESIAN_POINT('Origin',(152.021785697154,2.,3.89451831659521));
#18116=CARTESIAN_POINT('',(150.021785697154,0.,3.89451831659521));
#18117=CARTESIAN_POINT('',(150.021785697154,0.,3.89451831659521));
#18118=CARTESIAN_POINT('Origin',(152.021785697154,0.,3.89451831659521));
#18119=CARTESIAN_POINT('Origin',(256.021785697154,0.,3.89451831659521));
#18120=CARTESIAN_POINT('',(254.021785697154,2.,3.89451831659521));
#18121=CARTESIAN_POINT('Origin',(256.021785697154,2.,3.89451831659521));
#18122=CARTESIAN_POINT('',(254.021785697154,0.,3.89451831659521));
#18123=CARTESIAN_POINT('',(254.021785697154,0.,3.89451831659521));
#18124=CARTESIAN_POINT('Origin',(256.021785697154,0.,3.89451831659521));
#18125=CARTESIAN_POINT('Origin',(368.021785697154,0.,3.89451831659521));
#18126=CARTESIAN_POINT('',(366.021785697154,2.,3.89451831659521));
#18127=CARTESIAN_POINT('Origin',(368.021785697154,2.,3.89451831659521));
#18128=CARTESIAN_POINT('',(366.021785697154,0.,3.89451831659521));
#18129=CARTESIAN_POINT('',(366.021785697154,0.,3.89451831659521));
#18130=CARTESIAN_POINT('Origin',(368.021785697154,0.,3.89451831659521));
#18131=CARTESIAN_POINT('Origin',(296.021785697154,0.,3.89451831659521));
#18132=CARTESIAN_POINT('',(294.021785697154,2.,3.89451831659521));
#18133=CARTESIAN_POINT('Origin',(296.021785697154,2.,3.89451831659521));
#18134=CARTESIAN_POINT('',(294.021785697154,0.,3.89451831659521));
#18135=CARTESIAN_POINT('',(294.021785697154,0.,3.89451831659521));
#18136=CARTESIAN_POINT('Origin',(296.021785697154,0.,3.89451831659521));
#18137=CARTESIAN_POINT('Origin',(224.021785697154,0.,3.89451831659521));
#18138=CARTESIAN_POINT('',(222.021785697154,2.,3.89451831659521));
#18139=CARTESIAN_POINT('Origin',(224.021785697154,2.,3.89451831659521));
#18140=CARTESIAN_POINT('',(222.021785697154,0.,3.89451831659521));
#18141=CARTESIAN_POINT('',(222.021785697154,0.,3.89451831659521));
#18142=CARTESIAN_POINT('Origin',(224.021785697154,0.,3.89451831659521));
#18143=CARTESIAN_POINT('Origin',(312.021785697154,0.,3.89451831659521));
#18144=CARTESIAN_POINT('',(310.021785697154,2.,3.89451831659521));
#18145=CARTESIAN_POINT('Origin',(312.021785697154,2.,3.89451831659521));
#18146=CARTESIAN_POINT('',(310.021785697154,0.,3.89451831659521));
#18147=CARTESIAN_POINT('',(310.021785697154,0.,3.89451831659521));
#18148=CARTESIAN_POINT('Origin',(312.021785697154,0.,3.89451831659521));
#18149=CARTESIAN_POINT('Origin',(384.,0.,0.));
#18150=CARTESIAN_POINT('',(384.,0.,0.));
#18151=CARTESIAN_POINT('',(0.,0.,0.));
#18152=CARTESIAN_POINT('',(384.,2.,0.));
#18153=CARTESIAN_POINT('',(0.,2.,0.));
#18154=CARTESIAN_POINT('',(384.,0.,0.));
#18155=CARTESIAN_POINT('Origin',(384.,0.,10.));
#18156=CARTESIAN_POINT('',(384.,0.,0.));
#18157=CARTESIAN_POINT('',(384.,2.,0.));
#18158=CARTESIAN_POINT('Origin',(192.,2.,5.));
#18159=CARTESIAN_POINT('Origin',(192.,0.,5.));
#19195=UNCERTAINTY_MEASURE_WITH_UNIT(LENGTH_MEASURE(0.01),#19221,
'DISTANCE_ACCURACY_VALUE',
'Maximum model space distance between geometric entities at asserted c
onnectivities');
#19204=UNCERTAINTY_MEASURE_WITH_UNIT(LENGTH_MEASURE(0.01),#19221,
'DISTANCE_ACCURACY_VALUE',
'Maximum model space distance between geometric entities at asserted c
onnectivities');
#19211=(
GEOMETRIC_REPRESENTATION_CONTEXT(3)
GLOBAL_UNCERTAINTY_ASSIGNED_CONTEXT((#19195))
GLOBAL_UNIT_ASSIGNED_CONTEXT((#19221,#19223,#19224))
REPRESENTATION_CONTEXT('','3D')
);
#19220=(
GEOMETRIC_REPRESENTATION_CONTEXT(3)
GLOBAL_UNCERTAINTY_ASSIGNED_CONTEXT((#19204))
GLOBAL_UNIT_ASSIGNED_CONTEXT((#19221,#19223,#19224))
REPRESENTATION_CONTEXT('','3D')
);
#19221=(
LENGTH_UNIT()
NAMED_UNIT(*)
SI_UNIT(.MILLI.,.METRE.)
);
#19223=(
NAMED_UNIT(*)
PLANE_ANGLE_UNIT()
SI_UNIT($,.RADIAN.)
);
#19224=(
NAMED_UNIT(*)
SI_UNIT($,.STERADIAN.)
SOLID_ANGLE_UNIT()
);
#19231=SHAPE_DEFINITION_REPRESENTATION(#19246,#19275);
#19246=PRODUCT_DEFINITION_SHAPE('',$,#19291);
#19275=SHAPE_REPRESENTATION('',(#11759),#19211);
#19284=PRODUCT_DEFINITION_CONTEXT('part definition',#19331,'design');
#19291=PRODUCT_DEFINITION('Base (1)','Base (1)',#19306,#19284);
#19306=PRODUCT_DEFINITION_FORMATION('',$,#19339);
#19331=APPLICATION_CONTEXT(
'Core Data for Automotive Mechanical Design Process');
#19332=PRODUCT_CONTEXT('part definition',#19331,'mechanical');
#19339=PRODUCT('Base (1)','Base (1)',$,(#19332));
#19376=COLOUR_RGB('Dark Blue',0.08,0.2,0.34);
#19377=FILL_AREA_STYLE_COLOUR('',#19376);
#19378=FILL_AREA_STYLE('',(#19377));
#19379=SURFACE_STYLE_FILL_AREA(#19378);
#19380=SURFACE_SIDE_STYLE('',(#19379));
#19381=SURFACE_STYLE_USAGE(.BOTH.,#19380);
#19382=PRESENTATION_STYLE_ASSIGNMENT((#19381));
ENDSEC;
END-ISO-10303-21;
